ISO-10303-21;
HEADER;
/* Generated by software containing ST-Developer
 * from STEP Tools, Inc. (www.steptools.com) 
 */

FILE_DESCRIPTION(
/* description */ ('Independent hinged machine back cover with retained hinge pins, perim
eter gasket and quarter-turn cam latch. Nominal cover 360 x 260 x 3 mm
, frame 430 x 300 x 20 mm. No guarding, structural or ingress rating a
ssigned.'),
/* implementation_level */ '2;1');

FILE_NAME(
/* name */ 'Socket head cap screw M6x20.step',
/* time_stamp */ '2026-11-09T19:36:59-08:00',
/* author */ (''),
/* organization */ (''),
/* preprocessor_version */ 'ST-DEVELOPER v20.2',
/* originating_system */ 'Autodesk Translation Framework v15.17.0.0',
/* authorisation */ '');

FILE_SCHEMA (('AUTOMOTIVE_DESIGN { 1 0 10303 214 3 1 1 }'));
ENDSEC;

DATA;
#10=MECHANICAL_DESIGN_GEOMETRIC_PRESENTATION_REPRESENTATION('',(#212),#32627);
#160=CONICAL_SURFACE('',#9395,2.5,0.785398163397448);
#176=SHAPE_REPRESENTATION_RELATIONSHIP('SRR','None',#32722,#194);
#194=ADVANCED_BREP_SHAPE_REPRESENTATION('',(#230),#32623);
#212=STYLED_ITEM('',(#32809),#230);
#230=MANIFOLD_SOLID_BREP('Body1',#8689);
#285=FACE_BOUND('',#1386,.T.);
#286=FACE_BOUND('',#1389,.T.);
#305=B_SPLINE_SURFACE_WITH_KNOTS('',3,3,((#28103,#28104,#28105,#28106,#28107,
#28108,#28109,#28110,#28111,#28112,#28113,#28114,#28115,#28116,#28117,#28118,
#28119,#28120,#28121,#28122,#28123,#28124,#28125,#28126,#28127,#28128,#28129,
#28130,#28131,#28132,#28133,#28134,#28135,#28136,#28137,#28138,#28139,#28140,
#28141,#28142,#28143,#28144,#28145,#28146,#28147,#28148,#28149,#28150,#28151,
#28152,#28153,#28154,#28155,#28156,#28157,#28158,#28159,#28160,#28161,#28162,
#28163,#28164,#28165,#28166,#28167,#28168,#28169,#28170,#28171,#28172,#28173,
#28174,#28175,#28176,#28177,#28178,#28179,#28180,#28181,#28182,#28183,#28184,
#28185,#28186,#28187,#28188,#28189,#28190,#28191,#28192,#28193,#28194,#28195,
#28196,#28197,#28198,#28199,#28200,#28201,#28202,#28203,#28204,#28205,#28206,
#28207,#28208,#28209,#28210,#28211,#28212,#28213,#28214,#28215,#28216,#28217,
#28218,#28219,#28220,#28221,#28222,#28223,#28224,#28225,#28226,#28227,#28228,
#28229),(#28230,#28231,#28232,#28233,#28234,#28235,#28236,#28237,#28238,
#28239,#28240,#28241,#28242,#28243,#28244,#28245,#28246,#28247,#28248,#28249,
#28250,#28251,#28252,#28253,#28254,#28255,#28256,#28257,#28258,#28259,#28260,
#28261,#28262,#28263,#28264,#28265,#28266,#28267,#28268,#28269,#28270,#28271,
#28272,#28273,#28274,#28275,#28276,#28277,#28278,#28279,#28280,#28281,#28282,
#28283,#28284,#28285,#28286,#28287,#28288,#28289,#28290,#28291,#28292,#28293,
#28294,#28295,#28296,#28297,#28298,#28299,#28300,#28301,#28302,#28303,#28304,
#28305,#28306,#28307,#28308,#28309,#28310,#28311,#28312,#28313,#28314,#28315,
#28316,#28317,#28318,#28319,#28320,#28321,#28322,#28323,#28324,#28325,#28326,
#28327,#28328,#28329,#28330,#28331,#28332,#28333,#28334,#28335,#28336,#28337,
#28338,#28339,#28340,#28341,#28342,#28343,#28344,#28345,#28346,#28347,#28348,
#28349,#28350,#28351,#28352,#28353,#28354,#28355,#28356),(#28357,#28358,
#28359,#28360,#28361,#28362,#28363,#28364,#28365,#28366,#28367,#28368,#28369,
#28370,#28371,#28372,#28373,#28374,#28375,#28376,#28377,#28378,#28379,#28380,
#28381,#28382,#28383,#28384,#28385,#28386,#28387,#28388,#28389,#28390,#28391,
#28392,#28393,#28394,#28395,#28396,#28397,#28398,#28399,#28400,#28401,#28402,
#28403,#28404,#28405,#28406,#28407,#28408,#28409,#28410,#28411,#28412,#28413,
#28414,#28415,#28416,#28417,#28418,#28419,#28420,#28421,#28422,#28423,#28424,
#28425,#28426,#28427,#28428,#28429,#28430,#28431,#28432,#28433,#28434,#28435,
#28436,#28437,#28438,#28439,#28440,#28441,#28442,#28443,#28444,#28445,#28446,
#28447,#28448,#28449,#28450,#28451,#28452,#28453,#28454,#28455,#28456,#28457,
#28458,#28459,#28460,#28461,#28462,#28463,#28464,#28465,#28466,#28467,#28468,
#28469,#28470,#28471,#28472,#28473,#28474,#28475,#28476,#28477,#28478,#28479,
#28480,#28481,#28482,#28483),(#28484,#28485,#28486,#28487,#28488,#28489,
#28490,#28491,#28492,#28493,#28494,#28495,#28496,#28497,#28498,#28499,#28500,
#28501,#28502,#28503,#28504,#28505,#28506,#28507,#28508,#28509,#28510,#28511,
#28512,#28513,#28514,#28515,#28516,#28517,#28518,#28519,#28520,#28521,#28522,
#28523,#28524,#28525,#28526,#28527,#28528,#28529,#28530,#28531,#28532,#28533,
#28534,#28535,#28536,#28537,#28538,#28539,#28540,#28541,#28542,#28543,#28544,
#28545,#28546,#28547,#28548,#28549,#28550,#28551,#28552,#28553,#28554,#28555,
#28556,#28557,#28558,#28559,#28560,#28561,#28562,#28563,#28564,#28565,#28566,
#28567,#28568,#28569,#28570,#28571,#28572,#28573,#28574,#28575,#28576,#28577,
#28578,#28579,#28580,#28581,#28582,#28583,#28584,#28585,#28586,#28587,#28588,
#28589,#28590,#28591,#28592,#28593,#28594,#28595,#28596,#28597,#28598,#28599,
#28600,#28601,#28602,#28603,#28604,#28605,#28606,#28607,#28608,#28609,#28610)),
 .UNSPECIFIED.,.F.,.F.,.F.,(4,4),(4,1,1,1,1,1,1,1,1,1,1,1,1,1,1,1,1,1,1,
1,1,1,1,1,1,1,1,1,1,1,1,1,1,1,1,1,1,1,1,1,1,1,1,1,1,1,1,1,1,1,1,1,1,1,1,
1,1,1,1,1,1,1,1,1,1,1,1,1,1,1,1,1,1,1,1,1,1,1,1,1,1,1,1,1,1,1,1,1,1,1,1,
1,1,1,1,1,1,1,1,1,1,1,1,1,1,1,1,1,1,1,1,1,1,1,1,1,1,1,1,1,1,1,1,1,4),(0.,
0.0658467982010768),(11.6150328478182,12.609612944638,13.6041930414577,
14.5987731382775,15.5933532350972,16.5879333319169,17.5825134287367,18.5770935255564,
19.5716736223762,20.5662537191959,21.5608338160156,22.5554139128354,23.5499940096551,
24.5445741064749,25.5391542032946,26.5337343001143,27.5283143969341,28.5228944937538,
29.5174745905736,30.5120546873933,31.506634784213,32.5012148810328,33.4957949778525,
34.4903750746723,35.484955171492,36.4795352683117,37.4741153651315,38.4686954619512,
39.463275558771,40.4578556555907,41.4524357524104,42.4470158492302,43.4415959460499,
44.4361760428697,45.4307561396894,46.4253362365091,47.4199163333289,48.4144964301486,
49.4090765269684,50.4036566237881,51.3982367206078,52.3928168174276,53.3873969142473,
54.3819770110671,55.3765571078868,56.3711372047065,57.3657173015263,58.360297398346,
59.3548774951657,60.3494575919855,61.3440376888052,62.338617785625,63.3331978824447,
64.3277779792645,65.3223580760842,66.3169381729039,67.3115182697237,68.3060983665434,
69.3006784633631,70.2952585601829,71.2898386570026,72.2844187538224,73.2789988506421,
74.2735789474618,75.2681590442816,76.2627391411013,77.2573192379211,78.2518993347408,
79.2464794315605,80.2410595283803,81.2356396252,82.2302197220198,83.2247998188395,
84.2193799156592,85.213960012479,86.2085401092987,87.2031202061185,88.1977003029382,
89.1922803997579,90.1868604965777,91.1814405933974,92.1760206902171,93.1706007870369,
94.1651808838566,95.1597609806764,96.1543410774961,97.1489211743159,98.1435012711356,
99.1380813679553,100.132661464775,101.127241561595,102.121821658415,103.116401755234,
104.110981852054,105.105561948874,106.100142045694,107.094722142513,108.089302239333,
109.083882336153,110.078462432972,111.073042529792,112.067622626612,113.062202723432,
114.056782820251,115.051362917071,116.045943013891,117.040523110711,118.03510320753,
119.02968330435,120.02426340117,121.01884349799,122.013423594809,123.008003691629,
124.002583788449,124.997163885269,125.991743982088,126.986324078908,127.980904175728,
128.975484272548,129.970064369367,130.964644466187,131.959224563007,132.953804659826,
133.948384756646,134.942964853466),.UNSPECIFIED.);
#306=B_SPLINE_SURFACE_WITH_KNOTS('',3,3,((#28742,#28743,#28744,#28745,#28746,
#28747,#28748,#28749,#28750,#28751,#28752,#28753,#28754,#28755,#28756,#28757,
#28758,#28759,#28760,#28761,#28762,#28763,#28764,#28765,#28766,#28767,#28768,
#28769,#28770,#28771,#28772,#28773,#28774,#28775,#28776,#28777,#28778,#28779,
#28780,#28781,#28782,#28783,#28784,#28785,#28786,#28787,#28788,#28789,#28790,
#28791,#28792,#28793,#28794,#28795,#28796,#28797,#28798,#28799,#28800,#28801,
#28802,#28803,#28804,#28805,#28806,#28807,#28808,#28809,#28810,#28811,#28812,
#28813,#28814,#28815,#28816,#28817,#28818,#28819,#28820,#28821,#28822,#28823,
#28824,#28825,#28826,#28827,#28828,#28829,#28830,#28831,#28832,#28833,#28834,
#28835,#28836,#28837,#28838,#28839,#28840,#28841,#28842,#28843,#28844,#28845,
#28846,#28847,#28848,#28849,#28850,#28851,#28852,#28853,#28854,#28855,#28856,
#28857,#28858,#28859,#28860,#28861,#28862,#28863,#28864,#28865,#28866,#28867,
#28868,#28869,#28870),(#28871,#28872,#28873,#28874,#28875,#28876,#28877,
#28878,#28879,#28880,#28881,#28882,#28883,#28884,#28885,#28886,#28887,#28888,
#28889,#28890,#28891,#28892,#28893,#28894,#28895,#28896,#28897,#28898,#28899,
#28900,#28901,#28902,#28903,#28904,#28905,#28906,#28907,#28908,#28909,#28910,
#28911,#28912,#28913,#28914,#28915,#28916,#28917,#28918,#28919,#28920,#28921,
#28922,#28923,#28924,#28925,#28926,#28927,#28928,#28929,#28930,#28931,#28932,
#28933,#28934,#28935,#28936,#28937,#28938,#28939,#28940,#28941,#28942,#28943,
#28944,#28945,#28946,#28947,#28948,#28949,#28950,#28951,#28952,#28953,#28954,
#28955,#28956,#28957,#28958,#28959,#28960,#28961,#28962,#28963,#28964,#28965,
#28966,#28967,#28968,#28969,#28970,#28971,#28972,#28973,#28974,#28975,#28976,
#28977,#28978,#28979,#28980,#28981,#28982,#28983,#28984,#28985,#28986,#28987,
#28988,#28989,#28990,#28991,#28992,#28993,#28994,#28995,#28996,#28997,#28998,
#28999),(#29000,#29001,#29002,#29003,#29004,#29005,#29006,#29007,#29008,
#29009,#29010,#29011,#29012,#29013,#29014,#29015,#29016,#29017,#29018,#29019,
#29020,#29021,#29022,#29023,#29024,#29025,#29026,#29027,#29028,#29029,#29030,
#29031,#29032,#29033,#29034,#29035,#29036,#29037,#29038,#29039,#29040,#29041,
#29042,#29043,#29044,#29045,#29046,#29047,#29048,#29049,#29050,#29051,#29052,
#29053,#29054,#29055,#29056,#29057,#29058,#29059,#29060,#29061,#29062,#29063,
#29064,#29065,#29066,#29067,#29068,#29069,#29070,#29071,#29072,#29073,#29074,
#29075,#29076,#29077,#29078,#29079,#29080,#29081,#29082,#29083,#29084,#29085,
#29086,#29087,#29088,#29089,#29090,#29091,#29092,#29093,#29094,#29095,#29096,
#29097,#29098,#29099,#29100,#29101,#29102,#29103,#29104,#29105,#29106,#29107,
#29108,#29109,#29110,#29111,#29112,#29113,#29114,#29115,#29116,#29117,#29118,
#29119,#29120,#29121,#29122,#29123,#29124,#29125,#29126,#29127,#29128),
(#29129,#29130,#29131,#29132,#29133,#29134,#29135,#29136,#29137,#29138,
#29139,#29140,#29141,#29142,#29143,#29144,#29145,#29146,#29147,#29148,#29149,
#29150,#29151,#29152,#29153,#29154,#29155,#29156,#29157,#29158,#29159,#29160,
#29161,#29162,#29163,#29164,#29165,#29166,#29167,#29168,#29169,#29170,#29171,
#29172,#29173,#29174,#29175,#29176,#29177,#29178,#29179,#29180,#29181,#29182,
#29183,#29184,#29185,#29186,#29187,#29188,#29189,#29190,#29191,#29192,#29193,
#29194,#29195,#29196,#29197,#29198,#29199,#29200,#29201,#29202,#29203,#29204,
#29205,#29206,#29207,#29208,#29209,#29210,#29211,#29212,#29213,#29214,#29215,
#29216,#29217,#29218,#29219,#29220,#29221,#29222,#29223,#29224,#29225,#29226,
#29227,#29228,#29229,#29230,#29231,#29232,#29233,#29234,#29235,#29236,#29237,
#29238,#29239,#29240,#29241,#29242,#29243,#29244,#29245,#29246,#29247,#29248,
#29249,#29250,#29251,#29252,#29253,#29254,#29255,#29256,#29257)),
 .UNSPECIFIED.,.F.,.F.,.F.,(4,4),(4,1,1,1,1,1,1,1,1,1,1,1,1,1,1,1,1,1,1,
1,1,1,1,1,1,1,1,1,1,1,1,1,1,1,1,1,1,1,1,1,1,1,1,1,1,1,1,1,1,1,1,1,1,1,1,
1,1,1,1,1,1,1,1,1,1,1,1,1,1,1,1,1,1,1,1,1,1,1,1,1,1,1,1,1,1,1,1,1,1,1,1,
1,1,1,1,1,1,1,1,1,1,1,1,1,1,1,1,1,1,1,1,1,1,1,1,1,1,1,1,1,1,1,1,1,1,1,4),
(0.,0.0658467982010768),(8.30747755240104,9.3026884268499,10.2978993012988,
11.2931101757476,12.2883210501965,13.2835319246454,14.2787427990942,15.2739536735431,
16.2691645479919,17.2643754224408,18.2595862968897,19.2547971713385,20.2500080457874,
21.2452189202363,22.2404297946851,23.235640669134,24.2308515435829,25.2260624180317,
26.2212732924806,27.2164841669295,28.2116950413783,29.2069059158272,30.202116790276,
31.1973276647249,32.1925385391738,33.1877494136226,34.1829602880715,35.1781711625204,
36.1733820369692,37.1685929114181,38.163803785867,39.1590146603158,40.1542255347647,
41.1494364092135,42.1446472836624,43.1398581581113,44.1350690325601,45.130279907009,
46.1254907814579,47.1207016559067,48.1159125303556,49.1111234048045,50.1063342792533,
51.1015451537022,52.096756028151,53.0919669025999,54.0871777770488,55.0823886514976,
56.0775995259465,57.0728104003954,58.0680212748442,59.0632321492931,60.058443023742,
61.0536538981908,62.0488647726397,63.0440756470886,64.0392865215374,65.0344973959863,
66.0297082704352,67.024919144884,68.0201300193329,69.0153408937817,70.0105517682306,
71.0057626426795,72.0009735171283,72.9961843915772,73.9913952660261,74.9866061404749,
75.9818170149238,76.9770278893726,77.9722387638215,78.9674496382704,79.9626605127192,
80.9578713871681,81.953082261617,82.9482931360658,83.9435040105147,84.9387148849636,
85.9339257594124,86.9291366338613,87.9243475083101,88.919558382759,89.9147692572079,
90.9099801316567,91.9051910061056,92.9004018805545,93.8956127550033,94.8908236294522,
95.8860345039011,96.8812453783499,97.8764562527988,98.8716671272477,99.8668780016965,
100.862088876145,101.857299750594,102.852510625043,103.847721499492,104.842932373941,
105.83814324839,106.833354122839,107.828564997287,108.823775871736,109.818986746185,
110.814197620634,111.809408495083,112.804619369532,113.799830243981,114.795041118429,
115.790251992878,116.785462867327,117.780673741776,118.775884616225,119.771095490674,
120.766306365123,121.761517239572,122.75672811402,123.751938988469,124.747149862918,
125.742360737367,126.737571611816,127.732782486265,128.727993360714,129.723204235162,
130.718415109611,131.71362598406,132.708836858509,133.704047732958),
 .UNSPECIFIED.);
#422=PLANE('',#9401);
#423=PLANE('',#9402);
#424=PLANE('',#9403);
#425=PLANE('',#9404);
#426=PLANE('',#9405);
#427=PLANE('',#9406);
#428=PLANE('',#9407);
#429=PLANE('',#9408);
#430=PLANE('',#9412);
#431=PLANE('',#9413);
#809=FACE_OUTER_BOUND('',#1335,.T.);
#810=FACE_OUTER_BOUND('',#1336,.T.);
#811=FACE_OUTER_BOUND('',#1337,.T.);
#812=FACE_OUTER_BOUND('',#1338,.T.);
#813=FACE_OUTER_BOUND('',#1339,.T.);
#814=FACE_OUTER_BOUND('',#1340,.T.);
#815=FACE_OUTER_BOUND('',#1341,.T.);
#816=FACE_OUTER_BOUND('',#1342,.T.);
#817=FACE_OUTER_BOUND('',#1343,.T.);
#818=FACE_OUTER_BOUND('',#1344,.T.);
#819=FACE_OUTER_BOUND('',#1345,.T.);
#820=FACE_OUTER_BOUND('',#1346,.T.);
#821=FACE_OUTER_BOUND('',#1347,.T.);
#822=FACE_OUTER_BOUND('',#1348,.T.);
#823=FACE_OUTER_BOUND('',#1349,.T.);
#824=FACE_OUTER_BOUND('',#1350,.T.);
#825=FACE_OUTER_BOUND('',#1351,.T.);
#826=FACE_OUTER_BOUND('',#1352,.T.);
#827=FACE_OUTER_BOUND('',#1353,.T.);
#828=FACE_OUTER_BOUND('',#1354,.T.);
#829=FACE_OUTER_BOUND('',#1355,.T.);
#830=FACE_OUTER_BOUND('',#1356,.T.);
#831=FACE_OUTER_BOUND('',#1357,.T.);
#832=FACE_OUTER_BOUND('',#1358,.T.);
#833=FACE_OUTER_BOUND('',#1359,.T.);
#834=FACE_OUTER_BOUND('',#1360,.T.);
#835=FACE_OUTER_BOUND('',#1361,.T.);
#836=FACE_OUTER_BOUND('',#1362,.T.);
#837=FACE_OUTER_BOUND('',#1363,.T.);
#838=FACE_OUTER_BOUND('',#1364,.T.);
#839=FACE_OUTER_BOUND('',#1365,.T.);
#840=FACE_OUTER_BOUND('',#1366,.T.);
#841=FACE_OUTER_BOUND('',#1367,.T.);
#842=FACE_OUTER_BOUND('',#1368,.T.);
#843=FACE_OUTER_BOUND('',#1369,.T.);
#844=FACE_OUTER_BOUND('',#1370,.T.);
#845=FACE_OUTER_BOUND('',#1371,.T.);
#846=FACE_OUTER_BOUND('',#1372,.T.);
#847=FACE_OUTER_BOUND('',#1373,.T.);
#848=FACE_OUTER_BOUND('',#1374,.T.);
#849=FACE_OUTER_BOUND('',#1375,.T.);
#850=FACE_OUTER_BOUND('',#1376,.T.);
#851=FACE_OUTER_BOUND('',#1377,.T.);
#852=FACE_OUTER_BOUND('',#1378,.T.);
#853=FACE_OUTER_BOUND('',#1379,.T.);
#854=FACE_OUTER_BOUND('',#1380,.T.);
#855=FACE_OUTER_BOUND('',#1381,.T.);
#856=FACE_OUTER_BOUND('',#1382,.T.);
#857=FACE_OUTER_BOUND('',#1383,.T.);
#858=FACE_OUTER_BOUND('',#1384,.T.);
#859=FACE_OUTER_BOUND('',#1385,.T.);
#860=FACE_OUTER_BOUND('',#1387,.T.);
#861=FACE_OUTER_BOUND('',#1388,.T.);
#862=FACE_OUTER_BOUND('',#1390,.T.);
#1335=EDGE_LOOP('',(#7251,#7252,#7253,#7254));
#1336=EDGE_LOOP('',(#7255,#7256,#7257,#7258));
#1337=EDGE_LOOP('',(#7259,#7260,#7261,#7262));
#1338=EDGE_LOOP('',(#7263,#7264,#7265,#7266));
#1339=EDGE_LOOP('',(#7267,#7268,#7269,#7270));
#1340=EDGE_LOOP('',(#7271,#7272,#7273,#7274));
#1341=EDGE_LOOP('',(#7275,#7276,#7277,#7278));
#1342=EDGE_LOOP('',(#7279,#7280,#7281,#7282));
#1343=EDGE_LOOP('',(#7283,#7284,#7285,#7286));
#1344=EDGE_LOOP('',(#7287,#7288,#7289,#7290));
#1345=EDGE_LOOP('',(#7291,#7292,#7293,#7294));
#1346=EDGE_LOOP('',(#7295,#7296,#7297,#7298));
#1347=EDGE_LOOP('',(#7299,#7300,#7301,#7302));
#1348=EDGE_LOOP('',(#7303,#7304,#7305,#7306));
#1349=EDGE_LOOP('',(#7307,#7308,#7309,#7310));
#1350=EDGE_LOOP('',(#7311,#7312,#7313,#7314));
#1351=EDGE_LOOP('',(#7315,#7316,#7317,#7318));
#1352=EDGE_LOOP('',(#7319,#7320,#7321,#7322));
#1353=EDGE_LOOP('',(#7323,#7324,#7325,#7326));
#1354=EDGE_LOOP('',(#7327,#7328,#7329,#7330));
#1355=EDGE_LOOP('',(#7331,#7332,#7333,#7334));
#1356=EDGE_LOOP('',(#7335,#7336,#7337,#7338));
#1357=EDGE_LOOP('',(#7339,#7340,#7341,#7342));
#1358=EDGE_LOOP('',(#7343,#7344,#7345,#7346));
#1359=EDGE_LOOP('',(#7347,#7348,#7349,#7350));
#1360=EDGE_LOOP('',(#7351,#7352,#7353,#7354));
#1361=EDGE_LOOP('',(#7355,#7356,#7357,#7358));
#1362=EDGE_LOOP('',(#7359,#7360,#7361,#7362));
#1363=EDGE_LOOP('',(#7363,#7364,#7365,#7366));
#1364=EDGE_LOOP('',(#7367,#7368,#7369,#7370));
#1365=EDGE_LOOP('',(#7371,#7372,#7373,#7374));
#1366=EDGE_LOOP('',(#7375,#7376,#7377,#7378));
#1367=EDGE_LOOP('',(#7379,#7380,#7381,#7382));
#1368=EDGE_LOOP('',(#7383,#7384,#7385,#7386));
#1369=EDGE_LOOP('',(#7387,#7388,#7389,#7390));
#1370=EDGE_LOOP('',(#7391,#7392,#7393,#7394));
#1371=EDGE_LOOP('',(#7395,#7396,#7397,#7398));
#1372=EDGE_LOOP('',(#7399,#7400,#7401,#7402));
#1373=EDGE_LOOP('',(#7403,#7404,#7405,#7406,#7407,#7408,#7409,#7410));
#1374=EDGE_LOOP('',(#7411,#7412,#7413,#7414,#7415,#7416,#7417,#7418,#7419,
#7420,#7421,#7422,#7423,#7424,#7425,#7426,#7427,#7428,#7429,#7430,#7431,
#7432,#7433,#7434,#7435,#7436,#7437,#7438,#7439,#7440,#7441,#7442,#7443,
#7444,#7445,#7446,#7447,#7448,#7449,#7450,#7451,#7452));
#1375=EDGE_LOOP('',(#7453,#7454,#7455,#7456));
#1376=EDGE_LOOP('',(#7457,#7458,#7459,#7460,#7461,#7462,#7463,#7464,#7465,
#7466,#7467,#7468,#7469,#7470,#7471,#7472,#7473,#7474,#7475,#7476,#7477,
#7478,#7479,#7480,#7481,#7482,#7483,#7484,#7485,#7486,#7487,#7488,#7489,
#7490,#7491,#7492,#7493,#7494,#7495,#7496,#7497,#7498,#7499));
#1377=EDGE_LOOP('',(#7500,#7501,#7502,#7503));
#1378=EDGE_LOOP('',(#7504,#7505,#7506,#7507));
#1379=EDGE_LOOP('',(#7508,#7509,#7510,#7511));
#1380=EDGE_LOOP('',(#7512,#7513,#7514,#7515));
#1381=EDGE_LOOP('',(#7516,#7517,#7518,#7519));
#1382=EDGE_LOOP('',(#7520,#7521,#7522,#7523));
#1383=EDGE_LOOP('',(#7524,#7525,#7526,#7527));
#1384=EDGE_LOOP('',(#7528,#7529,#7530,#7531,#7532,#7533));
#1385=EDGE_LOOP('',(#7534));
#1386=EDGE_LOOP('',(#7535,#7536,#7537,#7538));
#1387=EDGE_LOOP('',(#7539,#7540,#7541,#7542));
#1388=EDGE_LOOP('',(#7543));
#1389=EDGE_LOOP('',(#7544,#7545,#7546,#7547,#7548,#7549));
#1390=EDGE_LOOP('',(#7550));
#1563=CIRCLE('',#9356,2.942);
#1564=CIRCLE('',#9376,2.37175);
#1565=CIRCLE('',#9396,2.942);
#1566=CIRCLE('',#9397,2.);
#1567=CIRCLE('',#9399,2.37175);
#1568=CIRCLE('',#9409,5.);
#1569=CIRCLE('',#9411,5.);
#2009=B_SPLINE_CURVE_WITH_KNOTS('',3,(#26402,#26403,#26404,#26405,#26406,
#26407,#26408,#26409,#26410,#26411),.UNSPECIFIED.,.F.,.F.,(4,3,3,4),(-4.09293042013066,
-3.97832038727896,-2.98374029045922,-2.06863817490914),.UNSPECIFIED.);
#2010=B_SPLINE_CURVE_WITH_KNOTS('',3,(#26414,#26415,#26416,#26417,#26418,
#26419,#26420),.UNSPECIFIED.,.F.,.F.,(4,3,4),(0.,0.995210874448857,1.11730040836817),
 .UNSPECIFIED.);
#2011=B_SPLINE_CURVE_WITH_KNOTS('',3,(#26425,#26426,#26427,#26428,#26429,
#26430,#26431,#26432,#26433,#26434,#26435,#26436,#26437,#26438,#26439,#26440,
#26441,#26442,#26443,#26444,#26445,#26446),.UNSPECIFIED.,.F.,.F.,(4,3,3,
3,3,3,3,4),(-10.3761157273102,-9.9458009681974,-8.95122087137766,-7.95664077455792,
-6.96206067773818,-5.96748058091844,-4.9729004840987,-4.09293042013066),
 .UNSPECIFIED.);
#2012=B_SPLINE_CURVE_WITH_KNOTS('',3,(#26447,#26448,#26449,#26450,#26451,
#26452,#26453,#26454,#26455,#26456,#26457,#26458,#26459,#26460,#26461,#26462,
#26463,#26464,#26465,#26466,#26467,#26468),.UNSPECIFIED.,.F.,.F.,(4,3,3,
3,3,3,3,4),(1.11730040836817,1.99042174889772,2.98563262334659,3.98084349779545,
4.97605437224432,5.97126524669318,6.96647612114205,7.40048571554776),
 .UNSPECIFIED.);
#2013=B_SPLINE_CURVE_WITH_KNOTS('',3,(#26473,#26474,#26475,#26476,#26477,
#26478,#26479,#26480,#26481,#26482,#26483,#26484,#26485,#26486,#26487,#26488,
#26489,#26490,#26491,#26492,#26493,#26494),.UNSPECIFIED.,.F.,.F.,(4,3,3,
3,3,3,3,4),(-16.6593010344898,-15.9132815491158,-14.9187014522961,-13.9241213554764,
-12.9295412586566,-11.9349611618369,-10.9403810650171,-10.3761157273102),
 .UNSPECIFIED.);
#2014=B_SPLINE_CURVE_WITH_KNOTS('',3,(#26495,#26496,#26497,#26498,#26499,
#26500,#26501,#26502,#26503,#26504,#26505,#26506,#26507,#26508,#26509,#26510,
#26511,#26512,#26513,#26514,#26515,#26516),.UNSPECIFIED.,.F.,.F.,(4,3,3,
3,3,3,3,4),(7.40048571554776,7.96168699559091,8.95689787003978,9.95210874448864,
10.9473196189375,11.9425304933864,12.9377413678352,13.6836710227273),
 .UNSPECIFIED.);
#2015=B_SPLINE_CURVE_WITH_KNOTS('',3,(#26521,#26522,#26523,#26524,#26525,
#26526,#26527,#26528,#26529,#26530,#26531,#26532,#26533,#26534,#26535,#26536,
#26537,#26538,#26539,#26540,#26541,#26542,#26543,#26544,#26545),
 .UNSPECIFIED.,.F.,.F.,(4,3,3,3,3,3,3,3,4),(-22.9424863416694,-22.875342226854,
-21.8807621300343,-20.8861820332145,-19.8916019363948,-18.8970218395751,
-17.9024417427553,-16.9078616459356,-16.6593010344898),.UNSPECIFIED.);
#2016=B_SPLINE_CURVE_WITH_KNOTS('',3,(#26546,#26547,#26548,#26549,#26550,
#26551,#26552,#26553,#26554,#26555,#26556,#26557,#26558,#26559,#26560,#26561,
#26562,#26563,#26564,#26565,#26566,#26567,#26568,#26569,#26570),
 .UNSPECIFIED.,.F.,.F.,(4,3,3,3,3,3,3,3,4),(13.6836710227273,13.9329522422841,
14.928163116733,15.9233739911818,16.9185848656307,17.9137957400795,18.9090066145284,
19.9042174889773,19.9668563299069),.UNSPECIFIED.);
#2017=B_SPLINE_CURVE_WITH_KNOTS('',3,(#26575,#26576,#26577,#26578,#26579,
#26580,#26581,#26582,#26583,#26584,#26585,#26586,#26587,#26588,#26589,#26590,
#26591,#26592,#26593,#26594,#26595,#26596),.UNSPECIFIED.,.F.,.F.,(4,3,3,
3,3,3,3,4),(-29.225671648849,-28.8428228077724,-27.8482427109527,-26.853662614133,
-25.8590825173132,-24.8645024204935,-23.8699223236738,-22.9424863416694),
 .UNSPECIFIED.);
#2018=B_SPLINE_CURVE_WITH_KNOTS('',3,(#26597,#26598,#26599,#26600,#26601,
#26602,#26603,#26604,#26605,#26606,#26607,#26608,#26609,#26610,#26611,#26612,
#26613,#26614,#26615,#26616,#26617,#26618),.UNSPECIFIED.,.F.,.F.,(4,3,3,
3,3,3,3,4),(19.9668563299069,20.8994283634261,21.894639237875,22.8898501123239,
23.8850609867727,24.8802718612216,25.8754827356705,26.2500416370865),
 .UNSPECIFIED.);
#2019=B_SPLINE_CURVE_WITH_KNOTS('',3,(#26623,#26624,#26625,#26626,#26627,
#26628,#26629,#26630,#26631,#26632,#26633,#26634,#26635,#26636,#26637,#26638,
#26639,#26640,#26641,#26642,#26643,#26644),.UNSPECIFIED.,.F.,.F.,(4,3,3,
3,3,3,3,4),(-35.5088569560286,-34.8103033886909,-33.8157232918711,-32.8211431950514,
-31.8265630982317,-30.8319830014119,-29.8374029045922,-29.225671648849),
 .UNSPECIFIED.);
#2020=B_SPLINE_CURVE_WITH_KNOTS('',3,(#26645,#26646,#26647,#26648,#26649,
#26650,#26651,#26652,#26653,#26654,#26655,#26656,#26657,#26658,#26659,#26660,
#26661,#26662,#26663,#26664,#26665,#26666),.UNSPECIFIED.,.F.,.F.,(4,3,3,
3,3,3,3,4),(26.2500416370865,26.8706936101193,27.8659044845682,28.861115359017,
29.8563262334659,30.8515371079148,31.8467479823636,32.5332269442661),
 .UNSPECIFIED.);
#2021=B_SPLINE_CURVE_WITH_KNOTS('',3,(#26671,#26672,#26673,#26674,#26675,
#26676,#26677,#26678,#26679,#26680,#26681,#26682,#26683,#26684,#26685,#26686,
#26687,#26688,#26689,#26690,#26691,#26692,#26693,#26694,#26695),
 .UNSPECIFIED.,.F.,.F.,(4,3,3,3,3,3,3,3,4),(-41.7920422632082,-41.7723640664291,
-40.7777839696093,-39.7832038727896,-38.7886237759698,-37.7940436791501,
-36.7994635823304,-35.8048834855106,-35.5088569560286),.UNSPECIFIED.);
#2022=B_SPLINE_CURVE_WITH_KNOTS('',3,(#26696,#26697,#26698,#26699,#26700,
#26701,#26702,#26703,#26704,#26705,#26706,#26707,#26708,#26709,#26710,#26711,
#26712,#26713,#26714,#26715,#26716,#26717,#26718,#26719,#26720),
 .UNSPECIFIED.,.F.,.F.,(4,3,3,3,3,3,3,3,4),(32.5332269442661,32.8419588568125,
33.8371697312614,34.8323806057102,35.8275914801591,36.822802354608,37.8180132290568,
38.8132241035057,38.8164122514457),.UNSPECIFIED.);
#2023=B_SPLINE_CURVE_WITH_KNOTS('',3,(#26725,#26726,#26727,#26728,#26729,
#26730,#26731,#26732,#26733,#26734,#26735,#26736,#26737,#26738,#26739,#26740,
#26741,#26742,#26743,#26744,#26745,#26746),.UNSPECIFIED.,.F.,.F.,(4,3,3,
3,3,3,3,4),(-48.0752275703878,-47.7398446473475,-46.7452645505278,-45.750684453708,
-44.7561043568883,-43.7615242600685,-42.7669441632488,-41.7920422632082),
 .UNSPECIFIED.);
#2024=B_SPLINE_CURVE_WITH_KNOTS('',3,(#26747,#26748,#26749,#26750,#26751,
#26752,#26753,#26754,#26755,#26756,#26757,#26758,#26759,#26760,#26761,#26762,
#26763,#26764,#26765,#26766,#26767,#26768),.UNSPECIFIED.,.F.,.F.,(4,3,3,
3,3,3,3,4),(38.8164122514457,39.8084349779546,40.8036458524034,41.7988567268523,
42.7940676013012,43.78927847575,44.7844893501989,45.0995975586253),
 .UNSPECIFIED.);
#2025=B_SPLINE_CURVE_WITH_KNOTS('',3,(#26773,#26774,#26775,#26776,#26777,
#26778,#26779,#26780,#26781,#26782,#26783,#26784,#26785,#26786,#26787,#26788,
#26789,#26790,#26791,#26792,#26793,#26794),.UNSPECIFIED.,.F.,.F.,(4,3,3,
3,3,3,3,4),(-54.3584128775674,-53.7073252282659,-52.7127451314462,-51.7181650346265,
-50.7235849378067,-49.729004840987,-48.7344247441672,-48.0752275703878),
 .UNSPECIFIED.);
#2026=B_SPLINE_CURVE_WITH_KNOTS('',3,(#26795,#26796,#26797,#26798,#26799,
#26800,#26801,#26802,#26803,#26804,#26805,#26806,#26807,#26808,#26809,#26810,
#26811,#26812,#26813,#26814,#26815,#26816),.UNSPECIFIED.,.F.,.F.,(4,3,3,
3,3,3,3,4),(45.0995975586253,45.7797002246477,46.7749110990966,47.7701219735455,
48.7653328479943,49.7605437224432,50.7557545968921,51.3827828658049),
 .UNSPECIFIED.);
#2027=B_SPLINE_CURVE_WITH_KNOTS('',3,(#26821,#26822,#26823,#26824,#26825,
#26826,#26827,#26828,#26829,#26830,#26831,#26832,#26833,#26834,#26835,#26836,
#26837,#26838,#26839,#26840,#26841,#26842),.UNSPECIFIED.,.F.,.F.,(4,3,3,
3,3,3,3,4),(-60.641598184747,-59.6748058091844,-58.6802257123646,-57.6856456155449,
-56.6910655187252,-55.6964854219054,-54.7019053250857,-54.3584128775674),
 .UNSPECIFIED.);
#2028=B_SPLINE_CURVE_WITH_KNOTS('',3,(#26843,#26844,#26845,#26846,#26847,
#26848,#26849,#26850,#26851,#26852,#26853,#26854,#26855,#26856,#26857,#26858,
#26859,#26860,#26861,#26862,#26863,#26864),.UNSPECIFIED.,.F.,.F.,(4,3,3,
3,3,3,3,4),(51.3827828658049,51.7509654713409,52.7461763457898,53.7413872202387,
54.7365980946875,55.7318089691364,56.7270198435852,57.6659681729845),
 .UNSPECIFIED.);
#2029=B_SPLINE_CURVE_WITH_KNOTS('',3,(#26869,#26870,#26871,#26872,#26873,
#26874,#26875,#26876,#26877,#26878,#26879,#26880,#26881,#26882,#26883,#26884,
#26885,#26886,#26887,#26888,#26889,#26890,#26891,#26892,#26893),
 .UNSPECIFIED.,.F.,.F.,(4,3,3,3,3,3,3,3,4),(-66.9247834919266,-66.6368664869226,
-65.6422863901028,-64.6477062932831,-63.6531261964633,-62.6585460996436,
-61.6639660028239,-60.6693859060041,-60.641598184747),.UNSPECIFIED.);
#2030=B_SPLINE_CURVE_WITH_KNOTS('',3,(#26894,#26895,#26896,#26897,#26898,
#26899,#26900,#26901,#26902,#26903,#26904,#26905,#26906,#26907,#26908,#26909,
#26910,#26911,#26912,#26913,#26914,#26915,#26916,#26917,#26918),
 .UNSPECIFIED.,.F.,.F.,(4,3,3,3,3,3,3,3,4),(57.6659681729845,57.7222307180341,
58.717441592483,59.7126524669318,60.7078633413807,61.7030742158296,62.6982850902784,
63.6934959647273,63.9491534801641),.UNSPECIFIED.);
#2031=B_SPLINE_CURVE_WITH_KNOTS('',3,(#26923,#26924,#26925,#26926,#26927,
#26928,#26929,#26930,#26931,#26932,#26933,#26934,#26935,#26936,#26937,#26938,
#26939,#26940,#26941,#26942,#26943,#26944),.UNSPECIFIED.,.F.,.F.,(4,3,3,
3,3,3,3,4),(-73.2079687991062,-72.604347067841,-71.6097669710212,-70.6151868742015,
-69.6206067773818,-68.626026680562,-67.6314465837423,-66.9247834919266),
 .UNSPECIFIED.);
#2032=B_SPLINE_CURVE_WITH_KNOTS('',3,(#26945,#26946,#26947,#26948,#26949,
#26950,#26951,#26952,#26953,#26954,#26955,#26956,#26957,#26958,#26959,#26960,
#26961,#26962,#26963,#26964,#26965,#26966),.UNSPECIFIED.,.F.,.F.,(4,3,3,
3,3,3,3,4),(63.9491534801641,64.6887068391762,65.683917713625,66.6791285880739,
67.6743394625228,68.6695503369716,69.6647612114205,70.2323387873437),
 .UNSPECIFIED.);
#2033=B_SPLINE_CURVE_WITH_KNOTS('',3,(#26971,#26972,#26973,#26974,#26975,
#26976,#26977,#26978,#26979,#26980,#26981,#26982,#26983,#26984,#26985,#26986,
#26987,#26988,#26989,#26990,#26991,#26992),.UNSPECIFIED.,.F.,.F.,(4,3,3,
3,3,3,3,4),(-79.4911541062857,-78.5718276487594,-77.5772475519397,-76.5826674551199,
-75.5880873583002,-74.5935072614805,-73.5989271646607,-73.2079687991062),
 .UNSPECIFIED.);
#2034=B_SPLINE_CURVE_WITH_KNOTS('',3,(#26993,#26994,#26995,#26996,#26997,
#26998,#26999,#27000,#27001,#27002,#27003,#27004,#27005,#27006,#27007,#27008,
#27009,#27010,#27011,#27012,#27013,#27014),.UNSPECIFIED.,.F.,.F.,(4,3,3,
3,3,3,3,4),(70.2323387873437,70.6599720858693,71.6551829603182,72.6503938347671,
73.6456047092159,74.6408155836648,75.6360264581137,76.5155240945233),
 .UNSPECIFIED.);
#2035=B_SPLINE_CURVE_WITH_KNOTS('',3,(#27019,#27020,#27021,#27022,#27023,
#27024,#27025,#27026,#27027,#27028,#27029,#27030,#27031,#27032,#27033,#27034,
#27035,#27036,#27037,#27038,#27039,#27040,#27041,#27042,#27043),
 .UNSPECIFIED.,.F.,.F.,(4,3,3,3,3,3,3,3,4),(-85.7743394134653,-85.5338883264976,
-84.5393082296779,-83.5447281328581,-82.5501480360384,-81.5555679392187,
-80.5609878423989,-79.5664077455792,-79.4911541062857),.UNSPECIFIED.);
#2036=B_SPLINE_CURVE_WITH_KNOTS('',3,(#27044,#27045,#27046,#27047,#27048,
#27049,#27050,#27051,#27052,#27053,#27054,#27055,#27056,#27057,#27058,#27059,
#27060,#27061,#27062,#27063,#27064,#27065,#27066,#27067,#27068),
 .UNSPECIFIED.,.F.,.F.,(4,3,3,3,3,3,3,3,4),(76.5155240945233,76.6312373325625,
77.6264482070114,78.6216590814603,79.6168699559091,80.612080830358,81.6072917048068,
82.6025025792557,82.7987094017029),.UNSPECIFIED.);
#2037=B_SPLINE_CURVE_WITH_KNOTS('',3,(#27073,#27074,#27075,#27076,#27077,
#27078,#27079,#27080,#27081,#27082,#27083,#27084,#27085,#27086,#27087,#27088,
#27089,#27090,#27091,#27092,#27093,#27094),.UNSPECIFIED.,.F.,.F.,(4,3,3,
3,3,3,3,4),(-92.0575247206449,-91.501368907416,-90.5067888105963,-89.5122087137766,
-88.5176286169568,-87.5230485201371,-86.5284684233173,-85.7743394134653),
 .UNSPECIFIED.);
#2038=B_SPLINE_CURVE_WITH_KNOTS('',3,(#27095,#27096,#27097,#27098,#27099,
#27100,#27101,#27102,#27103,#27104,#27105,#27106,#27107,#27108,#27109,#27110,
#27111,#27112,#27113,#27114,#27115,#27116),.UNSPECIFIED.,.F.,.F.,(4,3,3,
3,3,3,3,4),(82.7987094017029,83.5977134537046,84.5929243281534,85.5881352026023,
86.5833460770512,87.5785569515,88.5737678259489,89.0818947088824),
 .UNSPECIFIED.);
#2039=B_SPLINE_CURVE_WITH_KNOTS('',3,(#27121,#27122,#27123,#27124,#27125,
#27126,#27127,#27128,#27129,#27130,#27131,#27132,#27133,#27134,#27135,#27136,
#27137,#27138,#27139,#27140,#27141,#27142),.UNSPECIFIED.,.F.,.F.,(4,3,3,
3,3,3,3,4),(-98.3407100278245,-97.4688494883345,-96.4742693915147,-95.479689294695,
-94.4851091978752,-93.4905291010555,-92.4959490042358,-92.0575247206449),
 .UNSPECIFIED.);
#2040=B_SPLINE_CURVE_WITH_KNOTS('',3,(#27143,#27144,#27145,#27146,#27147,
#27148,#27149,#27150,#27151,#27152,#27153,#27154,#27155,#27156,#27157,#27158,
#27159,#27160,#27161,#27162,#27163,#27164),.UNSPECIFIED.,.F.,.F.,(4,3,3,
3,3,3,3,4),(89.0818947088824,89.5689787003978,90.5641895748466,91.5594004492955,
92.5546113237443,93.5498221981932,94.5450330726421,95.365080016062),
 .UNSPECIFIED.);
#2041=B_SPLINE_CURVE_WITH_KNOTS('',3,(#27169,#27170,#27171,#27172,#27173,
#27174,#27175,#27176,#27177,#27178,#27179,#27180,#27181,#27182,#27183,#27184,
#27185,#27186,#27187,#27188,#27189,#27190,#27191,#27192,#27193),
 .UNSPECIFIED.,.F.,.F.,(4,3,3,3,3,3,3,3,4),(-104.623895335004,-104.430910166073,
-103.436330069253,-102.441749972433,-101.447169875613,-100.452589778794,
-99.458009681974,-98.4634295851542,-98.3407100278245),.UNSPECIFIED.);
#2042=B_SPLINE_CURVE_WITH_KNOTS('',3,(#27194,#27195,#27196,#27197,#27198,
#27199,#27200,#27201,#27202,#27203,#27204,#27205,#27206,#27207,#27208,#27209,
#27210,#27211,#27212,#27213,#27214,#27215,#27216,#27217,#27218),
 .UNSPECIFIED.,.F.,.F.,(4,3,3,3,3,3,3,3,4),(95.365080016062,95.5402439470909,
96.5354548215398,97.5306656959886,98.5258765704375,99.5210874448864,100.516298319335,
101.511509193784,101.648265323242),.UNSPECIFIED.);
#2043=B_SPLINE_CURVE_WITH_KNOTS('',3,(#27223,#27224,#27225,#27226,#27227,
#27228,#27229,#27230,#27231,#27232,#27233,#27234,#27235,#27236,#27237,#27238,
#27239,#27240,#27241,#27242,#27243,#27244),.UNSPECIFIED.,.F.,.F.,(4,3,3,
3,3,3,3,4),(-110.907080642184,-110.398390746991,-109.403810650171,-108.409230553352,
-107.414650456532,-106.420070359712,-105.425490262892,-104.623895335004),
 .UNSPECIFIED.);
#2044=B_SPLINE_CURVE_WITH_KNOTS('',3,(#27245,#27246,#27247,#27248,#27249,
#27250,#27251,#27252,#27253,#27254,#27255,#27256,#27257,#27258,#27259,#27260,
#27261,#27262,#27263,#27264,#27265,#27266),.UNSPECIFIED.,.F.,.F.,(4,3,3,
3,3,3,3,4),(101.648265323242,102.506720068233,103.501930942682,104.497141817131,
105.49235269158,106.487563566028,107.482774440477,107.931450630421),
 .UNSPECIFIED.);
#2045=B_SPLINE_CURVE_WITH_KNOTS('',3,(#27271,#27272,#27273,#27274,#27275,
#27276,#27277,#27278,#27279,#27280,#27281,#27282,#27283,#27284,#27285,#27286,
#27287,#27288,#27289,#27290,#27291,#27292),.UNSPECIFIED.,.F.,.F.,(4,3,3,
3,3,3,3,4),(-117.190265949363,-116.36587132791,-115.37129123109,-114.37671113427,
-113.38213103745,-112.387550940631,-111.392970843811,-110.907080642184),
 .UNSPECIFIED.);
#2046=B_SPLINE_CURVE_WITH_KNOTS('',3,(#27293,#27294,#27295,#27296,#27297,
#27298,#27299,#27300,#27301,#27302,#27303,#27304,#27305,#27306,#27307,#27308,
#27309,#27310,#27311,#27312,#27313,#27314),.UNSPECIFIED.,.F.,.F.,(4,3,3,
3,3,3,3,4),(107.931450630421,108.477985314926,109.473196189375,110.468407063824,
111.463617938273,112.458828812722,113.454039687171,114.214635937601),
 .UNSPECIFIED.);
#2047=B_SPLINE_CURVE_WITH_KNOTS('',3,(#27320,#27321,#27322,#27323,#27324,
#27325,#27326,#27327,#27328,#27329),.UNSPECIFIED.,.F.,.F.,(4,1,1,1,1,1,
1,4),(128.805298797182,128.975484272548,129.970064369367,130.964644466187,
131.959224563007,132.953804659826,133.948384756646,134.942964853466),
 .UNSPECIFIED.);
#2048=B_SPLINE_CURVE_WITH_KNOTS('',3,(#27332,#27333,#27334,#27335,#27336,
#27337,#27338,#27339),.UNSPECIFIED.,.F.,.F.,(4,1,1,1,1,4),(128.805298797182,
129.723204235162,130.718415109611,131.71362598406,132.708836858509,133.704047732958),
 .UNSPECIFIED.);
#2049=B_SPLINE_CURVE_WITH_KNOTS('',3,(#27344,#27345,#27346,#27347,#27348,
#27349,#27350,#27351,#27352,#27353),.UNSPECIFIED.,.F.,.F.,(4,1,1,1,1,1,
1,4),(122.522113490002,123.008003691629,124.002583788449,124.997163885269,
125.991743982088,126.986324078908,127.980904175728,128.805298797182),
 .UNSPECIFIED.);
#2050=B_SPLINE_CURVE_WITH_KNOTS('',3,(#27354,#27355,#27356,#27357,#27358,
#27359,#27360,#27361,#27362,#27363,#27364),.UNSPECIFIED.,.F.,.F.,(4,1,1,
1,1,1,1,1,4),(122.522113490002,122.75672811402,123.751938988469,124.747149862918,
125.742360737367,126.737571611816,127.732782486265,128.727993360714,128.805298797182),
 .UNSPECIFIED.);
#2051=B_SPLINE_CURVE_WITH_KNOTS('',3,(#27369,#27370,#27371,#27372,#27373,
#27374,#27375,#27376,#27377,#27378),.UNSPECIFIED.,.F.,.F.,(4,1,1,1,1,1,
1,4),(116.238928182822,117.040523110711,118.03510320753,119.02968330435,
120.02426340117,121.01884349799,122.013423594809,122.522113490002),
 .UNSPECIFIED.);
#2052=B_SPLINE_CURVE_WITH_KNOTS('',3,(#27379,#27380,#27381,#27382,#27383,
#27384,#27385,#27386,#27387,#27388),.UNSPECIFIED.,.F.,.F.,(4,1,1,1,1,1,
1,4),(116.238928182822,116.785462867327,117.780673741776,118.775884616225,
119.771095490674,120.766306365123,121.761517239572,122.522113490002),
 .UNSPECIFIED.);
#2053=B_SPLINE_CURVE_WITH_KNOTS('',3,(#27393,#27394,#27395,#27396,#27397,
#27398,#27399,#27400,#27401,#27402,#27403),.UNSPECIFIED.,.F.,.F.,(4,1,1,
1,1,1,1,1,4),(109.955742875643,110.078462432972,111.073042529792,112.067622626612,
113.062202723432,114.056782820251,115.051362917071,116.045943013891,116.238928182822),
 .UNSPECIFIED.);
#2054=B_SPLINE_CURVE_WITH_KNOTS('',3,(#27404,#27405,#27406,#27407,#27408,
#27409,#27410,#27411,#27412,#27413),.UNSPECIFIED.,.F.,.F.,(4,1,1,1,1,1,
1,4),(109.955742875643,110.814197620634,111.809408495083,112.804619369532,
113.799830243981,114.795041118429,115.790251992878,116.238928182822),
 .UNSPECIFIED.);
#2055=B_SPLINE_CURVE_WITH_KNOTS('',3,(#27418,#27419,#27420,#27421,#27422,
#27423,#27424,#27425,#27426,#27427),.UNSPECIFIED.,.F.,.F.,(4,1,1,1,1,1,
1,4),(103.672557568463,104.110981852054,105.105561948874,106.100142045694,
107.094722142513,108.089302239333,109.083882336153,109.955742875643),
 .UNSPECIFIED.);
#2056=B_SPLINE_CURVE_WITH_KNOTS('',3,(#27428,#27429,#27430,#27431,#27432,
#27433,#27434,#27435,#27436,#27437,#27438),.UNSPECIFIED.,.F.,.F.,(4,1,1,
1,1,1,1,1,4),(103.672557568463,103.847721499492,104.842932373941,105.83814324839,
106.833354122839,107.828564997287,108.823775871736,109.818986746185,109.955742875643),
 .UNSPECIFIED.);
#2057=B_SPLINE_CURVE_WITH_KNOTS('',3,(#27443,#27444,#27445,#27446,#27447,
#27448,#27449,#27450,#27451,#27452),.UNSPECIFIED.,.F.,.F.,(4,1,1,1,1,1,
1,4),(97.3893722612836,98.1435012711356,99.1380813679553,100.132661464775,
101.127241561595,102.121821658415,103.116401755234,103.672557568463),
 .UNSPECIFIED.);
#2058=B_SPLINE_CURVE_WITH_KNOTS('',3,(#27453,#27454,#27455,#27456,#27457,
#27458,#27459,#27460,#27461,#27462),.UNSPECIFIED.,.F.,.F.,(4,1,1,1,1,1,
1,4),(97.3893722612836,97.8764562527988,98.8716671272477,99.8668780016965,
100.862088876145,101.857299750594,102.852510625043,103.672557568463),
 .UNSPECIFIED.);
#2059=B_SPLINE_CURVE_WITH_KNOTS('',3,(#27467,#27468,#27469,#27470,#27471,
#27472,#27473,#27474,#27475,#27476,#27477),.UNSPECIFIED.,.F.,.F.,(4,1,1,
1,1,1,1,1,4),(91.106186954104,91.1814405933974,92.1760206902171,93.1706007870369,
94.1651808838566,95.1597609806764,96.1543410774961,97.1489211743159,97.3893722612836),
 .UNSPECIFIED.);
#2060=B_SPLINE_CURVE_WITH_KNOTS('',3,(#27478,#27479,#27480,#27481,#27482,
#27483,#27484,#27485,#27486,#27487),.UNSPECIFIED.,.F.,.F.,(4,1,1,1,1,1,
1,4),(91.106186954104,91.9051910061056,92.9004018805545,93.8956127550033,
94.8908236294522,95.8860345039011,96.8812453783499,97.3893722612836),
 .UNSPECIFIED.);
#2061=B_SPLINE_CURVE_WITH_KNOTS('',3,(#27492,#27493,#27494,#27495,#27496,
#27497,#27498,#27499,#27500,#27501),.UNSPECIFIED.,.F.,.F.,(4,1,1,1,1,1,
1,4),(84.8230016469244,85.213960012479,86.2085401092987,87.2031202061185,
88.1977003029382,89.1922803997579,90.1868604965777,91.106186954104),
 .UNSPECIFIED.);
#2062=B_SPLINE_CURVE_WITH_KNOTS('',3,(#27502,#27503,#27504,#27505,#27506,
#27507,#27508,#27509,#27510,#27511,#27512),.UNSPECIFIED.,.F.,.F.,(4,1,1,
1,1,1,1,1,4),(84.8230016469244,84.9387148849636,85.9339257594124,86.9291366338613,
87.9243475083101,88.919558382759,89.9147692572079,90.9099801316567,91.106186954104),
 .UNSPECIFIED.);
#2063=B_SPLINE_CURVE_WITH_KNOTS('',3,(#27517,#27518,#27519,#27520,#27521,
#27522,#27523,#27524,#27525,#27526),.UNSPECIFIED.,.F.,.F.,(4,1,1,1,1,1,
1,4),(78.5398163397448,79.2464794315605,80.2410595283803,81.2356396252,
82.2302197220198,83.2247998188395,84.2193799156592,84.8230016469244),
 .UNSPECIFIED.);
#2064=B_SPLINE_CURVE_WITH_KNOTS('',3,(#27527,#27528,#27529,#27530,#27531,
#27532,#27533,#27534,#27535,#27536),.UNSPECIFIED.,.F.,.F.,(4,1,1,1,1,1,
1,4),(78.5398163397448,78.9674496382704,79.9626605127192,80.9578713871681,
81.953082261617,82.9482931360658,83.9435040105147,84.8230016469244),
 .UNSPECIFIED.);
#2065=B_SPLINE_CURVE_WITH_KNOTS('',3,(#27541,#27542,#27543,#27544,#27545,
#27546,#27547,#27548,#27549,#27550,#27551),.UNSPECIFIED.,.F.,.F.,(4,1,1,
1,1,1,1,1,4),(72.2566310325652,72.2844187538224,73.2789988506421,74.2735789474618,
75.2681590442816,76.2627391411013,77.2573192379211,78.2518993347408,78.5398163397448),
 .UNSPECIFIED.);
#2066=B_SPLINE_CURVE_WITH_KNOTS('',3,(#27552,#27553,#27554,#27555,#27556,
#27557,#27558,#27559,#27560,#27561),.UNSPECIFIED.,.F.,.F.,(4,1,1,1,1,1,
1,4),(72.2566310325652,72.9961843915772,73.9913952660261,74.9866061404749,
75.9818170149238,76.9770278893726,77.9722387638215,78.5398163397448),
 .UNSPECIFIED.);
#2067=B_SPLINE_CURVE_WITH_KNOTS('',3,(#27566,#27567,#27568,#27569,#27570,
#27571,#27572,#27573,#27574,#27575),.UNSPECIFIED.,.F.,.F.,(4,1,1,1,1,1,
1,4),(65.9734457253856,66.3169381729039,67.3115182697237,68.3060983665434,
69.3006784633631,70.2952585601829,71.2898386570026,72.2566310325652),
 .UNSPECIFIED.);
#2068=B_SPLINE_CURVE_WITH_KNOTS('',3,(#27576,#27577,#27578,#27579,#27580,
#27581,#27582,#27583,#27584,#27585,#27586),.UNSPECIFIED.,.F.,.F.,(4,1,1,
1,1,1,1,1,4),(65.9734457253856,66.0297082704352,67.024919144884,68.0201300193329,
69.0153408937817,70.0105517682306,71.0057626426795,72.0009735171283,72.2566310325652),
 .UNSPECIFIED.);
#2069=B_SPLINE_CURVE_WITH_KNOTS('',3,(#27591,#27592,#27593,#27594,#27595,
#27596,#27597,#27598,#27599,#27600),.UNSPECIFIED.,.F.,.F.,(4,1,1,1,1,1,
1,4),(59.690260418206,60.3494575919855,61.3440376888052,62.338617785625,
63.3331978824447,64.3277779792645,65.3223580760842,65.9734457253856),
 .UNSPECIFIED.);
#2070=B_SPLINE_CURVE_WITH_KNOTS('',3,(#27601,#27602,#27603,#27604,#27605,
#27606,#27607,#27608,#27609,#27610),.UNSPECIFIED.,.F.,.F.,(4,1,1,1,1,1,
1,4),(59.690260418206,60.058443023742,61.0536538981908,62.0488647726397,
63.0440756470886,64.0392865215374,65.0344973959863,65.9734457253856),
 .UNSPECIFIED.);
#2071=B_SPLINE_CURVE_WITH_KNOTS('',3,(#27615,#27616,#27617,#27618,#27619,
#27620,#27621,#27622,#27623,#27624),.UNSPECIFIED.,.F.,.F.,(4,1,1,1,1,1,
1,4),(53.4070751110264,54.3819770110671,55.3765571078868,56.3711372047065,
57.3657173015263,58.360297398346,59.3548774951657,59.690260418206),
 .UNSPECIFIED.);
#2072=B_SPLINE_CURVE_WITH_KNOTS('',3,(#27625,#27626,#27627,#27628,#27629,
#27630,#27631,#27632,#27633,#27634),.UNSPECIFIED.,.F.,.F.,(4,1,1,1,1,1,
1,4),(53.4070751110264,54.0871777770488,55.0823886514976,56.0775995259465,
57.0728104003954,58.0680212748442,59.0632321492931,59.690260418206),
 .UNSPECIFIED.);
#2073=B_SPLINE_CURVE_WITH_KNOTS('',3,(#27639,#27640,#27641,#27642,#27643,
#27644,#27645,#27646,#27647,#27648,#27649),.UNSPECIFIED.,.F.,.F.,(4,1,1,
1,1,1,1,1,4),(47.1238898038468,47.4199163333289,48.4144964301486,49.4090765269684,
50.4036566237881,51.3982367206078,52.3928168174276,53.3873969142473,53.4070751110264),
 .UNSPECIFIED.);
#2074=B_SPLINE_CURVE_WITH_KNOTS('',3,(#27650,#27651,#27652,#27653,#27654,
#27655,#27656,#27657,#27658,#27659),.UNSPECIFIED.,.F.,.F.,(4,1,1,1,1,1,
1,4),(47.1238898038468,48.1159125303556,49.1111234048045,50.1063342792533,
51.1015451537022,52.096756028151,53.0919669025999,53.4070751110264),
 .UNSPECIFIED.);
#2075=B_SPLINE_CURVE_WITH_KNOTS('',3,(#27664,#27665,#27666,#27667,#27668,
#27669,#27670,#27671,#27672,#27673),.UNSPECIFIED.,.F.,.F.,(4,1,1,1,1,1,
1,4),(40.8407044966673,41.4524357524104,42.4470158492302,43.4415959460499,
44.4361760428697,45.4307561396894,46.4253362365091,47.1238898038468),
 .UNSPECIFIED.);
#2076=B_SPLINE_CURVE_WITH_KNOTS('',3,(#27674,#27675,#27676,#27677,#27678,
#27679,#27680,#27681,#27682,#27683,#27684),.UNSPECIFIED.,.F.,.F.,(4,1,1,
1,1,1,1,1,4),(40.8407044966672,41.1494364092135,42.1446472836624,43.1398581581113,
44.1350690325601,45.130279907009,46.1254907814579,47.1207016559067,47.1238898038468),
 .UNSPECIFIED.);
#2077=B_SPLINE_CURVE_WITH_KNOTS('',3,(#27689,#27690,#27691,#27692,#27693,
#27694,#27695,#27696,#27697,#27698),.UNSPECIFIED.,.F.,.F.,(4,1,1,1,1,1,
1,4),(34.5575191894877,35.484955171492,36.4795352683117,37.4741153651315,
38.4686954619512,39.463275558771,40.4578556555907,40.8407044966673),
 .UNSPECIFIED.);
#2078=B_SPLINE_CURVE_WITH_KNOTS('',3,(#27699,#27700,#27701,#27702,#27703,
#27704,#27705,#27706,#27707,#27708),.UNSPECIFIED.,.F.,.F.,(4,1,1,1,1,1,
1,4),(34.5575191894876,35.1781711625204,36.1733820369692,37.1685929114181,
38.163803785867,39.1590146603158,40.1542255347647,40.8407044966672),
 .UNSPECIFIED.);
#2079=B_SPLINE_CURVE_WITH_KNOTS('',3,(#27713,#27714,#27715,#27716,#27717,
#27718,#27719,#27720,#27721,#27722,#27723),.UNSPECIFIED.,.F.,.F.,(4,1,1,
1,1,1,1,1,4),(28.2743338823081,28.5228944937538,29.5174745905736,30.5120546873933,
31.506634784213,32.5012148810328,33.4957949778525,34.4903750746723,34.5575191894877),
 .UNSPECIFIED.);
#2080=B_SPLINE_CURVE_WITH_KNOTS('',3,(#27724,#27725,#27726,#27727,#27728,
#27729,#27730,#27731,#27732,#27733),.UNSPECIFIED.,.F.,.F.,(4,1,1,1,1,1,
1,4),(28.274333882308,29.2069059158272,30.202116790276,31.1973276647249,
32.1925385391738,33.1877494136226,34.1829602880715,34.5575191894876),
 .UNSPECIFIED.);
#2081=B_SPLINE_CURVE_WITH_KNOTS('',3,(#27738,#27739,#27740,#27741,#27742,
#27743,#27744,#27745,#27746,#27747),.UNSPECIFIED.,.F.,.F.,(4,1,1,1,1,1,
1,4),(21.9911485751285,22.5554139128354,23.5499940096551,24.5445741064749,
25.5391542032946,26.5337343001143,27.5283143969341,28.2743338823081),
 .UNSPECIFIED.);
#2082=B_SPLINE_CURVE_WITH_KNOTS('',3,(#27748,#27749,#27750,#27751,#27752,
#27753,#27754,#27755,#27756,#27757,#27758),.UNSPECIFIED.,.F.,.F.,(4,1,1,
1,1,1,1,1,4),(21.9911485751285,22.2404297946851,23.235640669134,24.2308515435829,
25.2260624180317,26.2212732924806,27.2164841669295,28.2116950413783,28.274333882308),
 .UNSPECIFIED.);
#2083=B_SPLINE_CURVE_WITH_KNOTS('',3,(#27763,#27764,#27765,#27766,#27767,
#27768,#27769,#27770,#27771,#27772),.UNSPECIFIED.,.F.,.F.,(4,1,1,1,1,1,
1,4),(15.7079632679489,16.5879333319169,17.5825134287367,18.5770935255564,
19.5716736223762,20.5662537191959,21.5608338160156,21.9911485751285),
 .UNSPECIFIED.);
#2084=B_SPLINE_CURVE_WITH_KNOTS('',3,(#27773,#27774,#27775,#27776,#27777,
#27778,#27779,#27780,#27781,#27782),.UNSPECIFIED.,.F.,.F.,(4,1,1,1,1,1,
1,4),(15.7079632679489,16.2691645479919,17.2643754224408,18.2595862968897,
19.2547971713385,20.2500080457874,21.2452189202363,21.9911485751285),
 .UNSPECIFIED.);
#2085=B_SPLINE_CURVE_WITH_KNOTS('',3,(#27785,#27786,#27787,#27788,#27789,
#27790,#27791,#27792,#27793,#27794,#27795,#27796,#27797,#27798,#27799,#27800,
#27801,#27802,#27803,#27804,#27805,#27806,#27807,#27808,#27809,#27810,#27811,
#27812,#27813,#27814,#27815,#27816,#27817,#27818,#27819,#27820,#27821,#27822,
#27823,#27824,#27825,#27826,#27827,#27828,#27829,#27830,#27831,#27832,#27833,
#27834,#27835,#27836,#27837,#27838,#27839,#27840,#27841,#27842,#27843,#27844,
#27845,#27846,#27847,#27848,#27849,#27850,#27851,#27852,#27853,#27854,#27855,
#27856,#27857,#27858,#27859,#27860,#27861,#27862,#27863,#27864,#27865,#27866,
#27867,#27868,#27869,#27870,#27871,#27872,#27873,#27874,#27875,#27876,#27877,
#27878,#27879,#27880,#27881,#27882,#27883,#27884,#27885,#27886,#27887,#27888,
#27889,#27890,#27891,#27892,#27893,#27894,#27895,#27896,#27897,#27898,#27899,
#27900,#27901,#27902,#27903,#27904,#27905,#27906,#27907,#27908,#27909,#27910,
#27911,#27912,#27913,#27914,#27915,#27916,#27917,#27918,#27919,#27920,#27921,
#27922,#27923,#27924,#27925,#27926,#27927,#27928,#27929,#27930,#27931,#27932,
#27933,#27934,#27935,#27936,#27937,#27938,#27939,#27940,#27941,#27942,#27943,
#27944,#27945,#27946,#27947,#27948,#27949,#27950,#27951,#27952,#27953,#27954,
#27955,#27956,#27957,#27958,#27959,#27960,#27961,#27962,#27963,#27964,#27965,
#27966,#27967,#27968,#27969,#27970,#27971,#27972,#27973,#27974,#27975,#27976,
#27977,#27978,#27979,#27980,#27981,#27982,#27983,#27984,#27985,#27986,#27987,
#27988,#27989,#27990,#27991,#27992,#27993,#27994,#27995,#27996,#27997,#27998,
#27999,#28000,#28001),.UNSPECIFIED.,.F.,.F.,(4,3,3,3,3,3,3,3,3,3,3,3,3,
3,3,3,3,3,3,3,3,3,3,3,3,3,3,3,3,3,3,3,3,3,3,3,3,3,3,3,3,3,3,3,3,3,3,3,3,
3,3,3,3,3,3,3,3,3,3,3,3,3,3,3,3,3,3,3,3,3,3,3,4),(-1.51155304937218,-1.48679589018691,
-1.46138238829548,-1.44932968678137,-1.44202339889261,-1.43723753989169,
-1.41130220328917,-1.38513854317652,-1.36889998110575,-1.36503952627177,
-1.33858827470488,-1.31226992028779,-1.2904045421787,-1.27947185312415,
-1.2739418323947,-1.26910255727935,-1.26853916406961,-1.24320807613995,
-1.21713370060773,-1.19192364256778,-1.1808942421753,-1.17533077231359,
-1.17132639907569,-1.14454252235409,-1.11744879668778,-1.09194990658787,
-1.08205955713065,-1.07541108639849,-1.07098105357362,-1.04321714493087,
-1.01545323628813,-0.988586919757226,-0.977559947169411,-0.973454614695351,
-0.945849052593242,-0.918335863837345,-0.890659863078365,-0.880780750637945,
-0.874611135600851,-0.869075769037592,-0.839959356247813,-0.812088250518227,
-0.784649362472489,-0.774142465660809,-0.769176292614452,-0.765440171794195,
-0.752610117878475,-0.725564556570394,-0.697804528028517,-0.670559901065443,
-0.663513210433686,-0.658766646015375,-0.63051115053422,-0.601912995645473,
-0.573421525171605,-0.561724773565645,-0.556706216040174,-0.552062451237872,
-0.523185606324559,-0.494757836998693,-0.479847512323927,-0.451360048372548,
-0.445014903039589,-0.416674688960391,-0.387739897039467,-0.3585492715235,
-0.342105607427002,-0.337686588976065,-0.308251612910489,-0.278764630960614,
-0.249889482606856,-0.226999958751517,-0.219677966288002),.UNSPECIFIED.);
#2086=B_SPLINE_CURVE_WITH_KNOTS('',3,(#28003,#28004,#28005,#28006,#28007,
#28008,#28009,#28010,#28011,#28012,#28013,#28014,#28015,#28016,#28017,#28018,
#28019,#28020,#28021,#28022,#28023,#28024,#28025,#28026,#28027,#28028,#28029,
#28030,#28031,#28032,#28033,#28034,#28035,#28036,#28037,#28038,#28039,#28040,
#28041,#28042,#28043,#28044,#28045,#28046,#28047,#28048,#28049,#28050,#28051,
#28052,#28053,#28054,#28055,#28056,#28057,#28058,#28059,#28060,#28061,#28062,
#28063,#28064,#28065,#28066),.UNSPECIFIED.,.F.,.F.,(4,3,3,3,3,3,3,3,3,3,
3,3,3,3,3,3,3,3,3,3,3,4),(-0.410648750432968,-0.381297076896285,-0.351072899913787,
-0.328404767176913,-0.311403667624258,-0.306442089482872,-0.302102601213264,
-0.274553556804158,-0.260400368966293,-0.232154047098012,-0.20313479121076,
-0.198616600552917,-0.194415645561828,-0.167218225709786,-0.140141557977483,
-0.113536626964066,-0.0982426601520032,-0.0937832747631835,-0.0680349364798781,
-0.0426775990213316,-0.0180562547442421,0.),.UNSPECIFIED.);
#2087=B_SPLINE_CURVE_WITH_KNOTS('',3,(#28069,#28070,#28071,#28072,#28073,
#28074,#28075,#28076,#28077,#28078,#28079,#28080,#28081,#28082,#28083,#28084,
#28085,#28086,#28087,#28088,#28089,#28090,#28091,#28092,#28093,#28094,#28095,
#28096,#28097,#28098,#28099),.UNSPECIFIED.,.F.,.F.,(4,3,3,3,3,3,3,3,3,3,
4),(-0.219677966288002,-0.197396196086295,-0.168503105981079,-0.139030379252539,
-0.121651581845971,-0.11563839456145,-0.111282058235295,-0.0816044721193899,
-0.0515653636756491,-0.0216265990765453,0.),.UNSPECIFIED.);
#2088=B_SPLINE_CURVE_WITH_KNOTS('',3,(#28612,#28613,#28614,#28615,#28616,
#28617,#28618,#28619),.UNSPECIFIED.,.F.,.F.,(4,1,1,1,1,4),(11.6150328478182,
12.609612944638,13.6041930414577,14.5987731382775,15.5933532350972,15.7079632679489),
 .UNSPECIFIED.);
#2089=B_SPLINE_CURVE_WITH_KNOTS('',3,(#28620,#28621,#28622,#28623,#28624,
#28625,#28626,#28627,#28628,#28629,#28630,#28631,#28632,#28633,#28634,#28635,
#28636,#28637,#28638,#28639,#28640,#28641,#28642,#28643,#28644,#28645,#28646,
#28647,#28648,#28649,#28650,#28651,#28652,#28653,#28654,#28655,#28656,#28657,
#28658,#28659,#28660,#28661,#28662,#28663,#28664,#28665,#28666,#28667,#28668,
#28669,#28670,#28671,#28672,#28673,#28674,#28675,#28676,#28677,#28678,#28679,
#28680,#28681,#28682,#28683,#28684,#28685,#28686,#28687,#28688,#28689,#28690,
#28691,#28692,#28693,#28694,#28695,#28696,#28697,#28698,#28699,#28700,#28701,
#28702,#28703,#28704,#28705,#28706,#28707,#28708,#28709,#28710),
 .UNSPECIFIED.,.F.,.F.,(4,3,3,3,3,3,3,3,3,3,3,3,3,3,3,3,3,3,3,3,3,3,3,3,
3,3,3,3,3,3,4),(-0.552745378375042,-0.529416010123812,-0.500021421858097,
-0.484490821675271,-0.477389212266168,-0.472189171636004,-0.443139563409207,
-0.419188595349667,-0.408465056144172,-0.40220615535047,-0.397553084820015,
-0.369246017540656,-0.339817467888714,-0.312695003632551,-0.296611352770663,
-0.291417321934603,-0.264612611533511,-0.251531818932889,-0.224160792273692,
-0.19614069323948,-0.191761200285163,-0.165152286051105,-0.138522950074249,
-0.112274345430976,-0.0982400522521039,-0.0941400538979384,-0.0901685480379393,
-0.064623178524502,-0.0394785441680361,-0.0151170408359151,0.),
 .UNSPECIFIED.);
#2090=B_SPLINE_CURVE_WITH_KNOTS('',3,(#28711,#28712,#28713,#28714,#28715,
#28716,#28717,#28718,#28719,#28720,#28721,#28722,#28723,#28724,#28725,#28726,
#28727,#28728,#28729),.UNSPECIFIED.,.F.,.F.,(4,3,3,3,3,3,4),(-121.813583759138,
-121.338771812008,-120.344191715188,-119.349611618369,-118.355031521549,
-117.360451424729,-117.190265949363),.UNSPECIFIED.);
#2091=B_SPLINE_CURVE_WITH_KNOTS('',3,(#28732,#28733,#28734,#28735,#28736,
#28737,#28738,#28739,#28740),.UNSPECIFIED.,.F.,.F.,(4,1,1,1,1,1,4),(10.3761157273101,
11.2931101757476,12.2883210501965,13.2835319246454,14.2787427990942,15.2739536735431,
15.7079632679489),.UNSPECIFIED.);
#2092=B_SPLINE_CURVE_WITH_KNOTS('',3,(#29258,#29259,#29260,#29261,#29262,
#29263,#29264,#29265,#29266,#29267,#29268,#29269,#29270,#29271,#29272,#29273,
#29274,#29275,#29276,#29277,#29278,#29279),.UNSPECIFIED.,.F.,.F.,(4,3,3,
3,3,3,3,4),(114.214635937601,114.449250561619,115.444461436068,116.439672310517,
117.434883184966,118.430094059415,119.425304933864,119.744945584229),
 .UNSPECIFIED.);
#2093=B_SPLINE_CURVE_WITH_KNOTS('',3,(#29280,#29281,#29282,#29283,#29284,
#29285,#29286,#29287,#29288,#29289,#29290,#29291,#29292,#29293,#29294,#29295,
#29296,#29297,#29298,#29299,#29300,#29301,#29302,#29303,#29304,#29305,#29306,
#29307,#29308,#29309,#29310,#29311,#29312,#29313,#29314,#29315,#29316,#29317,
#29318,#29319,#29320,#29321,#29322,#29323,#29324,#29325,#29326,#29327,#29328,
#29329,#29330,#29331,#29332,#29333,#29334,#29335,#29336,#29337,#29338,#29339,
#29340,#29341,#29342,#29343,#29344,#29345,#29346,#29347,#29348,#29349,#29350,
#29351,#29352,#29353,#29354,#29355,#29356,#29357,#29358,#29359,#29360,#29361,
#29362,#29363,#29364,#29365,#29366,#29367,#29368,#29369,#29370),
 .UNSPECIFIED.,.F.,.F.,(4,3,3,3,3,3,3,3,3,3,3,3,3,3,3,3,3,3,3,3,3,3,3,3,
3,3,3,3,3,3,4),(-0.555272788399385,-0.536419916279172,-0.511694572405047,
-0.497319076721282,-0.491892658567545,-0.487001163442623,-0.461206429703333,
-0.438766456173517,-0.427478497207602,-0.421962696929991,-0.395379115887254,
-0.366955997281641,-0.345638658327431,-0.329650654111773,-0.325133772019457,
-0.321069591482979,-0.293154594927527,-0.2816866414648,-0.254736587799489,
-0.227248158920029,-0.221184076554202,-0.216726936955391,-0.188773314511124,
-0.160283879462109,-0.131556417226141,-0.114343955822663,-0.109568083488329,
-0.0800957844431539,-0.0505511580101775,-0.0215769774899928,0.),
 .UNSPECIFIED.);
#2591=LINE('',#26400,#3137);
#2592=LINE('',#26424,#3138);
#2593=LINE('',#26472,#3139);
#2594=LINE('',#26520,#3140);
#2595=LINE('',#26574,#3141);
#2596=LINE('',#26622,#3142);
#2597=LINE('',#26670,#3143);
#2598=LINE('',#26724,#3144);
#2599=LINE('',#26772,#3145);
#2600=LINE('',#26820,#3146);
#2601=LINE('',#26868,#3147);
#2602=LINE('',#26922,#3148);
#2603=LINE('',#26970,#3149);
#2604=LINE('',#27018,#3150);
#2605=LINE('',#27072,#3151);
#2606=LINE('',#27120,#3152);
#2607=LINE('',#27168,#3153);
#2608=LINE('',#27222,#3154);
#2609=LINE('',#27270,#3155);
#2610=LINE('',#27318,#3156);
#2611=LINE('',#27343,#3157);
#2612=LINE('',#27368,#3158);
#2613=LINE('',#27392,#3159);
#2614=LINE('',#27417,#3160);
#2615=LINE('',#27442,#3161);
#2616=LINE('',#27466,#3162);
#2617=LINE('',#27491,#3163);
#2618=LINE('',#27516,#3164);
#2619=LINE('',#27540,#3165);
#2620=LINE('',#27565,#3166);
#2621=LINE('',#27590,#3167);
#2622=LINE('',#27614,#3168);
#2623=LINE('',#27638,#3169);
#2624=LINE('',#27663,#3170);
#2625=LINE('',#27688,#3171);
#2626=LINE('',#27712,#3172);
#2627=LINE('',#27737,#3173);
#2628=LINE('',#27762,#3174);
#2629=LINE('',#28101,#3175);
#2630=LINE('',#29375,#3176);
#2631=LINE('',#29377,#3177);
#2632=LINE('',#29379,#3178);
#2633=LINE('',#29380,#3179);
#2634=LINE('',#29383,#3180);
#2635=LINE('',#29385,#3181);
#2636=LINE('',#29386,#3182);
#2637=LINE('',#29389,#3183);
#2638=LINE('',#29391,#3184);
#2639=LINE('',#29392,#3185);
#2640=LINE('',#29395,#3186);
#2641=LINE('',#29397,#3187);
#2642=LINE('',#29398,#3188);
#2643=LINE('',#29401,#3189);
#2644=LINE('',#29403,#3190);
#2645=LINE('',#29404,#3191);
#2646=LINE('',#29406,#3192);
#2647=LINE('',#29407,#3193);
#2648=LINE('',#29414,#3194);
#3137=VECTOR('',#10873,3.);
#3138=VECTOR('',#10878,3.);
#3139=VECTOR('',#10881,3.);
#3140=VECTOR('',#10884,3.);
#3141=VECTOR('',#10887,3.);
#3142=VECTOR('',#10890,3.);
#3143=VECTOR('',#10893,3.);
#3144=VECTOR('',#10896,3.);
#3145=VECTOR('',#10899,3.);
#3146=VECTOR('',#10902,3.);
#3147=VECTOR('',#10905,3.);
#3148=VECTOR('',#10908,3.);
#3149=VECTOR('',#10911,3.);
#3150=VECTOR('',#10914,3.);
#3151=VECTOR('',#10917,3.);
#3152=VECTOR('',#10920,3.);
#3153=VECTOR('',#10923,3.);
#3154=VECTOR('',#10926,3.);
#3155=VECTOR('',#10929,3.);
#3156=VECTOR('',#10932,2.37175);
#3157=VECTOR('',#10937,2.37175);
#3158=VECTOR('',#10940,2.37175);
#3159=VECTOR('',#10943,2.37175);
#3160=VECTOR('',#10946,2.37175);
#3161=VECTOR('',#10949,2.37175);
#3162=VECTOR('',#10952,2.37175);
#3163=VECTOR('',#10955,2.37175);
#3164=VECTOR('',#10958,2.37175);
#3165=VECTOR('',#10961,2.37175);
#3166=VECTOR('',#10964,2.37175);
#3167=VECTOR('',#10967,2.37175);
#3168=VECTOR('',#10970,2.37175);
#3169=VECTOR('',#10973,2.37175);
#3170=VECTOR('',#10976,2.37175);
#3171=VECTOR('',#10979,2.37175);
#3172=VECTOR('',#10982,2.37175);
#3173=VECTOR('',#10985,2.37175);
#3174=VECTOR('',#10988,2.37175);
#3175=VECTOR('',#10993,2.5);
#3176=VECTOR('',#11004,10.);
#3177=VECTOR('',#11005,10.);
#3178=VECTOR('',#11006,10.);
#3179=VECTOR('',#11007,10.);
#3180=VECTOR('',#11010,10.);
#3181=VECTOR('',#11011,10.);
#3182=VECTOR('',#11012,10.);
#3183=VECTOR('',#11015,10.);
#3184=VECTOR('',#11016,10.);
#3185=VECTOR('',#11017,10.);
#3186=VECTOR('',#11020,10.);
#3187=VECTOR('',#11021,10.);
#3188=VECTOR('',#11022,10.);
#3189=VECTOR('',#11025,10.);
#3190=VECTOR('',#11026,10.);
#3191=VECTOR('',#11027,10.);
#3192=VECTOR('',#11030,10.);
#3193=VECTOR('',#11031,10.);
#3194=VECTOR('',#11040,5.);
#3895=VERTEX_POINT('',#26398);
#3896=VERTEX_POINT('',#26399);
#3897=VERTEX_POINT('',#26401);
#3898=VERTEX_POINT('',#26412);
#3899=VERTEX_POINT('',#26422);
#3900=VERTEX_POINT('',#26423);
#3901=VERTEX_POINT('',#26470);
#3902=VERTEX_POINT('',#26471);
#3903=VERTEX_POINT('',#26518);
#3904=VERTEX_POINT('',#26519);
#3905=VERTEX_POINT('',#26572);
#3906=VERTEX_POINT('',#26573);
#3907=VERTEX_POINT('',#26620);
#3908=VERTEX_POINT('',#26621);
#3909=VERTEX_POINT('',#26668);
#3910=VERTEX_POINT('',#26669);
#3911=VERTEX_POINT('',#26722);
#3912=VERTEX_POINT('',#26723);
#3913=VERTEX_POINT('',#26770);
#3914=VERTEX_POINT('',#26771);
#3915=VERTEX_POINT('',#26818);
#3916=VERTEX_POINT('',#26819);
#3917=VERTEX_POINT('',#26866);
#3918=VERTEX_POINT('',#26867);
#3919=VERTEX_POINT('',#26920);
#3920=VERTEX_POINT('',#26921);
#3921=VERTEX_POINT('',#26968);
#3922=VERTEX_POINT('',#26969);
#3923=VERTEX_POINT('',#27016);
#3924=VERTEX_POINT('',#27017);
#3925=VERTEX_POINT('',#27070);
#3926=VERTEX_POINT('',#27071);
#3927=VERTEX_POINT('',#27118);
#3928=VERTEX_POINT('',#27119);
#3929=VERTEX_POINT('',#27166);
#3930=VERTEX_POINT('',#27167);
#3931=VERTEX_POINT('',#27220);
#3932=VERTEX_POINT('',#27221);
#3933=VERTEX_POINT('',#27268);
#3934=VERTEX_POINT('',#27269);
#3935=VERTEX_POINT('',#27316);
#3936=VERTEX_POINT('',#27317);
#3937=VERTEX_POINT('',#27319);
#3938=VERTEX_POINT('',#27330);
#3939=VERTEX_POINT('',#27341);
#3940=VERTEX_POINT('',#27342);
#3941=VERTEX_POINT('',#27366);
#3942=VERTEX_POINT('',#27367);
#3943=VERTEX_POINT('',#27390);
#3944=VERTEX_POINT('',#27391);
#3945=VERTEX_POINT('',#27415);
#3946=VERTEX_POINT('',#27416);
#3947=VERTEX_POINT('',#27440);
#3948=VERTEX_POINT('',#27441);
#3949=VERTEX_POINT('',#27464);
#3950=VERTEX_POINT('',#27465);
#3951=VERTEX_POINT('',#27489);
#3952=VERTEX_POINT('',#27490);
#3953=VERTEX_POINT('',#27514);
#3954=VERTEX_POINT('',#27515);
#3955=VERTEX_POINT('',#27538);
#3956=VERTEX_POINT('',#27539);
#3957=VERTEX_POINT('',#27563);
#3958=VERTEX_POINT('',#27564);
#3959=VERTEX_POINT('',#27588);
#3960=VERTEX_POINT('',#27589);
#3961=VERTEX_POINT('',#27612);
#3962=VERTEX_POINT('',#27613);
#3963=VERTEX_POINT('',#27636);
#3964=VERTEX_POINT('',#27637);
#3965=VERTEX_POINT('',#27661);
#3966=VERTEX_POINT('',#27662);
#3967=VERTEX_POINT('',#27686);
#3968=VERTEX_POINT('',#27687);
#3969=VERTEX_POINT('',#27710);
#3970=VERTEX_POINT('',#27711);
#3971=VERTEX_POINT('',#27735);
#3972=VERTEX_POINT('',#27736);
#3973=VERTEX_POINT('',#27760);
#3974=VERTEX_POINT('',#27761);
#3975=VERTEX_POINT('',#27784);
#3976=VERTEX_POINT('',#28002);
#3977=VERTEX_POINT('',#28067);
#3978=VERTEX_POINT('',#28100);
#3979=VERTEX_POINT('',#28611);
#3980=VERTEX_POINT('',#28731);
#3981=VERTEX_POINT('',#29373);
#3982=VERTEX_POINT('',#29374);
#3983=VERTEX_POINT('',#29376);
#3984=VERTEX_POINT('',#29378);
#3985=VERTEX_POINT('',#29382);
#3986=VERTEX_POINT('',#29384);
#3987=VERTEX_POINT('',#29388);
#3988=VERTEX_POINT('',#29390);
#3989=VERTEX_POINT('',#29394);
#3990=VERTEX_POINT('',#29396);
#3991=VERTEX_POINT('',#29400);
#3992=VERTEX_POINT('',#29402);
#3993=VERTEX_POINT('',#29410);
#3994=VERTEX_POINT('',#29413);
#5049=EDGE_CURVE('',#3895,#3896,#2591,.T.);
#5050=EDGE_CURVE('',#3895,#3897,#2009,.T.);
#5051=EDGE_CURVE('',#3897,#3898,#1563,.F.);
#5052=EDGE_CURVE('',#3898,#3896,#2010,.T.);
#5053=EDGE_CURVE('',#3899,#3900,#2592,.T.);
#5054=EDGE_CURVE('',#3899,#3895,#2011,.T.);
#5055=EDGE_CURVE('',#3896,#3900,#2012,.T.);
#5056=EDGE_CURVE('',#3901,#3902,#2593,.T.);
#5057=EDGE_CURVE('',#3901,#3899,#2013,.T.);
#5058=EDGE_CURVE('',#3900,#3902,#2014,.T.);
#5059=EDGE_CURVE('',#3903,#3904,#2594,.T.);
#5060=EDGE_CURVE('',#3903,#3901,#2015,.T.);
#5061=EDGE_CURVE('',#3902,#3904,#2016,.T.);
#5062=EDGE_CURVE('',#3905,#3906,#2595,.T.);
#5063=EDGE_CURVE('',#3905,#3903,#2017,.T.);
#5064=EDGE_CURVE('',#3904,#3906,#2018,.T.);
#5065=EDGE_CURVE('',#3907,#3908,#2596,.T.);
#5066=EDGE_CURVE('',#3907,#3905,#2019,.T.);
#5067=EDGE_CURVE('',#3906,#3908,#2020,.T.);
#5068=EDGE_CURVE('',#3909,#3910,#2597,.T.);
#5069=EDGE_CURVE('',#3909,#3907,#2021,.T.);
#5070=EDGE_CURVE('',#3908,#3910,#2022,.T.);
#5071=EDGE_CURVE('',#3911,#3912,#2598,.T.);
#5072=EDGE_CURVE('',#3911,#3909,#2023,.T.);
#5073=EDGE_CURVE('',#3910,#3912,#2024,.T.);
#5074=EDGE_CURVE('',#3913,#3914,#2599,.T.);
#5075=EDGE_CURVE('',#3913,#3911,#2025,.T.);
#5076=EDGE_CURVE('',#3912,#3914,#2026,.T.);
#5077=EDGE_CURVE('',#3915,#3916,#2600,.T.);
#5078=EDGE_CURVE('',#3915,#3913,#2027,.T.);
#5079=EDGE_CURVE('',#3914,#3916,#2028,.T.);
#5080=EDGE_CURVE('',#3917,#3918,#2601,.T.);
#5081=EDGE_CURVE('',#3917,#3915,#2029,.T.);
#5082=EDGE_CURVE('',#3916,#3918,#2030,.T.);
#5083=EDGE_CURVE('',#3919,#3920,#2602,.T.);
#5084=EDGE_CURVE('',#3919,#3917,#2031,.T.);
#5085=EDGE_CURVE('',#3918,#3920,#2032,.T.);
#5086=EDGE_CURVE('',#3921,#3922,#2603,.T.);
#5087=EDGE_CURVE('',#3921,#3919,#2033,.T.);
#5088=EDGE_CURVE('',#3920,#3922,#2034,.T.);
#5089=EDGE_CURVE('',#3923,#3924,#2604,.T.);
#5090=EDGE_CURVE('',#3923,#3921,#2035,.T.);
#5091=EDGE_CURVE('',#3922,#3924,#2036,.T.);
#5092=EDGE_CURVE('',#3925,#3926,#2605,.T.);
#5093=EDGE_CURVE('',#3925,#3923,#2037,.T.);
#5094=EDGE_CURVE('',#3924,#3926,#2038,.T.);
#5095=EDGE_CURVE('',#3927,#3928,#2606,.T.);
#5096=EDGE_CURVE('',#3927,#3925,#2039,.T.);
#5097=EDGE_CURVE('',#3926,#3928,#2040,.T.);
#5098=EDGE_CURVE('',#3929,#3930,#2607,.T.);
#5099=EDGE_CURVE('',#3929,#3927,#2041,.T.);
#5100=EDGE_CURVE('',#3928,#3930,#2042,.T.);
#5101=EDGE_CURVE('',#3931,#3932,#2608,.T.);
#5102=EDGE_CURVE('',#3931,#3929,#2043,.T.);
#5103=EDGE_CURVE('',#3930,#3932,#2044,.T.);
#5104=EDGE_CURVE('',#3933,#3934,#2609,.T.);
#5105=EDGE_CURVE('',#3933,#3931,#2045,.T.);
#5106=EDGE_CURVE('',#3932,#3934,#2046,.T.);
#5107=EDGE_CURVE('',#3935,#3936,#2610,.T.);
#5108=EDGE_CURVE('',#3935,#3937,#2047,.T.);
#5109=EDGE_CURVE('',#3937,#3938,#1564,.T.);
#5110=EDGE_CURVE('',#3936,#3938,#2048,.T.);
#5111=EDGE_CURVE('',#3939,#3940,#2611,.T.);
#5112=EDGE_CURVE('',#3939,#3935,#2049,.T.);
#5113=EDGE_CURVE('',#3940,#3936,#2050,.T.);
#5114=EDGE_CURVE('',#3941,#3942,#2612,.T.);
#5115=EDGE_CURVE('',#3941,#3939,#2051,.T.);
#5116=EDGE_CURVE('',#3942,#3940,#2052,.T.);
#5117=EDGE_CURVE('',#3943,#3944,#2613,.T.);
#5118=EDGE_CURVE('',#3943,#3941,#2053,.T.);
#5119=EDGE_CURVE('',#3944,#3942,#2054,.T.);
#5120=EDGE_CURVE('',#3945,#3946,#2614,.T.);
#5121=EDGE_CURVE('',#3945,#3943,#2055,.T.);
#5122=EDGE_CURVE('',#3946,#3944,#2056,.T.);
#5123=EDGE_CURVE('',#3947,#3948,#2615,.T.);
#5124=EDGE_CURVE('',#3947,#3945,#2057,.T.);
#5125=EDGE_CURVE('',#3948,#3946,#2058,.T.);
#5126=EDGE_CURVE('',#3949,#3950,#2616,.T.);
#5127=EDGE_CURVE('',#3949,#3947,#2059,.T.);
#5128=EDGE_CURVE('',#3950,#3948,#2060,.T.);
#5129=EDGE_CURVE('',#3951,#3952,#2617,.T.);
#5130=EDGE_CURVE('',#3951,#3949,#2061,.T.);
#5131=EDGE_CURVE('',#3952,#3950,#2062,.T.);
#5132=EDGE_CURVE('',#3953,#3954,#2618,.T.);
#5133=EDGE_CURVE('',#3953,#3951,#2063,.T.);
#5134=EDGE_CURVE('',#3954,#3952,#2064,.T.);
#5135=EDGE_CURVE('',#3955,#3956,#2619,.T.);
#5136=EDGE_CURVE('',#3955,#3953,#2065,.T.);
#5137=EDGE_CURVE('',#3956,#3954,#2066,.T.);
#5138=EDGE_CURVE('',#3957,#3958,#2620,.T.);
#5139=EDGE_CURVE('',#3957,#3955,#2067,.T.);
#5140=EDGE_CURVE('',#3958,#3956,#2068,.T.);
#5141=EDGE_CURVE('',#3959,#3960,#2621,.T.);
#5142=EDGE_CURVE('',#3959,#3957,#2069,.T.);
#5143=EDGE_CURVE('',#3960,#3958,#2070,.T.);
#5144=EDGE_CURVE('',#3961,#3962,#2622,.T.);
#5145=EDGE_CURVE('',#3961,#3959,#2071,.T.);
#5146=EDGE_CURVE('',#3962,#3960,#2072,.T.);
#5147=EDGE_CURVE('',#3963,#3964,#2623,.T.);
#5148=EDGE_CURVE('',#3963,#3961,#2073,.T.);
#5149=EDGE_CURVE('',#3964,#3962,#2074,.T.);
#5150=EDGE_CURVE('',#3965,#3966,#2624,.T.);
#5151=EDGE_CURVE('',#3965,#3963,#2075,.T.);
#5152=EDGE_CURVE('',#3966,#3964,#2076,.T.);
#5153=EDGE_CURVE('',#3967,#3968,#2625,.T.);
#5154=EDGE_CURVE('',#3967,#3965,#2077,.T.);
#5155=EDGE_CURVE('',#3968,#3966,#2078,.T.);
#5156=EDGE_CURVE('',#3969,#3970,#2626,.T.);
#5157=EDGE_CURVE('',#3969,#3967,#2079,.T.);
#5158=EDGE_CURVE('',#3970,#3968,#2080,.T.);
#5159=EDGE_CURVE('',#3971,#3972,#2627,.T.);
#5160=EDGE_CURVE('',#3971,#3969,#2081,.T.);
#5161=EDGE_CURVE('',#3972,#3970,#2082,.T.);
#5162=EDGE_CURVE('',#3973,#3974,#2628,.T.);
#5163=EDGE_CURVE('',#3973,#3971,#2083,.T.);
#5164=EDGE_CURVE('',#3974,#3972,#2084,.T.);
#5165=EDGE_CURVE('',#3938,#3975,#2085,.T.);
#5166=EDGE_CURVE('',#3976,#3937,#2086,.T.);
#5167=EDGE_CURVE('',#3977,#3976,#1565,.T.);
#5168=EDGE_CURVE('',#3975,#3977,#2087,.T.);
#5169=EDGE_CURVE('',#3975,#3978,#2629,.T.);
#5170=EDGE_CURVE('',#3978,#3978,#1566,.T.);
#5171=EDGE_CURVE('',#3979,#3973,#2088,.T.);
#5172=EDGE_CURVE('',#3897,#3979,#2089,.T.);
#5173=EDGE_CURVE('',#3976,#3933,#2090,.T.);
#5174=EDGE_CURVE('',#3980,#3974,#2091,.T.);
#5175=EDGE_CURVE('',#3979,#3980,#1567,.T.);
#5176=EDGE_CURVE('',#3934,#3977,#2092,.T.);
#5177=EDGE_CURVE('',#3980,#3898,#2093,.T.);
#5178=EDGE_CURVE('',#3981,#3982,#2630,.T.);
#5179=EDGE_CURVE('',#3981,#3983,#2631,.T.);
#5180=EDGE_CURVE('',#3983,#3984,#2632,.T.);
#5181=EDGE_CURVE('',#3982,#3984,#2633,.T.);
#5182=EDGE_CURVE('',#3985,#3981,#2634,.T.);
#5183=EDGE_CURVE('',#3985,#3986,#2635,.T.);
#5184=EDGE_CURVE('',#3986,#3983,#2636,.T.);
#5185=EDGE_CURVE('',#3987,#3985,#2637,.T.);
#5186=EDGE_CURVE('',#3987,#3988,#2638,.T.);
#5187=EDGE_CURVE('',#3988,#3986,#2639,.T.);
#5188=EDGE_CURVE('',#3989,#3987,#2640,.T.);
#5189=EDGE_CURVE('',#3989,#3990,#2641,.T.);
#5190=EDGE_CURVE('',#3990,#3988,#2642,.T.);
#5191=EDGE_CURVE('',#3991,#3989,#2643,.T.);
#5192=EDGE_CURVE('',#3991,#3992,#2644,.T.);
#5193=EDGE_CURVE('',#3992,#3990,#2645,.T.);
#5194=EDGE_CURVE('',#3982,#3991,#2646,.T.);
#5195=EDGE_CURVE('',#3984,#3992,#2647,.T.);
#5196=EDGE_CURVE('',#3993,#3993,#1568,.T.);
#5197=EDGE_CURVE('',#3993,#3994,#2648,.T.);
#5198=EDGE_CURVE('',#3994,#3994,#1569,.T.);
#7251=ORIENTED_EDGE('',*,*,#5049,.F.);
#7252=ORIENTED_EDGE('',*,*,#5050,.T.);
#7253=ORIENTED_EDGE('',*,*,#5051,.T.);
#7254=ORIENTED_EDGE('',*,*,#5052,.T.);
#7255=ORIENTED_EDGE('',*,*,#5053,.F.);
#7256=ORIENTED_EDGE('',*,*,#5054,.T.);
#7257=ORIENTED_EDGE('',*,*,#5049,.T.);
#7258=ORIENTED_EDGE('',*,*,#5055,.T.);
#7259=ORIENTED_EDGE('',*,*,#5056,.F.);
#7260=ORIENTED_EDGE('',*,*,#5057,.T.);
#7261=ORIENTED_EDGE('',*,*,#5053,.T.);
#7262=ORIENTED_EDGE('',*,*,#5058,.T.);
#7263=ORIENTED_EDGE('',*,*,#5059,.F.);
#7264=ORIENTED_EDGE('',*,*,#5060,.T.);
#7265=ORIENTED_EDGE('',*,*,#5056,.T.);
#7266=ORIENTED_EDGE('',*,*,#5061,.T.);
#7267=ORIENTED_EDGE('',*,*,#5062,.F.);
#7268=ORIENTED_EDGE('',*,*,#5063,.T.);
#7269=ORIENTED_EDGE('',*,*,#5059,.T.);
#7270=ORIENTED_EDGE('',*,*,#5064,.T.);
#7271=ORIENTED_EDGE('',*,*,#5065,.F.);
#7272=ORIENTED_EDGE('',*,*,#5066,.T.);
#7273=ORIENTED_EDGE('',*,*,#5062,.T.);
#7274=ORIENTED_EDGE('',*,*,#5067,.T.);
#7275=ORIENTED_EDGE('',*,*,#5068,.F.);
#7276=ORIENTED_EDGE('',*,*,#5069,.T.);
#7277=ORIENTED_EDGE('',*,*,#5065,.T.);
#7278=ORIENTED_EDGE('',*,*,#5070,.T.);
#7279=ORIENTED_EDGE('',*,*,#5071,.F.);
#7280=ORIENTED_EDGE('',*,*,#5072,.T.);
#7281=ORIENTED_EDGE('',*,*,#5068,.T.);
#7282=ORIENTED_EDGE('',*,*,#5073,.T.);
#7283=ORIENTED_EDGE('',*,*,#5074,.F.);
#7284=ORIENTED_EDGE('',*,*,#5075,.T.);
#7285=ORIENTED_EDGE('',*,*,#5071,.T.);
#7286=ORIENTED_EDGE('',*,*,#5076,.T.);
#7287=ORIENTED_EDGE('',*,*,#5077,.F.);
#7288=ORIENTED_EDGE('',*,*,#5078,.T.);
#7289=ORIENTED_EDGE('',*,*,#5074,.T.);
#7290=ORIENTED_EDGE('',*,*,#5079,.T.);
#7291=ORIENTED_EDGE('',*,*,#5080,.F.);
#7292=ORIENTED_EDGE('',*,*,#5081,.T.);
#7293=ORIENTED_EDGE('',*,*,#5077,.T.);
#7294=ORIENTED_EDGE('',*,*,#5082,.T.);
#7295=ORIENTED_EDGE('',*,*,#5083,.F.);
#7296=ORIENTED_EDGE('',*,*,#5084,.T.);
#7297=ORIENTED_EDGE('',*,*,#5080,.T.);
#7298=ORIENTED_EDGE('',*,*,#5085,.T.);
#7299=ORIENTED_EDGE('',*,*,#5086,.F.);
#7300=ORIENTED_EDGE('',*,*,#5087,.T.);
#7301=ORIENTED_EDGE('',*,*,#5083,.T.);
#7302=ORIENTED_EDGE('',*,*,#5088,.T.);
#7303=ORIENTED_EDGE('',*,*,#5089,.F.);
#7304=ORIENTED_EDGE('',*,*,#5090,.T.);
#7305=ORIENTED_EDGE('',*,*,#5086,.T.);
#7306=ORIENTED_EDGE('',*,*,#5091,.T.);
#7307=ORIENTED_EDGE('',*,*,#5092,.F.);
#7308=ORIENTED_EDGE('',*,*,#5093,.T.);
#7309=ORIENTED_EDGE('',*,*,#5089,.T.);
#7310=ORIENTED_EDGE('',*,*,#5094,.T.);
#7311=ORIENTED_EDGE('',*,*,#5095,.F.);
#7312=ORIENTED_EDGE('',*,*,#5096,.T.);
#7313=ORIENTED_EDGE('',*,*,#5092,.T.);
#7314=ORIENTED_EDGE('',*,*,#5097,.T.);
#7315=ORIENTED_EDGE('',*,*,#5098,.F.);
#7316=ORIENTED_EDGE('',*,*,#5099,.T.);
#7317=ORIENTED_EDGE('',*,*,#5095,.T.);
#7318=ORIENTED_EDGE('',*,*,#5100,.T.);
#7319=ORIENTED_EDGE('',*,*,#5101,.F.);
#7320=ORIENTED_EDGE('',*,*,#5102,.T.);
#7321=ORIENTED_EDGE('',*,*,#5098,.T.);
#7322=ORIENTED_EDGE('',*,*,#5103,.T.);
#7323=ORIENTED_EDGE('',*,*,#5104,.F.);
#7324=ORIENTED_EDGE('',*,*,#5105,.T.);
#7325=ORIENTED_EDGE('',*,*,#5101,.T.);
#7326=ORIENTED_EDGE('',*,*,#5106,.T.);
#7327=ORIENTED_EDGE('',*,*,#5107,.F.);
#7328=ORIENTED_EDGE('',*,*,#5108,.T.);
#7329=ORIENTED_EDGE('',*,*,#5109,.T.);
#7330=ORIENTED_EDGE('',*,*,#5110,.F.);
#7331=ORIENTED_EDGE('',*,*,#5111,.F.);
#7332=ORIENTED_EDGE('',*,*,#5112,.T.);
#7333=ORIENTED_EDGE('',*,*,#5107,.T.);
#7334=ORIENTED_EDGE('',*,*,#5113,.F.);
#7335=ORIENTED_EDGE('',*,*,#5114,.F.);
#7336=ORIENTED_EDGE('',*,*,#5115,.T.);
#7337=ORIENTED_EDGE('',*,*,#5111,.T.);
#7338=ORIENTED_EDGE('',*,*,#5116,.F.);
#7339=ORIENTED_EDGE('',*,*,#5117,.F.);
#7340=ORIENTED_EDGE('',*,*,#5118,.T.);
#7341=ORIENTED_EDGE('',*,*,#5114,.T.);
#7342=ORIENTED_EDGE('',*,*,#5119,.F.);
#7343=ORIENTED_EDGE('',*,*,#5120,.F.);
#7344=ORIENTED_EDGE('',*,*,#5121,.T.);
#7345=ORIENTED_EDGE('',*,*,#5117,.T.);
#7346=ORIENTED_EDGE('',*,*,#5122,.F.);
#7347=ORIENTED_EDGE('',*,*,#5123,.F.);
#7348=ORIENTED_EDGE('',*,*,#5124,.T.);
#7349=ORIENTED_EDGE('',*,*,#5120,.T.);
#7350=ORIENTED_EDGE('',*,*,#5125,.F.);
#7351=ORIENTED_EDGE('',*,*,#5126,.F.);
#7352=ORIENTED_EDGE('',*,*,#5127,.T.);
#7353=ORIENTED_EDGE('',*,*,#5123,.T.);
#7354=ORIENTED_EDGE('',*,*,#5128,.F.);
#7355=ORIENTED_EDGE('',*,*,#5129,.F.);
#7356=ORIENTED_EDGE('',*,*,#5130,.T.);
#7357=ORIENTED_EDGE('',*,*,#5126,.T.);
#7358=ORIENTED_EDGE('',*,*,#5131,.F.);
#7359=ORIENTED_EDGE('',*,*,#5132,.F.);
#7360=ORIENTED_EDGE('',*,*,#5133,.T.);
#7361=ORIENTED_EDGE('',*,*,#5129,.T.);
#7362=ORIENTED_EDGE('',*,*,#5134,.F.);
#7363=ORIENTED_EDGE('',*,*,#5135,.F.);
#7364=ORIENTED_EDGE('',*,*,#5136,.T.);
#7365=ORIENTED_EDGE('',*,*,#5132,.T.);
#7366=ORIENTED_EDGE('',*,*,#5137,.F.);
#7367=ORIENTED_EDGE('',*,*,#5138,.F.);
#7368=ORIENTED_EDGE('',*,*,#5139,.T.);
#7369=ORIENTED_EDGE('',*,*,#5135,.T.);
#7370=ORIENTED_EDGE('',*,*,#5140,.F.);
#7371=ORIENTED_EDGE('',*,*,#5141,.F.);
#7372=ORIENTED_EDGE('',*,*,#5142,.T.);
#7373=ORIENTED_EDGE('',*,*,#5138,.T.);
#7374=ORIENTED_EDGE('',*,*,#5143,.F.);
#7375=ORIENTED_EDGE('',*,*,#5144,.F.);
#7376=ORIENTED_EDGE('',*,*,#5145,.T.);
#7377=ORIENTED_EDGE('',*,*,#5141,.T.);
#7378=ORIENTED_EDGE('',*,*,#5146,.F.);
#7379=ORIENTED_EDGE('',*,*,#5147,.F.);
#7380=ORIENTED_EDGE('',*,*,#5148,.T.);
#7381=ORIENTED_EDGE('',*,*,#5144,.T.);
#7382=ORIENTED_EDGE('',*,*,#5149,.F.);
#7383=ORIENTED_EDGE('',*,*,#5150,.F.);
#7384=ORIENTED_EDGE('',*,*,#5151,.T.);
#7385=ORIENTED_EDGE('',*,*,#5147,.T.);
#7386=ORIENTED_EDGE('',*,*,#5152,.F.);
#7387=ORIENTED_EDGE('',*,*,#5153,.F.);
#7388=ORIENTED_EDGE('',*,*,#5154,.T.);
#7389=ORIENTED_EDGE('',*,*,#5150,.T.);
#7390=ORIENTED_EDGE('',*,*,#5155,.F.);
#7391=ORIENTED_EDGE('',*,*,#5156,.F.);
#7392=ORIENTED_EDGE('',*,*,#5157,.T.);
#7393=ORIENTED_EDGE('',*,*,#5153,.T.);
#7394=ORIENTED_EDGE('',*,*,#5158,.F.);
#7395=ORIENTED_EDGE('',*,*,#5159,.F.);
#7396=ORIENTED_EDGE('',*,*,#5160,.T.);
#7397=ORIENTED_EDGE('',*,*,#5156,.T.);
#7398=ORIENTED_EDGE('',*,*,#5161,.F.);
#7399=ORIENTED_EDGE('',*,*,#5162,.F.);
#7400=ORIENTED_EDGE('',*,*,#5163,.T.);
#7401=ORIENTED_EDGE('',*,*,#5159,.T.);
#7402=ORIENTED_EDGE('',*,*,#5164,.F.);
#7403=ORIENTED_EDGE('',*,*,#5165,.F.);
#7404=ORIENTED_EDGE('',*,*,#5109,.F.);
#7405=ORIENTED_EDGE('',*,*,#5166,.F.);
#7406=ORIENTED_EDGE('',*,*,#5167,.F.);
#7407=ORIENTED_EDGE('',*,*,#5168,.F.);
#7408=ORIENTED_EDGE('',*,*,#5169,.T.);
#7409=ORIENTED_EDGE('',*,*,#5170,.F.);
#7410=ORIENTED_EDGE('',*,*,#5169,.F.);
#7411=ORIENTED_EDGE('',*,*,#5166,.T.);
#7412=ORIENTED_EDGE('',*,*,#5108,.F.);
#7413=ORIENTED_EDGE('',*,*,#5112,.F.);
#7414=ORIENTED_EDGE('',*,*,#5115,.F.);
#7415=ORIENTED_EDGE('',*,*,#5118,.F.);
#7416=ORIENTED_EDGE('',*,*,#5121,.F.);
#7417=ORIENTED_EDGE('',*,*,#5124,.F.);
#7418=ORIENTED_EDGE('',*,*,#5127,.F.);
#7419=ORIENTED_EDGE('',*,*,#5130,.F.);
#7420=ORIENTED_EDGE('',*,*,#5133,.F.);
#7421=ORIENTED_EDGE('',*,*,#5136,.F.);
#7422=ORIENTED_EDGE('',*,*,#5139,.F.);
#7423=ORIENTED_EDGE('',*,*,#5142,.F.);
#7424=ORIENTED_EDGE('',*,*,#5145,.F.);
#7425=ORIENTED_EDGE('',*,*,#5148,.F.);
#7426=ORIENTED_EDGE('',*,*,#5151,.F.);
#7427=ORIENTED_EDGE('',*,*,#5154,.F.);
#7428=ORIENTED_EDGE('',*,*,#5157,.F.);
#7429=ORIENTED_EDGE('',*,*,#5160,.F.);
#7430=ORIENTED_EDGE('',*,*,#5163,.F.);
#7431=ORIENTED_EDGE('',*,*,#5171,.F.);
#7432=ORIENTED_EDGE('',*,*,#5172,.F.);
#7433=ORIENTED_EDGE('',*,*,#5050,.F.);
#7434=ORIENTED_EDGE('',*,*,#5054,.F.);
#7435=ORIENTED_EDGE('',*,*,#5057,.F.);
#7436=ORIENTED_EDGE('',*,*,#5060,.F.);
#7437=ORIENTED_EDGE('',*,*,#5063,.F.);
#7438=ORIENTED_EDGE('',*,*,#5066,.F.);
#7439=ORIENTED_EDGE('',*,*,#5069,.F.);
#7440=ORIENTED_EDGE('',*,*,#5072,.F.);
#7441=ORIENTED_EDGE('',*,*,#5075,.F.);
#7442=ORIENTED_EDGE('',*,*,#5078,.F.);
#7443=ORIENTED_EDGE('',*,*,#5081,.F.);
#7444=ORIENTED_EDGE('',*,*,#5084,.F.);
#7445=ORIENTED_EDGE('',*,*,#5087,.F.);
#7446=ORIENTED_EDGE('',*,*,#5090,.F.);
#7447=ORIENTED_EDGE('',*,*,#5093,.F.);
#7448=ORIENTED_EDGE('',*,*,#5096,.F.);
#7449=ORIENTED_EDGE('',*,*,#5099,.F.);
#7450=ORIENTED_EDGE('',*,*,#5102,.F.);
#7451=ORIENTED_EDGE('',*,*,#5105,.F.);
#7452=ORIENTED_EDGE('',*,*,#5173,.F.);
#7453=ORIENTED_EDGE('',*,*,#5162,.T.);
#7454=ORIENTED_EDGE('',*,*,#5174,.F.);
#7455=ORIENTED_EDGE('',*,*,#5175,.F.);
#7456=ORIENTED_EDGE('',*,*,#5171,.T.);
#7457=ORIENTED_EDGE('',*,*,#5165,.T.);
#7458=ORIENTED_EDGE('',*,*,#5168,.T.);
#7459=ORIENTED_EDGE('',*,*,#5176,.F.);
#7460=ORIENTED_EDGE('',*,*,#5106,.F.);
#7461=ORIENTED_EDGE('',*,*,#5103,.F.);
#7462=ORIENTED_EDGE('',*,*,#5100,.F.);
#7463=ORIENTED_EDGE('',*,*,#5097,.F.);
#7464=ORIENTED_EDGE('',*,*,#5094,.F.);
#7465=ORIENTED_EDGE('',*,*,#5091,.F.);
#7466=ORIENTED_EDGE('',*,*,#5088,.F.);
#7467=ORIENTED_EDGE('',*,*,#5085,.F.);
#7468=ORIENTED_EDGE('',*,*,#5082,.F.);
#7469=ORIENTED_EDGE('',*,*,#5079,.F.);
#7470=ORIENTED_EDGE('',*,*,#5076,.F.);
#7471=ORIENTED_EDGE('',*,*,#5073,.F.);
#7472=ORIENTED_EDGE('',*,*,#5070,.F.);
#7473=ORIENTED_EDGE('',*,*,#5067,.F.);
#7474=ORIENTED_EDGE('',*,*,#5064,.F.);
#7475=ORIENTED_EDGE('',*,*,#5061,.F.);
#7476=ORIENTED_EDGE('',*,*,#5058,.F.);
#7477=ORIENTED_EDGE('',*,*,#5055,.F.);
#7478=ORIENTED_EDGE('',*,*,#5052,.F.);
#7479=ORIENTED_EDGE('',*,*,#5177,.F.);
#7480=ORIENTED_EDGE('',*,*,#5174,.T.);
#7481=ORIENTED_EDGE('',*,*,#5164,.T.);
#7482=ORIENTED_EDGE('',*,*,#5161,.T.);
#7483=ORIENTED_EDGE('',*,*,#5158,.T.);
#7484=ORIENTED_EDGE('',*,*,#5155,.T.);
#7485=ORIENTED_EDGE('',*,*,#5152,.T.);
#7486=ORIENTED_EDGE('',*,*,#5149,.T.);
#7487=ORIENTED_EDGE('',*,*,#5146,.T.);
#7488=ORIENTED_EDGE('',*,*,#5143,.T.);
#7489=ORIENTED_EDGE('',*,*,#5140,.T.);
#7490=ORIENTED_EDGE('',*,*,#5137,.T.);
#7491=ORIENTED_EDGE('',*,*,#5134,.T.);
#7492=ORIENTED_EDGE('',*,*,#5131,.T.);
#7493=ORIENTED_EDGE('',*,*,#5128,.T.);
#7494=ORIENTED_EDGE('',*,*,#5125,.T.);
#7495=ORIENTED_EDGE('',*,*,#5122,.T.);
#7496=ORIENTED_EDGE('',*,*,#5119,.T.);
#7497=ORIENTED_EDGE('',*,*,#5116,.T.);
#7498=ORIENTED_EDGE('',*,*,#5113,.T.);
#7499=ORIENTED_EDGE('',*,*,#5110,.T.);
#7500=ORIENTED_EDGE('',*,*,#5104,.T.);
#7501=ORIENTED_EDGE('',*,*,#5176,.T.);
#7502=ORIENTED_EDGE('',*,*,#5167,.T.);
#7503=ORIENTED_EDGE('',*,*,#5173,.T.);
#7504=ORIENTED_EDGE('',*,*,#5178,.F.);
#7505=ORIENTED_EDGE('',*,*,#5179,.T.);
#7506=ORIENTED_EDGE('',*,*,#5180,.T.);
#7507=ORIENTED_EDGE('',*,*,#5181,.F.);
#7508=ORIENTED_EDGE('',*,*,#5182,.F.);
#7509=ORIENTED_EDGE('',*,*,#5183,.T.);
#7510=ORIENTED_EDGE('',*,*,#5184,.T.);
#7511=ORIENTED_EDGE('',*,*,#5179,.F.);
#7512=ORIENTED_EDGE('',*,*,#5185,.F.);
#7513=ORIENTED_EDGE('',*,*,#5186,.T.);
#7514=ORIENTED_EDGE('',*,*,#5187,.T.);
#7515=ORIENTED_EDGE('',*,*,#5183,.F.);
#7516=ORIENTED_EDGE('',*,*,#5188,.F.);
#7517=ORIENTED_EDGE('',*,*,#5189,.T.);
#7518=ORIENTED_EDGE('',*,*,#5190,.T.);
#7519=ORIENTED_EDGE('',*,*,#5186,.F.);
#7520=ORIENTED_EDGE('',*,*,#5191,.F.);
#7521=ORIENTED_EDGE('',*,*,#5192,.T.);
#7522=ORIENTED_EDGE('',*,*,#5193,.T.);
#7523=ORIENTED_EDGE('',*,*,#5189,.F.);
#7524=ORIENTED_EDGE('',*,*,#5194,.F.);
#7525=ORIENTED_EDGE('',*,*,#5181,.T.);
#7526=ORIENTED_EDGE('',*,*,#5195,.T.);
#7527=ORIENTED_EDGE('',*,*,#5192,.F.);
#7528=ORIENTED_EDGE('',*,*,#5195,.F.);
#7529=ORIENTED_EDGE('',*,*,#5180,.F.);
#7530=ORIENTED_EDGE('',*,*,#5184,.F.);
#7531=ORIENTED_EDGE('',*,*,#5187,.F.);
#7532=ORIENTED_EDGE('',*,*,#5190,.F.);
#7533=ORIENTED_EDGE('',*,*,#5193,.F.);
#7534=ORIENTED_EDGE('',*,*,#5196,.T.);
#7535=ORIENTED_EDGE('',*,*,#5172,.T.);
#7536=ORIENTED_EDGE('',*,*,#5175,.T.);
#7537=ORIENTED_EDGE('',*,*,#5177,.T.);
#7538=ORIENTED_EDGE('',*,*,#5051,.F.);
#7539=ORIENTED_EDGE('',*,*,#5196,.F.);
#7540=ORIENTED_EDGE('',*,*,#5197,.T.);
#7541=ORIENTED_EDGE('',*,*,#5198,.T.);
#7542=ORIENTED_EDGE('',*,*,#5197,.F.);
#7543=ORIENTED_EDGE('',*,*,#5198,.F.);
#7544=ORIENTED_EDGE('',*,*,#5178,.T.);
#7545=ORIENTED_EDGE('',*,*,#5194,.T.);
#7546=ORIENTED_EDGE('',*,*,#5191,.T.);
#7547=ORIENTED_EDGE('',*,*,#5188,.T.);
#7548=ORIENTED_EDGE('',*,*,#5185,.T.);
#7549=ORIENTED_EDGE('',*,*,#5182,.T.);
#7550=ORIENTED_EDGE('',*,*,#5170,.T.);
#8120=CYLINDRICAL_SURFACE('',#9355,2.942);
#8121=CYLINDRICAL_SURFACE('',#9357,2.942);
#8122=CYLINDRICAL_SURFACE('',#9358,2.942);
#8123=CYLINDRICAL_SURFACE('',#9359,2.942);
#8124=CYLINDRICAL_SURFACE('',#9360,2.942);
#8125=CYLINDRICAL_SURFACE('',#9361,2.942);
#8126=CYLINDRICAL_SURFACE('',#9362,2.942);
#8127=CYLINDRICAL_SURFACE('',#9363,2.942);
#8128=CYLINDRICAL_SURFACE('',#9364,2.942);
#8129=CYLINDRICAL_SURFACE('',#9365,2.942);
#8130=CYLINDRICAL_SURFACE('',#9366,2.942);
#8131=CYLINDRICAL_SURFACE('',#9367,2.942);
#8132=CYLINDRICAL_SURFACE('',#9368,2.942);
#8133=CYLINDRICAL_SURFACE('',#9369,2.942);
#8134=CYLINDRICAL_SURFACE('',#9370,2.942);
#8135=CYLINDRICAL_SURFACE('',#9371,2.942);
#8136=CYLINDRICAL_SURFACE('',#9372,2.942);
#8137=CYLINDRICAL_SURFACE('',#9373,2.942);
#8138=CYLINDRICAL_SURFACE('',#9374,2.942);
#8139=CYLINDRICAL_SURFACE('',#9375,2.37175);
#8140=CYLINDRICAL_SURFACE('',#9377,2.37175);
#8141=CYLINDRICAL_SURFACE('',#9378,2.37175);
#8142=CYLINDRICAL_SURFACE('',#9379,2.37175);
#8143=CYLINDRICAL_SURFACE('',#9380,2.37175);
#8144=CYLINDRICAL_SURFACE('',#9381,2.37175);
#8145=CYLINDRICAL_SURFACE('',#9382,2.37175);
#8146=CYLINDRICAL_SURFACE('',#9383,2.37175);
#8147=CYLINDRICAL_SURFACE('',#9384,2.37175);
#8148=CYLINDRICAL_SURFACE('',#9385,2.37175);
#8149=CYLINDRICAL_SURFACE('',#9386,2.37175);
#8150=CYLINDRICAL_SURFACE('',#9387,2.37175);
#8151=CYLINDRICAL_SURFACE('',#9388,2.37175);
#8152=CYLINDRICAL_SURFACE('',#9389,2.37175);
#8153=CYLINDRICAL_SURFACE('',#9390,2.37175);
#8154=CYLINDRICAL_SURFACE('',#9391,2.37175);
#8155=CYLINDRICAL_SURFACE('',#9392,2.37175);
#8156=CYLINDRICAL_SURFACE('',#9393,2.37175);
#8157=CYLINDRICAL_SURFACE('',#9394,2.37175);
#8158=CYLINDRICAL_SURFACE('',#9398,2.37175);
#8159=CYLINDRICAL_SURFACE('',#9400,2.942);
#8160=CYLINDRICAL_SURFACE('',#9410,5.);
#8557=ADVANCED_FACE('',(#809),#8120,.T.);
#8558=ADVANCED_FACE('',(#810),#8121,.T.);
#8559=ADVANCED_FACE('',(#811),#8122,.T.);
#8560=ADVANCED_FACE('',(#812),#8123,.T.);
#8561=ADVANCED_FACE('',(#813),#8124,.T.);
#8562=ADVANCED_FACE('',(#814),#8125,.T.);
#8563=ADVANCED_FACE('',(#815),#8126,.T.);
#8564=ADVANCED_FACE('',(#816),#8127,.T.);
#8565=ADVANCED_FACE('',(#817),#8128,.T.);
#8566=ADVANCED_FACE('',(#818),#8129,.T.);
#8567=ADVANCED_FACE('',(#819),#8130,.T.);
#8568=ADVANCED_FACE('',(#820),#8131,.T.);
#8569=ADVANCED_FACE('',(#821),#8132,.T.);
#8570=ADVANCED_FACE('',(#822),#8133,.T.);
#8571=ADVANCED_FACE('',(#823),#8134,.T.);
#8572=ADVANCED_FACE('',(#824),#8135,.T.);
#8573=ADVANCED_FACE('',(#825),#8136,.T.);
#8574=ADVANCED_FACE('',(#826),#8137,.T.);
#8575=ADVANCED_FACE('',(#827),#8138,.T.);
#8576=ADVANCED_FACE('',(#828),#8139,.T.);
#8577=ADVANCED_FACE('',(#829),#8140,.T.);
#8578=ADVANCED_FACE('',(#830),#8141,.T.);
#8579=ADVANCED_FACE('',(#831),#8142,.T.);
#8580=ADVANCED_FACE('',(#832),#8143,.T.);
#8581=ADVANCED_FACE('',(#833),#8144,.T.);
#8582=ADVANCED_FACE('',(#834),#8145,.T.);
#8583=ADVANCED_FACE('',(#835),#8146,.T.);
#8584=ADVANCED_FACE('',(#836),#8147,.T.);
#8585=ADVANCED_FACE('',(#837),#8148,.T.);
#8586=ADVANCED_FACE('',(#838),#8149,.T.);
#8587=ADVANCED_FACE('',(#839),#8150,.T.);
#8588=ADVANCED_FACE('',(#840),#8151,.T.);
#8589=ADVANCED_FACE('',(#841),#8152,.T.);
#8590=ADVANCED_FACE('',(#842),#8153,.T.);
#8591=ADVANCED_FACE('',(#843),#8154,.T.);
#8592=ADVANCED_FACE('',(#844),#8155,.T.);
#8593=ADVANCED_FACE('',(#845),#8156,.T.);
#8594=ADVANCED_FACE('',(#846),#8157,.T.);
#8595=ADVANCED_FACE('',(#847),#160,.T.);
#8596=ADVANCED_FACE('',(#848),#305,.F.);
#8597=ADVANCED_FACE('',(#849),#8158,.T.);
#8598=ADVANCED_FACE('',(#850),#306,.F.);
#8599=ADVANCED_FACE('',(#851),#8159,.T.);
#8600=ADVANCED_FACE('',(#852),#422,.F.);
#8601=ADVANCED_FACE('',(#853),#423,.F.);
#8602=ADVANCED_FACE('',(#854),#424,.F.);
#8603=ADVANCED_FACE('',(#855),#425,.F.);
#8604=ADVANCED_FACE('',(#856),#426,.F.);
#8605=ADVANCED_FACE('',(#857),#427,.F.);
#8606=ADVANCED_FACE('',(#858),#428,.F.);
#8607=ADVANCED_FACE('',(#859,#285),#429,.T.);
#8608=ADVANCED_FACE('',(#860),#8160,.T.);
#8609=ADVANCED_FACE('',(#861,#286),#430,.F.);
#8610=ADVANCED_FACE('',(#862),#431,.T.);
#8689=CLOSED_SHELL('',(#8557,#8558,#8559,#8560,#8561,#8562,#8563,#8564,
#8565,#8566,#8567,#8568,#8569,#8570,#8571,#8572,#8573,#8574,#8575,#8576,
#8577,#8578,#8579,#8580,#8581,#8582,#8583,#8584,#8585,#8586,#8587,#8588,
#8589,#8590,#8591,#8592,#8593,#8594,#8595,#8596,#8597,#8598,#8599,#8600,
#8601,#8602,#8603,#8604,#8605,#8606,#8607,#8608,#8609,#8610));
#9354=AXIS2_PLACEMENT_3D('',#26396,#10869,#10870);
#9355=AXIS2_PLACEMENT_3D('',#26397,#10871,#10872);
#9356=AXIS2_PLACEMENT_3D('',#26413,#10874,#10875);
#9357=AXIS2_PLACEMENT_3D('',#26421,#10876,#10877);
#9358=AXIS2_PLACEMENT_3D('',#26469,#10879,#10880);
#9359=AXIS2_PLACEMENT_3D('',#26517,#10882,#10883);
#9360=AXIS2_PLACEMENT_3D('',#26571,#10885,#10886);
#9361=AXIS2_PLACEMENT_3D('',#26619,#10888,#10889);
#9362=AXIS2_PLACEMENT_3D('',#26667,#10891,#10892);
#9363=AXIS2_PLACEMENT_3D('',#26721,#10894,#10895);
#9364=AXIS2_PLACEMENT_3D('',#26769,#10897,#10898);
#9365=AXIS2_PLACEMENT_3D('',#26817,#10900,#10901);
#9366=AXIS2_PLACEMENT_3D('',#26865,#10903,#10904);
#9367=AXIS2_PLACEMENT_3D('',#26919,#10906,#10907);
#9368=AXIS2_PLACEMENT_3D('',#26967,#10909,#10910);
#9369=AXIS2_PLACEMENT_3D('',#27015,#10912,#10913);
#9370=AXIS2_PLACEMENT_3D('',#27069,#10915,#10916);
#9371=AXIS2_PLACEMENT_3D('',#27117,#10918,#10919);
#9372=AXIS2_PLACEMENT_3D('',#27165,#10921,#10922);
#9373=AXIS2_PLACEMENT_3D('',#27219,#10924,#10925);
#9374=AXIS2_PLACEMENT_3D('',#27267,#10927,#10928);
#9375=AXIS2_PLACEMENT_3D('',#27315,#10930,#10931);
#9376=AXIS2_PLACEMENT_3D('',#27331,#10933,#10934);
#9377=AXIS2_PLACEMENT_3D('',#27340,#10935,#10936);
#9378=AXIS2_PLACEMENT_3D('',#27365,#10938,#10939);
#9379=AXIS2_PLACEMENT_3D('',#27389,#10941,#10942);
#9380=AXIS2_PLACEMENT_3D('',#27414,#10944,#10945);
#9381=AXIS2_PLACEMENT_3D('',#27439,#10947,#10948);
#9382=AXIS2_PLACEMENT_3D('',#27463,#10950,#10951);
#9383=AXIS2_PLACEMENT_3D('',#27488,#10953,#10954);
#9384=AXIS2_PLACEMENT_3D('',#27513,#10956,#10957);
#9385=AXIS2_PLACEMENT_3D('',#27537,#10959,#10960);
#9386=AXIS2_PLACEMENT_3D('',#27562,#10962,#10963);
#9387=AXIS2_PLACEMENT_3D('',#27587,#10965,#10966);
#9388=AXIS2_PLACEMENT_3D('',#27611,#10968,#10969);
#9389=AXIS2_PLACEMENT_3D('',#27635,#10971,#10972);
#9390=AXIS2_PLACEMENT_3D('',#27660,#10974,#10975);
#9391=AXIS2_PLACEMENT_3D('',#27685,#10977,#10978);
#9392=AXIS2_PLACEMENT_3D('',#27709,#10980,#10981);
#9393=AXIS2_PLACEMENT_3D('',#27734,#10983,#10984);
#9394=AXIS2_PLACEMENT_3D('',#27759,#10986,#10987);
#9395=AXIS2_PLACEMENT_3D('',#27783,#10989,#10990);
#9396=AXIS2_PLACEMENT_3D('',#28068,#10991,#10992);
#9397=AXIS2_PLACEMENT_3D('',#28102,#10994,#10995);
#9398=AXIS2_PLACEMENT_3D('',#28730,#10996,#10997);
#9399=AXIS2_PLACEMENT_3D('',#28741,#10998,#10999);
#9400=AXIS2_PLACEMENT_3D('',#29371,#11000,#11001);
#9401=AXIS2_PLACEMENT_3D('',#29372,#11002,#11003);
#9402=AXIS2_PLACEMENT_3D('',#29381,#11008,#11009);
#9403=AXIS2_PLACEMENT_3D('',#29387,#11013,#11014);
#9404=AXIS2_PLACEMENT_3D('',#29393,#11018,#11019);
#9405=AXIS2_PLACEMENT_3D('',#29399,#11023,#11024);
#9406=AXIS2_PLACEMENT_3D('',#29405,#11028,#11029);
#9407=AXIS2_PLACEMENT_3D('',#29408,#11032,#11033);
#9408=AXIS2_PLACEMENT_3D('',#29409,#11034,#11035);
#9409=AXIS2_PLACEMENT_3D('',#29411,#11036,#11037);
#9410=AXIS2_PLACEMENT_3D('',#29412,#11038,#11039);
#9411=AXIS2_PLACEMENT_3D('',#29415,#11041,#11042);
#9412=AXIS2_PLACEMENT_3D('',#29416,#11043,#11044);
#9413=AXIS2_PLACEMENT_3D('',#29417,#11045,#11046);
#10869=DIRECTION('axis',(0.,0.,1.));
#10870=DIRECTION('refdir',(1.,0.,0.));
#10871=DIRECTION('center_axis',(0.,0.,1.));
#10872=DIRECTION('ref_axis',(1.,0.,0.));
#10873=DIRECTION('',(0.,0.,-1.));
#10874=DIRECTION('center_axis',(0.,0.,-1.));
#10875=DIRECTION('ref_axis',(1.,0.,0.));
#10876=DIRECTION('center_axis',(0.,0.,1.));
#10877=DIRECTION('ref_axis',(1.,0.,0.));
#10878=DIRECTION('',(0.,0.,-1.));
#10879=DIRECTION('center_axis',(0.,0.,1.));
#10880=DIRECTION('ref_axis',(1.,0.,0.));
#10881=DIRECTION('',(0.,0.,-1.));
#10882=DIRECTION('center_axis',(0.,0.,1.));
#10883=DIRECTION('ref_axis',(1.,0.,0.));
#10884=DIRECTION('',(0.,0.,-1.));
#10885=DIRECTION('center_axis',(0.,0.,1.));
#10886=DIRECTION('ref_axis',(1.,0.,0.));
#10887=DIRECTION('',(0.,0.,-1.));
#10888=DIRECTION('center_axis',(0.,0.,1.));
#10889=DIRECTION('ref_axis',(1.,0.,0.));
#10890=DIRECTION('',(0.,0.,-1.));
#10891=DIRECTION('center_axis',(0.,0.,1.));
#10892=DIRECTION('ref_axis',(1.,0.,0.));
#10893=DIRECTION('',(0.,0.,-1.));
#10894=DIRECTION('center_axis',(0.,0.,1.));
#10895=DIRECTION('ref_axis',(1.,0.,0.));
#10896=DIRECTION('',(0.,0.,-1.));
#10897=DIRECTION('center_axis',(0.,0.,1.));
#10898=DIRECTION('ref_axis',(1.,0.,0.));
#10899=DIRECTION('',(0.,0.,-1.));
#10900=DIRECTION('center_axis',(0.,0.,1.));
#10901=DIRECTION('ref_axis',(1.,0.,0.));
#10902=DIRECTION('',(0.,0.,-1.));
#10903=DIRECTION('center_axis',(0.,0.,1.));
#10904=DIRECTION('ref_axis',(1.,0.,0.));
#10905=DIRECTION('',(0.,0.,-1.));
#10906=DIRECTION('center_axis',(0.,0.,1.));
#10907=DIRECTION('ref_axis',(1.,0.,0.));
#10908=DIRECTION('',(0.,0.,-1.));
#10909=DIRECTION('center_axis',(0.,0.,1.));
#10910=DIRECTION('ref_axis',(1.,0.,0.));
#10911=DIRECTION('',(0.,0.,-1.));
#10912=DIRECTION('center_axis',(0.,0.,1.));
#10913=DIRECTION('ref_axis',(1.,0.,0.));
#10914=DIRECTION('',(0.,0.,-1.));
#10915=DIRECTION('center_axis',(0.,0.,1.));
#10916=DIRECTION('ref_axis',(1.,0.,0.));
#10917=DIRECTION('',(0.,0.,-1.));
#10918=DIRECTION('center_axis',(0.,0.,1.));
#10919=DIRECTION('ref_axis',(1.,0.,0.));
#10920=DIRECTION('',(0.,0.,-1.));
#10921=DIRECTION('center_axis',(0.,0.,1.));
#10922=DIRECTION('ref_axis',(1.,0.,0.));
#10923=DIRECTION('',(0.,0.,-1.));
#10924=DIRECTION('center_axis',(0.,0.,1.));
#10925=DIRECTION('ref_axis',(1.,0.,0.));
#10926=DIRECTION('',(0.,0.,-1.));
#10927=DIRECTION('center_axis',(0.,0.,1.));
#10928=DIRECTION('ref_axis',(1.,0.,0.));
#10929=DIRECTION('',(0.,0.,-1.));
#10930=DIRECTION('center_axis',(0.,0.,1.));
#10931=DIRECTION('ref_axis',(0.997337382943289,-0.0729256099311623,0.));
#10932=DIRECTION('',(0.,0.,1.));
#10933=DIRECTION('center_axis',(0.,0.,-1.));
#10934=DIRECTION('ref_axis',(1.,7.52212518638754E-14,0.));
#10935=DIRECTION('center_axis',(0.,0.,1.));
#10936=DIRECTION('ref_axis',(1.,7.52212518638754E-14,0.));
#10937=DIRECTION('',(0.,0.,1.));
#10938=DIRECTION('center_axis',(0.,0.,1.));
#10939=DIRECTION('ref_axis',(1.,7.52212518638754E-14,0.));
#10940=DIRECTION('',(0.,0.,1.));
#10941=DIRECTION('center_axis',(0.,0.,1.));
#10942=DIRECTION('ref_axis',(1.,7.52212518638754E-14,0.));
#10943=DIRECTION('',(0.,0.,1.));
#10944=DIRECTION('center_axis',(0.,0.,1.));
#10945=DIRECTION('ref_axis',(1.,7.52212518638754E-14,0.));
#10946=DIRECTION('',(0.,0.,1.));
#10947=DIRECTION('center_axis',(0.,0.,1.));
#10948=DIRECTION('ref_axis',(1.,7.52212518638754E-14,0.));
#10949=DIRECTION('',(0.,0.,1.));
#10950=DIRECTION('center_axis',(0.,0.,1.));
#10951=DIRECTION('ref_axis',(1.,7.52212518638754E-14,0.));
#10952=DIRECTION('',(0.,0.,1.));
#10953=DIRECTION('center_axis',(0.,0.,1.));
#10954=DIRECTION('ref_axis',(1.,7.52212518638754E-14,0.));
#10955=DIRECTION('',(0.,0.,1.));
#10956=DIRECTION('center_axis',(0.,0.,1.));
#10957=DIRECTION('ref_axis',(1.,7.52212518638754E-14,0.));
#10958=DIRECTION('',(0.,0.,1.));
#10959=DIRECTION('center_axis',(0.,0.,1.));
#10960=DIRECTION('ref_axis',(1.,7.52212518638754E-14,0.));
#10961=DIRECTION('',(0.,0.,1.));
#10962=DIRECTION('center_axis',(0.,0.,1.));
#10963=DIRECTION('ref_axis',(1.,7.52212518638754E-14,0.));
#10964=DIRECTION('',(0.,0.,1.));
#10965=DIRECTION('center_axis',(0.,0.,1.));
#10966=DIRECTION('ref_axis',(1.,7.52212518638754E-14,0.));
#10967=DIRECTION('',(0.,0.,1.));
#10968=DIRECTION('center_axis',(0.,0.,1.));
#10969=DIRECTION('ref_axis',(1.,7.52212518638754E-14,0.));
#10970=DIRECTION('',(0.,0.,1.));
#10971=DIRECTION('center_axis',(0.,0.,1.));
#10972=DIRECTION('ref_axis',(1.,7.52212518638754E-14,0.));
#10973=DIRECTION('',(0.,0.,1.));
#10974=DIRECTION('center_axis',(0.,0.,1.));
#10975=DIRECTION('ref_axis',(1.,7.52212518638754E-14,0.));
#10976=DIRECTION('',(0.,0.,1.));
#10977=DIRECTION('center_axis',(0.,0.,1.));
#10978=DIRECTION('ref_axis',(1.,7.52212518638754E-14,0.));
#10979=DIRECTION('',(0.,0.,1.));
#10980=DIRECTION('center_axis',(0.,0.,1.));
#10981=DIRECTION('ref_axis',(1.,7.52212518638754E-14,0.));
#10982=DIRECTION('',(0.,0.,1.));
#10983=DIRECTION('center_axis',(0.,0.,1.));
#10984=DIRECTION('ref_axis',(1.,7.52212518638754E-14,0.));
#10985=DIRECTION('',(0.,0.,1.));
#10986=DIRECTION('center_axis',(0.,0.,1.));
#10987=DIRECTION('ref_axis',(1.,7.52212518638754E-14,0.));
#10988=DIRECTION('',(0.,0.,1.));
#10989=DIRECTION('center_axis',(0.,0.,-1.));
#10990=DIRECTION('ref_axis',(1.,0.,0.));
#10991=DIRECTION('center_axis',(0.,0.,-1.));
#10992=DIRECTION('ref_axis',(1.,0.,0.));
#10993=DIRECTION('',(0.707106781186547,8.65956056235493E-17,0.707106781186548));
#10994=DIRECTION('center_axis',(0.,0.,1.));
#10995=DIRECTION('ref_axis',(1.,0.,0.));
#10996=DIRECTION('center_axis',(0.,0.,1.));
#10997=DIRECTION('ref_axis',(1.,7.52212518638754E-14,0.));
#10998=DIRECTION('center_axis',(0.,0.,-1.));
#10999=DIRECTION('ref_axis',(1.,7.52212518638754E-14,0.));
#11000=DIRECTION('center_axis',(0.,0.,1.));
#11001=DIRECTION('ref_axis',(1.,0.,0.));
#11002=DIRECTION('center_axis',(-1.92296268638356E-16,-1.,0.));
#11003=DIRECTION('ref_axis',(1.,-1.92296268638356E-16,0.));
#11004=DIRECTION('',(1.,-1.92296268638356E-16,0.));
#11005=DIRECTION('',(0.,0.,1.));
#11006=DIRECTION('',(1.,-1.92296268638356E-16,0.));
#11007=DIRECTION('',(0.,0.,1.));
#11008=DIRECTION('center_axis',(-0.866025403784439,-0.5,0.));
#11009=DIRECTION('ref_axis',(0.5,-0.866025403784439,0.));
#11010=DIRECTION('',(0.5,-0.866025403784439,0.));
#11011=DIRECTION('',(0.,0.,1.));
#11012=DIRECTION('',(0.5,-0.866025403784439,0.));
#11013=DIRECTION('center_axis',(-0.866025403784439,0.5,0.));
#11014=DIRECTION('ref_axis',(-0.5,-0.866025403784438,0.));
#11015=DIRECTION('',(-0.5,-0.866025403784438,0.));
#11016=DIRECTION('',(0.,0.,1.));
#11017=DIRECTION('',(-0.5,-0.866025403784439,0.));
#11018=DIRECTION('center_axis',(1.92296268638356E-16,1.,0.));
#11019=DIRECTION('ref_axis',(-1.,1.92296268638356E-16,0.));
#11020=DIRECTION('',(-1.,1.92296268638356E-16,0.));
#11021=DIRECTION('',(0.,0.,1.));
#11022=DIRECTION('',(-1.,1.92296268638356E-16,0.));
#11023=DIRECTION('center_axis',(0.866025403784439,0.5,0.));
#11024=DIRECTION('ref_axis',(-0.5,0.866025403784439,0.));
#11025=DIRECTION('',(-0.5,0.866025403784439,0.));
#11026=DIRECTION('',(0.,0.,1.));
#11027=DIRECTION('',(-0.5,0.866025403784439,0.));
#11028=DIRECTION('center_axis',(0.866025403784439,-0.5,0.));
#11029=DIRECTION('ref_axis',(0.5,0.866025403784439,0.));
#11030=DIRECTION('',(0.5,0.866025403784439,0.));
#11031=DIRECTION('',(0.5,0.866025403784439,0.));
#11032=DIRECTION('center_axis',(0.,0.,1.));
#11033=DIRECTION('ref_axis',(1.,0.,0.));
#11034=DIRECTION('center_axis',(0.,0.,1.));
#11035=DIRECTION('ref_axis',(1.,0.,0.));
#11036=DIRECTION('center_axis',(0.,0.,1.));
#11037=DIRECTION('ref_axis',(1.,0.,0.));
#11038=DIRECTION('center_axis',(0.,0.,1.));
#11039=DIRECTION('ref_axis',(1.,0.,0.));
#11040=DIRECTION('',(0.,0.,-1.));
#11041=DIRECTION('center_axis',(0.,0.,1.));
#11042=DIRECTION('ref_axis',(1.,0.,0.));
#11043=DIRECTION('center_axis',(0.,0.,1.));
#11044=DIRECTION('ref_axis',(1.,0.,0.));
#11045=DIRECTION('center_axis',(0.,0.,1.));
#11046=DIRECTION('ref_axis',(1.,0.,0.));
#26396=CARTESIAN_POINT('',(0.,0.,0.));
#26397=CARTESIAN_POINT('Origin',(0.,0.,0.));
#26398=CARTESIAN_POINT('',(-2.94521004790112,0.00203952464144973,0.322176117089595));
#26399=CARTESIAN_POINT('',(-2.94462969622312,0.00314068971924443,0.177823882910389));
#26400=CARTESIAN_POINT('',(-2.942,-3.60291088309151E-16,0.));
#26401=CARTESIAN_POINT('',(1.28892185405323,2.64462557919717,0.));
#26402=CARTESIAN_POINT('Ctrl Pts',(-2.94521004790112,0.00203952464144973,
0.322176117089595));
#26403=CARTESIAN_POINT('Ctrl Pts',(-2.94603324667188,0.114074791781704,
0.316095866004171));
#26404=CARTESIAN_POINT('Ctrl Pts',(-2.94019223072851,0.226018346108296,
0.310015614918747));
#26405=CARTESIAN_POINT('Ctrl Pts',(-2.92739988843454,0.337155312555215,
0.303935363833323));
#26406=CARTESIAN_POINT('Ctrl Pts',(-2.81638858583978,1.30159631391204,0.251171250930097));
#26407=CARTESIAN_POINT('Ctrl Pts',(-2.18189506715083,2.20529575467607,0.198407138026871));
#26408=CARTESIAN_POINT('Ctrl Pts',(-1.31250721789878,2.63803669000119,0.145643025123645));
#26409=CARTESIAN_POINT('Ctrl Pts',(-0.512593100747222,3.03619682478308,
0.0970953500824302));
#26410=CARTESIAN_POINT('Ctrl Pts',(0.486174006333883,3.03566063209391,0.0485476750412151));
#26411=CARTESIAN_POINT('Ctrl Pts',(1.29201086331817,2.64828936846223,6.93889390390723E-17));
#26412=CARTESIAN_POINT('',(-1.28892185405326,2.64462557919716,0.));
#26413=CARTESIAN_POINT('Origin',(0.,0.,0.));
#26414=CARTESIAN_POINT('Ctrl Pts',(-1.28892185405326,2.64462557919716,1.59594559789866E-15));
#26415=CARTESIAN_POINT('Ctrl Pts',(-2.16624189914079,2.21704256404097,0.0527975766957825));
#26416=CARTESIAN_POINT('Ctrl Pts',(-2.80665150218763,1.32243360512987,0.105595153391563));
#26417=CARTESIAN_POINT('Ctrl Pts',(-2.92450934358977,0.359669350507257,
0.158392730087344));
#26418=CARTESIAN_POINT('Ctrl Pts',(-2.93896779585848,0.241560272181372,
0.164869781028359));
#26419=CARTESIAN_POINT('Ctrl Pts',(-2.94556202255218,0.122425479928277,
0.171346831969374));
#26420=CARTESIAN_POINT('Ctrl Pts',(-2.94462969622312,0.00314068971924443,
0.177823882910389));
#26421=CARTESIAN_POINT('Origin',(0.,0.,0.));
#26422=CARTESIAN_POINT('',(-2.93759410342513,0.00104371380931417,1.32217611708959));
#26423=CARTESIAN_POINT('',(-2.93753976560994,0.00101398507028504,1.17782388291039));
#26424=CARTESIAN_POINT('',(-2.942,-3.60291088309151E-16,0.));
#26425=CARTESIAN_POINT('Ctrl Pts',(-2.93759410342513,0.00104371380931417,
1.32217611708959));
#26426=CARTESIAN_POINT('Ctrl Pts',(-2.93894740988071,0.424518101105222,
1.29934721009019));
#26427=CARTESIAN_POINT('Ctrl Pts',(-2.85336411585787,0.847470416247501,
1.27651830309079));
#26428=CARTESIAN_POINT('Ctrl Pts',(-2.67811890996276,1.22926576308214,1.25368939609139));
#26429=CARTESIAN_POINT('Ctrl Pts',(-2.27307727438026,2.11170366459169,1.20092528318816));
#26430=CARTESIAN_POINT('Ctrl Pts',(-1.38905821992549,2.77427944140463,1.14816117028494));
#26431=CARTESIAN_POINT('Ctrl Pts',(-0.428414463428333,2.91544748851427,
1.09539705738171));
#26432=CARTESIAN_POINT('Ctrl Pts',(0.532229293068828,3.05661553562391,1.04263294447848));
#26433=CARTESIAN_POINT('Ctrl Pts',(1.56949775160839,2.67637585303025,0.989868831575259));
#26434=CARTESIAN_POINT('Ctrl Pts',(2.21127556875009,1.94774980228162,0.937104718672033));
#26435=CARTESIAN_POINT('Ctrl Pts',(2.8530533858918,1.21912375153298,0.884340605768807));
#26436=CARTESIAN_POINT('Ctrl Pts',(3.09934056163565,0.142111332629363,0.831576492865582));
#26437=CARTESIAN_POINT('Ctrl Pts',(2.83805568324674,-0.79300892305516,0.778812379962356));
#26438=CARTESIAN_POINT('Ctrl Pts',(2.57677080485782,-1.72812917873969,0.72604826705913));
#26439=CARTESIAN_POINT('Ctrl Pts',(1.80791387233614,-2.52135727120512,0.673284154155903));
#26440=CARTESIAN_POINT('Ctrl Pts',(0.881397688767813,-2.81181555894288,
0.620520041252678));
#26441=CARTESIAN_POINT('Ctrl Pts',(-0.0451184948005073,-3.10227384668064,
0.567755928349452));
#26442=CARTESIAN_POINT('Ctrl Pts',(-1.12929392941546,-2.88996232969074,
0.514991815446226));
#26443=CARTESIAN_POINT('Ctrl Pts',(-1.87761710347266,-2.27121529022098,
0.462227702543001));
#26444=CARTESIAN_POINT('Ctrl Pts',(-2.53970756099287,-1.72376931413192,
0.415543840725199));
#26445=CARTESIAN_POINT('Ctrl Pts',(-2.93888956917045,-0.858161617780837,
0.368859978907397));
#26446=CARTESIAN_POINT('Ctrl Pts',(-2.94521004790112,0.00203952464144973,
0.322176117089595));
#26447=CARTESIAN_POINT('Ctrl Pts',(-2.94462969622312,0.00314068971924443,
0.177823882910389));
#26448=CARTESIAN_POINT('Ctrl Pts',(-2.93796217945806,-0.849922571222733,
0.224144408665155));
#26449=CARTESIAN_POINT('Ctrl Pts',(-2.54635872365652,-1.71065728599598,
0.270464934419922));
#26450=CARTESIAN_POINT('Ctrl Pts',(-1.89332424994401,-2.25876726457989,
0.316785460174689));
#26451=CARTESIAN_POINT('Ctrl Pts',(-1.14897523513868,-2.88352007471027,
0.36958303687047));
#26452=CARTESIAN_POINT('Ctrl Pts',(-0.064971125770581,-3.1021061446369,
0.422380613566252));
#26453=CARTESIAN_POINT('Ctrl Pts',(0.864001826933897,-2.81700059999635,
0.475178190262033));
#26454=CARTESIAN_POINT('Ctrl Pts',(1.79297477963837,-2.5318950553558,0.527975766957815));
#26455=CARTESIAN_POINT('Ctrl Pts',(2.56691657567923,-1.74309789614807,0.580773343653596));
#26456=CARTESIAN_POINT('Ctrl Pts',(2.83354070514343,-0.808991748766537,
0.633570920349377));
#26457=CARTESIAN_POINT('Ctrl Pts',(3.10016483460764,0.125114398615,0.686368497045159));
#26458=CARTESIAN_POINT('Ctrl Pts',(2.85947129749519,1.20452953417034,0.73916607374094));
#26459=CARTESIAN_POINT('Ctrl Pts',(2.22094023442363,1.93684572412005,0.791963650436722));
#26460=CARTESIAN_POINT('Ctrl Pts',(1.58240917135208,2.66916191406976,0.844761227132503));
#26461=CARTESIAN_POINT('Ctrl Pts',(0.546040582321433,3.05437915841384,0.897558803828285));
#26462=CARTESIAN_POINT('Ctrl Pts',(-0.415815893186985,2.9172496831673,0.950356380524066));
#26463=CARTESIAN_POINT('Ctrl Pts',(-1.3776723686954,2.78012020792076,1.00315395721985));
#26464=CARTESIAN_POINT('Ctrl Pts',(-2.26501673068159,2.12064401308361,1.05595153391563));
#26465=CARTESIAN_POINT('Ctrl Pts',(-2.67356337698776,1.2391776980577,1.10874911061141));
#26466=CARTESIAN_POINT('Ctrl Pts',(-2.85172980262831,0.854771892525725,
1.13177403471107));
#26467=CARTESIAN_POINT('Ctrl Pts',(-2.93883772557839,0.428147656758027,
1.15479895881073));
#26468=CARTESIAN_POINT('Ctrl Pts',(-2.93753976560994,0.00101398507028504,
1.17782388291039));
#26469=CARTESIAN_POINT('Origin',(0.,0.,0.));
#26470=CARTESIAN_POINT('',(-2.94150578537287,-0.00264448079833085,2.32217611708959));
#26471=CARTESIAN_POINT('',(-2.94148820905054,-0.00265277056903863,2.17782388291039));
#26472=CARTESIAN_POINT('',(-2.942,-3.60291088309151E-16,0.));
#26473=CARTESIAN_POINT('Ctrl Pts',(-2.94150578537287,-0.00264448079833085,
2.32217611708959));
#26474=CARTESIAN_POINT('Ctrl Pts',(-2.93495612048696,0.729051641444702,
2.28259855417621));
#26475=CARTESIAN_POINT('Ctrl Pts',(-2.65840516263949,1.46516741567181,2.24302099126283));
#26476=CARTESIAN_POINT('Ctrl Pts',(-2.16409169020457,2.00002938162346,2.20344342834945));
#26477=CARTESIAN_POINT('Ctrl Pts',(-1.50508163629538,2.71309797609147,2.15067931544623));
#26478=CARTESIAN_POINT('Ctrl Pts',(-0.459025827121477,3.0684629852044,2.097915202543));
#26479=CARTESIAN_POINT('Ctrl Pts',(0.497968791484761,2.90438227824113,2.04515108963977));
#26480=CARTESIAN_POINT('Ctrl Pts',(1.45496341009101,2.74030157127786,1.99238697673655));
#26481=CARTESIAN_POINT('Ctrl Pts',(2.32289683812959,2.05677514823839,1.93962286383332));
#26482=CARTESIAN_POINT('Ctrl Pts',(2.70673338784322,1.16490573313425,1.8868587509301));
#26483=CARTESIAN_POINT('Ctrl Pts',(3.09056993755685,0.273036318030111,1.83409463802687));
#26484=CARTESIAN_POINT('Ctrl Pts',(2.99030960894553,-0.827176089138696,
1.78133052512364));
#26485=CARTESIAN_POINT('Ctrl Pts',(2.4515856938222,-1.63497366892159,1.72856641222042));
#26486=CARTESIAN_POINT('Ctrl Pts',(1.91286177869886,-2.44277124870449,1.67580229931719));
#26487=CARTESIAN_POINT('Ctrl Pts',(0.935674277063515,-2.95815400110147,
1.62303818641397));
#26488=CARTESIAN_POINT('Ctrl Pts',(-0.035215432819809,-2.94655128352351,
1.57027407351074));
#26489=CARTESIAN_POINT('Ctrl Pts',(-1.00610514270313,-2.93494856594555,
1.51750996060752));
#26490=CARTESIAN_POINT('Ctrl Pts',(-1.97069706083443,-2.39636037839263,
1.46474584770429));
#26491=CARTESIAN_POINT('Ctrl Pts',(-2.48996091154496,-1.57591627151309,
1.41198173480107));
#26492=CARTESIAN_POINT('Ctrl Pts',(-2.78456020326321,-1.11044529283744,
1.38204652889724));
#26493=CARTESIAN_POINT('Ctrl Pts',(-2.93581953281605,-0.554251946163811,
1.35211132299342));
#26494=CARTESIAN_POINT('Ctrl Pts',(-2.93759410342513,0.00104371380931417,
1.32217611708959));
#26495=CARTESIAN_POINT('Ctrl Pts',(-2.93753976560994,0.00101398507028504,
1.17782388291039));
#26496=CARTESIAN_POINT('Ctrl Pts',(-2.93586142299925,-0.551296301131853,
1.20759653550651));
#26497=CARTESIAN_POINT('Ctrl Pts',(-2.78636763677815,-1.10445836884475,
1.23736918810263));
#26498=CARTESIAN_POINT('Ctrl Pts',(-2.49479340097823,-1.56829689931507,
1.26714184069876));
#26499=CARTESIAN_POINT('Ctrl Pts',(-1.97772784803637,-2.39084874644727,
1.31993941739454));
#26500=CARTESIAN_POINT('Ctrl Pts',(-1.01384781152648,-2.93249600549699,
1.37273699409032));
#26501=CARTESIAN_POINT('Ctrl Pts',(-0.0423832056000787,-2.94646510892246,
1.4255345707861));
#26502=CARTESIAN_POINT('Ctrl Pts',(0.929081400326319,-2.96043421234793,
1.47833214748188));
#26503=CARTESIAN_POINT('Ctrl Pts',(1.90813057566922,-2.44672516014913,1.53112972417766));
#26504=CARTESIAN_POINT('Ctrl Pts',(2.44864484529323,-1.63940033793356,1.58392730087344));
#26505=CARTESIAN_POINT('Ctrl Pts',(2.98915911491722,-0.832075515717996,
1.63672487756922));
#26506=CARTESIAN_POINT('Ctrl Pts',(3.09113847882232,0.268865076514346,1.68952245426501));
#26507=CARTESIAN_POINT('Ctrl Pts',(2.70810952187376,1.16174019749111,1.74232003096079));
#26508=CARTESIAN_POINT('Ctrl Pts',(2.3250805649252,2.05461531846787,1.79511760765657));
#26509=CARTESIAN_POINT('Ctrl Pts',(1.45704328712297,2.73942496818906,1.84791518435235));
#26510=CARTESIAN_POINT('Ctrl Pts',(0.499541834730426,2.9041250846367,1.90071276104813));
#26511=CARTESIAN_POINT('Ctrl Pts',(-0.457959617662116,3.06882520108433,
1.95351033774391));
#26512=CARTESIAN_POINT('Ctrl Pts',(-1.50492524464497,2.71341578425843,2.00630791443969));
#26513=CARTESIAN_POINT('Ctrl Pts',(-2.16428115211478,1.99984458038746,2.05910549113548));
#26514=CARTESIAN_POINT('Ctrl Pts',(-2.6584810620408,1.4650092650688,2.09867828839378));
#26515=CARTESIAN_POINT('Ctrl Pts',(-2.93492996134342,0.728966169940792,
2.13825108565208));
#26516=CARTESIAN_POINT('Ctrl Pts',(-2.94148820905054,-0.00265277056903863,
2.17782388291039));
#26517=CARTESIAN_POINT('Origin',(0.,0.,0.));
#26518=CARTESIAN_POINT('',(-2.94619134998316,0.00116105206271745,3.3221761170896));
#26519=CARTESIAN_POINT('',(-2.94627397750243,0.0010917140638196,3.17782388291039));
#26520=CARTESIAN_POINT('',(-2.942,-3.60291088309151E-16,0.));
#26521=CARTESIAN_POINT('Ctrl Pts',(-2.94619134998316,0.00116105206271745,
3.3221761170896));
#26522=CARTESIAN_POINT('Ctrl Pts',(-2.94652200322202,0.0667444906727352,
3.31861401116546));
#26523=CARTESIAN_POINT('Ctrl Pts',(-2.94452061107706,0.132307391291658,
3.31505190524133));
#26524=CARTESIAN_POINT('Ctrl Pts',(-2.94012265777212,0.197709134686594,
3.3114897993172));
#26525=CARTESIAN_POINT('Ctrl Pts',(-2.87497745724548,1.16648014993856,3.25872568641397));
#26526=CARTESIAN_POINT('Ctrl Pts',(-2.28399404876592,2.09989107203918,3.20596157351074));
#26527=CARTESIAN_POINT('Ctrl Pts',(-1.43615555362721,2.57310461829436,3.15319746060752));
#26528=CARTESIAN_POINT('Ctrl Pts',(-0.588317058488505,3.04631816454953,
3.10043334770429));
#26529=CARTESIAN_POINT('Ctrl Pts',(0.516376523309347,3.05933433495927,3.04766923480106));
#26530=CARTESIAN_POINT('Ctrl Pts',(1.37512947635203,2.60622889469009,2.99490512189784));
#26531=CARTESIAN_POINT('Ctrl Pts',(2.23388242939471,2.15312345442092,2.94214100899461));
#26532=CARTESIAN_POINT('Ctrl Pts',(2.84669475368223,1.23389640347284,2.88937689609139));
#26533=CARTESIAN_POINT('Ctrl Pts',(2.93464800446939,0.266929283846224,2.83661278318816));
#26534=CARTESIAN_POINT('Ctrl Pts',(3.02260125525656,-0.700037835780391,
2.78384867028493));
#26535=CARTESIAN_POINT('Ctrl Pts',(2.58569543254338,-1.71474502408554,2.73108455738171));
#26536=CARTESIAN_POINT('Ctrl Pts',(1.8227860263141,-2.31535338267893,2.67832044447848));
#26537=CARTESIAN_POINT('Ctrl Pts',(1.05987662008482,-2.91596174127233,2.62555633157526));
#26538=CARTESIAN_POINT('Ctrl Pts',(-0.0290363696605579,-3.10247127015397,
2.57279221867203));
#26539=CARTESIAN_POINT('Ctrl Pts',(-0.948339694866047,-2.78999316350398,
2.52002810576881));
#26540=CARTESIAN_POINT('Ctrl Pts',(-1.86764302007153,-2.47751505685399,
2.46726399286558));
#26541=CARTESIAN_POINT('Ctrl Pts',(-2.61733668073713,-1.66604931467237,
2.41449987996235));
#26542=CARTESIAN_POINT('Ctrl Pts',(-2.85620136174769,-0.724930353670017,
2.36173576705913));
#26543=CARTESIAN_POINT('Ctrl Pts',(-2.91589725889527,-0.489730488784397,
2.34854921706928));
#26544=CARTESIAN_POINT('Ctrl Pts',(-2.94368801886774,-0.24643279880189,
2.33536266707944));
#26545=CARTESIAN_POINT('Ctrl Pts',(-2.94150578537287,-0.00264448079833085,
2.32217611708959));
#26546=CARTESIAN_POINT('Ctrl Pts',(-2.94148820905054,-0.00265277056903863,
2.17782388291039));
#26547=CARTESIAN_POINT('Ctrl Pts',(-2.94367990095588,-0.247151511898062,
2.19104866234787));
#26548=CARTESIAN_POINT('Ctrl Pts',(-2.91572965175503,-0.491156154572101,
2.20427344178534));
#26549=CARTESIAN_POINT('Ctrl Pts',(-2.8556914602692,-0.72699192409469,2.21749822122282));
#26550=CARTESIAN_POINT('Ctrl Pts',(-2.61599967299705,-1.66852423378984,
2.2702957979186));
#26551=CARTESIAN_POINT('Ctrl Pts',(-1.864869910496,-2.47985586226411,2.32309337461438));
#26552=CARTESIAN_POINT('Ctrl Pts',(-0.944572778809107,-2.79128493002216,
2.37589095131016));
#26553=CARTESIAN_POINT('Ctrl Pts',(-0.0242756471222212,-3.1027139977802,
2.42868852800595));
#26554=CARTESIAN_POINT('Ctrl Pts',(1.06518885375051,-2.91424050482202,2.48148610470173));
#26555=CARTESIAN_POINT('Ctrl Pts',(1.82738024207177,-2.31174647809792,2.53428368139751));
#26556=CARTESIAN_POINT('Ctrl Pts',(2.58957163039303,-1.70925245137381,2.58708125809329));
#26557=CARTESIAN_POINT('Ctrl Pts',(3.02448990616283,-0.692737890883784,
2.63987883478907));
#26558=CARTESIAN_POINT('Ctrl Pts',(2.93395403704711,0.274597720394451,2.69267641148485));
#26559=CARTESIAN_POINT('Ctrl Pts',(2.8434181679314,1.24193333167269,2.74547398818063));
#26560=CARTESIAN_POINT('Ctrl Pts',(2.22742815393017,2.16008999373912,2.79827156487642));
#26561=CARTESIAN_POINT('Ctrl Pts',(1.36667466982157,2.61068771331245,2.8510691415722));
#26562=CARTESIAN_POINT('Ctrl Pts',(0.505921185712974,3.06128543288579,2.90386671826798));
#26563=CARTESIAN_POINT('Ctrl Pts',(-0.599595768502999,3.04432420996601,
2.95666429496376));
#26564=CARTESIAN_POINT('Ctrl Pts',(-1.44612088828002,2.56753276921717,3.00946187165954));
#26565=CARTESIAN_POINT('Ctrl Pts',(-2.29264600805703,2.09074132846833,3.06225944835532));
#26566=CARTESIAN_POINT('Ctrl Pts',(-2.8801792933951,1.15411966989042,3.1150570250511));
#26567=CARTESIAN_POINT('Ctrl Pts',(-2.9409970926588,0.184461960144107,3.16785460174689));
#26568=CARTESIAN_POINT('Ctrl Pts',(-2.94482498135212,0.123431442294656,
3.17117769546805));
#26569=CARTESIAN_POINT('Ctrl Pts',(-2.9465662984666,0.0622700528698149,
3.17450078918922));
#26570=CARTESIAN_POINT('Ctrl Pts',(-2.94627397750243,0.0010917140638196,
3.17782388291039));
#26571=CARTESIAN_POINT('Origin',(0.,0.,0.));
#26572=CARTESIAN_POINT('',(-2.93825501966817,0.00168812480491387,4.3221761170896));
#26573=CARTESIAN_POINT('',(-2.93839638220268,0.00179748935179793,4.17782388291039));
#26574=CARTESIAN_POINT('',(-2.942,-3.60291088309151E-16,0.));
#26575=CARTESIAN_POINT('Ctrl Pts',(-2.93825501966817,0.00168812480491387,
4.3221761170896));
#26576=CARTESIAN_POINT('Ctrl Pts',(-2.94023496409179,0.378238072324008,
4.30186535525148));
#26577=CARTESIAN_POINT('Ctrl Pts',(-2.87305142275175,0.754108328434651,
4.28155459341337));
#26578=CARTESIAN_POINT('Ctrl Pts',(-2.73342934159449,1.1008061494448,4.26124383157526));
#26579=CARTESIAN_POINT('Ctrl Pts',(-2.3707134911166,2.00147167429752,4.20847971867203));
#26580=CARTESIAN_POINT('Ctrl Pts',(-1.51912634074217,2.70525904140838,4.15571560576881));
#26581=CARTESIAN_POINT('Ctrl Pts',(-0.566263490800549,2.89184297694709,
4.10295149286558));
#26582=CARTESIAN_POINT('Ctrl Pts',(0.38659935914108,3.07842691248581,4.05018737996236));
#26583=CARTESIAN_POINT('Ctrl Pts',(1.44073790864989,2.74780741645236,3.99742326705913));
#26584=CARTESIAN_POINT('Ctrl Pts',(2.1163663088001,2.05046428665802,3.9446591541559));
#26585=CARTESIAN_POINT('Ctrl Pts',(2.79199470895031,1.35312115686368,3.89189504125268));
#26586=CARTESIAN_POINT('Ctrl Pts',(3.08911295974191,0.289054393308455,3.83913092834945));
#26587=CARTESIAN_POINT('Ctrl Pts',(2.87248918644939,-0.657431378827086,
3.78636681544623));
#26588=CARTESIAN_POINT('Ctrl Pts',(2.65586541315687,-1.60391715096264,3.733602702543));
#26589=CARTESIAN_POINT('Ctrl Pts',(1.9254996157802,-2.4328219316785,3.68083858963977));
#26590=CARTESIAN_POINT('Ctrl Pts',(1.01381410678357,-2.76687388619937,3.62807447673655));
#26591=CARTESIAN_POINT('Ctrl Pts',(0.102128597786946,-3.10092584072023,
3.57531036383332));
#26592=CARTESIAN_POINT('Ctrl Pts',(-0.990876622829635,-2.94012496904611,
3.5225462509301));
#26593=CARTESIAN_POINT('Ctrl Pts',(-1.76772573685106,-2.35765897900741,
3.46978213802687));
#26594=CARTESIAN_POINT('Ctrl Pts',(-2.4921297574377,-1.81451527526447,3.42058013104778));
#26595=CARTESIAN_POINT('Ctrl Pts',(-2.94162416323671,-0.904717906319905,
3.37137812406869));
#26596=CARTESIAN_POINT('Ctrl Pts',(-2.94619134998316,0.00116105206271745,
3.3221761170896));
#26597=CARTESIAN_POINT('Ctrl Pts',(-2.94627397750243,0.0010917140638196,
3.17782388291039));
#26598=CARTESIAN_POINT('Ctrl Pts',(-2.94192187979514,-0.909736247962167,
3.227298365885));
#26599=CARTESIAN_POINT('Ctrl Pts',(-2.48680392404959,-1.82432112348186,
3.27677284885962));
#26600=CARTESIAN_POINT('Ctrl Pts',(-1.75560149895312,-2.36671786778377,
3.32624733183423));
#26601=CARTESIAN_POINT('Ctrl Pts',(-0.97528579279443,-2.9455462250506,3.37904490853001));
#26602=CARTESIAN_POINT('Ctrl Pts',(0.119447932712268,-3.10050917866955,
3.43184248522579));
#26603=CARTESIAN_POINT('Ctrl Pts',(1.02975799022302,-2.76099413129472,3.48464006192158));
#26604=CARTESIAN_POINT('Ctrl Pts',(1.94006804773377,-2.42147908391989,3.53743763861736));
#26605=CARTESIAN_POINT('Ctrl Pts',(2.66595443724857,-1.58748603555126,3.59023521531314));
#26606=CARTESIAN_POINT('Ctrl Pts',(2.87664960568935,-0.639043935488772,
3.64303279200892));
#26607=CARTESIAN_POINT('Ctrl Pts',(3.08734477413012,0.309398164573712,3.6958303687047));
#26608=CARTESIAN_POINT('Ctrl Pts',(2.78284872149689,1.37228931633006,3.74862794540048));
#26609=CARTESIAN_POINT('Ctrl Pts',(2.10191238159562,2.06529766444029,3.80142552209626));
#26610=CARTESIAN_POINT('Ctrl Pts',(1.42097604169435,2.75830601255052,3.85422309879205));
#26611=CARTESIAN_POINT('Ctrl Pts',(0.363599414525042,3.08143155701465,3.90702067548783));
#26612=CARTESIAN_POINT('Ctrl Pts',(-0.588398467996306,2.88743438864685,
3.95981825218361));
#26613=CARTESIAN_POINT('Ctrl Pts',(-1.54039635051765,2.69343722027906,4.01261582887939));
#26614=CARTESIAN_POINT('Ctrl Pts',(-2.38701548839103,1.98231733907935,4.06541340557517));
#26615=CARTESIAN_POINT('Ctrl Pts',(-2.7424735561947,1.07811358323904,4.11821098227095));
#26616=CARTESIAN_POINT('Ctrl Pts',(-2.87625423202358,0.73780624321788,4.13808194915077));
#26617=CARTESIAN_POINT('Ctrl Pts',(-2.94046299306174,0.370148985435419,
4.15795291603058));
#26618=CARTESIAN_POINT('Ctrl Pts',(-2.93839638220268,0.00179748935179793,
4.17782388291039));
#26619=CARTESIAN_POINT('Origin',(0.,0.,0.));
#26620=CARTESIAN_POINT('',(-2.940183414122,-0.00248894513365655,5.32217611708959));
#26621=CARTESIAN_POINT('',(-2.93985340888279,-0.00241994382505922,5.17782388291038));
#26622=CARTESIAN_POINT('',(-2.942,-3.60291088309151E-16,0.));
#26623=CARTESIAN_POINT('Ctrl Pts',(-2.940183414122,-0.00248894513365655,
5.32217611708959));
#26624=CARTESIAN_POINT('Ctrl Pts',(-2.93461614813994,0.683436241442127,
5.28511669933751));
#26625=CARTESIAN_POINT('Ctrl Pts',(-2.69512958010689,1.37286568437424,5.24805728158542));
#26626=CARTESIAN_POINT('Ctrl Pts',(-2.2565518807566,1.89509465558241,5.21099786383333));
#26627=CARTESIAN_POINT('Ctrl Pts',(-1.6321178057218,2.63862895993905,5.1582337509301));
#26628=CARTESIAN_POINT('Ctrl Pts',(-0.604101521911408,3.04322734464819,
5.10546963802687));
#26629=CARTESIAN_POINT('Ctrl Pts',(0.35960053931388,2.92473889369513,5.05270552512364));
#26630=CARTESIAN_POINT('Ctrl Pts',(1.32330260053916,2.80625044274206,4.99994141222042));
#26631=CARTESIAN_POINT('Ctrl Pts',(2.22269043917934,2.16467515612679,4.94717729931719));
#26632=CARTESIAN_POINT('Ctrl Pts',(2.64841221253011,1.29202279263227,4.89441318641397));
#26633=CARTESIAN_POINT('Ctrl Pts',(3.07413398588089,0.419370429137726,4.84164907351074));
#26634=CARTESIAN_POINT('Ctrl Pts',(3.02618969394223,-0.684359011236085,
4.78888496060752));
#26635=CARTESIAN_POINT('Ctrl Pts',(2.52640093959537,-1.51680863544845,4.73612084770429));
#26636=CARTESIAN_POINT('Ctrl Pts',(2.02661218524851,-2.34925825966081,4.68335673480107));
#26637=CARTESIAN_POINT('Ctrl Pts',(1.07497896849345,-2.91042806771174,4.63059262189784));
#26638=CARTESIAN_POINT('Ctrl Pts',(0.104632352620345,-2.94490444920961,
4.57782850899461));
#26639=CARTESIAN_POINT('Ctrl Pts',(-0.86571426325276,-2.97938083070748,
4.52506439609139));
#26640=CARTESIAN_POINT('Ctrl Pts',(-1.8547742782439,-2.4871637856523,4.47230028318816));
#26641=CARTESIAN_POINT('Ctrl Pts',(-2.41238201044881,-1.69228342182741,
4.41953617028494));
#26642=CARTESIAN_POINT('Ctrl Pts',(-2.75534692531544,-1.20338045193787,
4.38708281921983));
#26643=CARTESIAN_POINT('Ctrl Pts',(-2.93509138494185,-0.599978505811401,
4.35462946815471));
#26644=CARTESIAN_POINT('Ctrl Pts',(-2.93825501966817,0.00168812480491387,
4.3221761170896));
#26645=CARTESIAN_POINT('Ctrl Pts',(-2.93839638220268,0.00179748935179793,
4.17782388291039));
#26646=CARTESIAN_POINT('Ctrl Pts',(-2.93497196456819,-0.608568682562856,
4.21075049272636));
#26647=CARTESIAN_POINT('Ctrl Pts',(-2.74957402147642,-1.22084103753697,
4.24367710254233));
#26648=CARTESIAN_POINT('Ctrl Pts',(-2.39720087876282,-1.71374386983141,
4.2766037123583));
#26649=CARTESIAN_POINT('Ctrl Pts',(-1.83217313579332,-2.50410993658064,
4.32940128905408));
#26650=CARTESIAN_POINT('Ctrl Pts',(-0.837820652120374,-2.98755443959817,
4.38219886574986));
#26651=CARTESIAN_POINT('Ctrl Pts',(0.132756003210123,-2.9437842904309,4.43499644244564));
#26652=CARTESIAN_POINT('Ctrl Pts',(1.10333265854061,-2.90001414126364,4.48779401914142));
#26653=CARTESIAN_POINT('Ctrl Pts',(2.05013348552865,-2.32902933991158,4.5405915958372));
#26654=CARTESIAN_POINT('Ctrl Pts',(2.5417259684161,-1.4910128122426,4.59338917253299));
#26655=CARTESIAN_POINT('Ctrl Pts',(3.03331845130357,-0.652996284573612,
4.64618674922877));
#26656=CARTESIAN_POINT('Ctrl Pts',(3.06970259009044,0.452051969412309,4.69898432592455));
#26657=CARTESIAN_POINT('Ctrl Pts',(2.63429907890363,1.32059019671555,4.75178190262033));
#26658=CARTESIAN_POINT('Ctrl Pts',(2.19889556771682,2.18912842401878,4.80457947931611));
#26659=CARTESIAN_POINT('Ctrl Pts',(1.29170440655633,2.82115662463934,4.85737705601189));
#26660=CARTESIAN_POINT('Ctrl Pts',(0.326109016449051,2.92867598314074,4.91017463270768));
#26661=CARTESIAN_POINT('Ctrl Pts',(-0.639486373658232,3.03619534164214,
4.96297220940346));
#26662=CARTESIAN_POINT('Ctrl Pts',(-1.66348599271231,2.61920585802438,5.01576978609924));
#26663=CARTESIAN_POINT('Ctrl Pts',(-2.2792798429615,1.86771879635947,5.06856736279502));
#26664=CARTESIAN_POINT('Ctrl Pts',(-2.70404361305101,1.34935623499724,5.10498620283347));
#26665=CARTESIAN_POINT('Ctrl Pts',(-2.93458316728716,0.671839798883881,
5.14140504287193));
#26666=CARTESIAN_POINT('Ctrl Pts',(-2.93985340888279,-0.00241994382505922,
5.17782388291038));
#26667=CARTESIAN_POINT('Origin',(0.,0.,0.));
#26668=CARTESIAN_POINT('',(-2.94670914091441,0.000353147988772619,6.3221761170896));
#26669=CARTESIAN_POINT('',(-2.94677477477595,5.75751945360796E-5,6.17782388291039));
#26670=CARTESIAN_POINT('',(-2.942,-3.60291088309151E-16,0.));
#26671=CARTESIAN_POINT('Ctrl Pts',(-2.94670914091441,0.000353147988772619,
6.3221761170896));
#26672=CARTESIAN_POINT('Ctrl Pts',(-2.94674188304789,0.0195649300909904,
6.32113215632675));
#26673=CARTESIAN_POINT('Ctrl Pts',(-2.94657014404334,0.0387761113611483,
6.32008819556391));
#26674=CARTESIAN_POINT('Ctrl Pts',(-2.94619213372924,0.0579832330598756,
6.31904423480106));
#26675=CARTESIAN_POINT('Ctrl Pts',(-2.92708664662515,1.02875414124661,6.26628012189784));
#26676=CARTESIAN_POINT('Ctrl Pts',(-2.38105743179868,1.98915480203517,6.21351600899462));
#26677=CARTESIAN_POINT('Ctrl Pts',(-1.55662693491459,2.50206369416578,6.16075189609139));
#26678=CARTESIAN_POINT('Ctrl Pts',(-0.732196438030497,3.01497258629639,
6.10798778318816));
#26679=CARTESIAN_POINT('Ctrl Pts',(0.370635340911205,3.08038970976906,6.05522367028493));
#26680=CARTESIAN_POINT('Ctrl Pts',(1.24992007493953,2.6685407904747,6.00245955738171));
#26681=CARTESIAN_POINT('Ctrl Pts',(2.12920480896786,2.25669187118035,5.94969544447848));
#26682=CARTESIAN_POINT('Ctrl Pts',(2.78494249808281,1.36757690911897,5.89693133157526));
#26683=CARTESIAN_POINT('Ctrl Pts',(2.91867743737271,0.405872098986324,5.84416721867204));
#26684=CARTESIAN_POINT('Ctrl Pts',(3.0524123766626,-0.555832711146327,5.79140310576881));
#26685=CARTESIAN_POINT('Ctrl Pts',(2.66414456612744,-1.59012736935025,5.73863899286558));
#26686=CARTESIAN_POINT('Ctrl Pts',(1.93059214323493,-2.22625787379709,5.68587487996235));
#26687=CARTESIAN_POINT('Ctrl Pts',(1.19703972034241,-2.86238837824392,5.63311076705913));
#26688=CARTESIAN_POINT('Ctrl Pts',(0.118202685092545,-3.10035472893366,
5.58034665415591));
#26689=CARTESIAN_POINT('Ctrl Pts',(-0.81489172222448,-2.8318477404717,5.52758254125268));
#26690=CARTESIAN_POINT('Ctrl Pts',(-1.7479861295415,-2.56334075200975,5.47481842834945));
#26691=CARTESIAN_POINT('Ctrl Pts',(-2.53533790892568,-1.78836042439612,
5.42205431544622));
#26692=CARTESIAN_POINT('Ctrl Pts',(-2.81858786548815,-0.859635148587238,
5.369290202543));
#26693=CARTESIAN_POINT('Ctrl Pts',(-2.90289429981681,-0.58320962879346,
5.35358550739186));
#26694=CARTESIAN_POINT('Ctrl Pts',(-2.94254265828655,-0.293163936945955,
5.33788081224073));
#26695=CARTESIAN_POINT('Ctrl Pts',(-2.940183414122,-0.00248894513365655,
5.32217611708959));
#26696=CARTESIAN_POINT('Ctrl Pts',(-2.93985340888279,-0.00241994382505923,
5.17782388291039));
#26697=CARTESIAN_POINT('Ctrl Pts',(-2.94222360790956,-0.305656476147461,
5.19420261956771));
#26698=CARTESIAN_POINT('Ctrl Pts',(-2.89903098481243,-0.608234311816698,
5.21058135622504));
#26699=CARTESIAN_POINT('Ctrl Pts',(-2.80745159681895,-0.895380163016774,
5.22696009288236));
#26700=CARTESIAN_POINT('Ctrl Pts',(-2.51224141898293,-1.82100742101599,
5.27975766957815));
#26701=CARTESIAN_POINT('Ctrl Pts',(-1.71423298186661,-2.58627729730233,
5.33255524627393));
#26702=CARTESIAN_POINT('Ctrl Pts',(-0.777057978406682,-2.8424762097523,
5.38535282296971));
#26703=CARTESIAN_POINT('Ctrl Pts',(0.160117025053262,-3.09867512220227,
5.43815039966549));
#26704=CARTESIAN_POINT('Ctrl Pts',(1.23645859485682,-2.84580307081584,5.49094797636127));
#26705=CARTESIAN_POINT('Ctrl Pts',(1.96150586742938,-2.19908727358619,5.54374555305705));
#26706=CARTESIAN_POINT('Ctrl Pts',(2.68655314000193,-1.55237147635655,5.59654312975283));
#26707=CARTESIAN_POINT('Ctrl Pts',(3.06030611534348,-0.511811933283709,
5.64934070644862));
#26708=CARTESIAN_POINT('Ctrl Pts',(2.91245528187179,0.448435431144968,5.7021382831444));
#26709=CARTESIAN_POINT('Ctrl Pts',(2.76460444840011,1.40868279557365,5.75493585984018));
#26710=CARTESIAN_POINT('Ctrl Pts',(2.09514980611517,2.28861798135817,5.80773343653596));
#26711=CARTESIAN_POINT('Ctrl Pts',(1.2091444266347,2.68727740666057,5.86053101323174));
#26712=CARTESIAN_POINT('Ctrl Pts',(0.323139047154223,3.08593683196296,5.91332858992752));
#26713=CARTESIAN_POINT('Ctrl Pts',(-0.779417069521796,3.00332049678325,
5.9661261666233));
#26714=CARTESIAN_POINT('Ctrl Pts',(-1.59611777250727,2.47707451666191,6.01892374331908));
#26715=CARTESIAN_POINT('Ctrl Pts',(-2.41281847549274,1.95082853654058,6.07172132001487));
#26716=CARTESIAN_POINT('Ctrl Pts',(-2.94366376478766,0.980952911477632,
6.12451889671065));
#26717=CARTESIAN_POINT('Ctrl Pts',(-2.94676124645694,0.00939474262821921,
6.17731647340643));
#26718=CARTESIAN_POINT('Ctrl Pts',(-2.94677116920804,0.00628236589065139,
6.17748560990775));
#26719=CARTESIAN_POINT('Ctrl Pts',(-2.94677567602789,0.0031699718862354,
6.17765474640907));
#26720=CARTESIAN_POINT('Ctrl Pts',(-2.94677477477595,5.75751945359972E-5,
6.17782388291039));
#26721=CARTESIAN_POINT('Origin',(0.,0.,0.));
#26722=CARTESIAN_POINT('',(-2.93921061841706,0.00219993862087403,7.3221761170896));
#26723=CARTESIAN_POINT('',(-2.9396928876012,0.00237510757666561,7.17782388291039));
#26724=CARTESIAN_POINT('',(-2.942,-3.60291088309151E-16,0.));
#26725=CARTESIAN_POINT('Ctrl Pts',(-2.93921061841706,0.00219993862087403,
7.3221761170896));
#26726=CARTESIAN_POINT('Ctrl Pts',(-2.94151862483926,0.331795310107375,
7.30438350041277));
#26727=CARTESIAN_POINT('Ctrl Pts',(-2.89034506178059,0.660694979142846,
7.28659088373595));
#26728=CARTESIAN_POINT('Ctrl Pts',(-2.78258184963522,0.969870297640249,
7.26879826705912));
#26729=CARTESIAN_POINT('Ctrl Pts',(-2.46300938900557,1.8867315838915,7.2160341541559));
#26730=CARTESIAN_POINT('Ctrl Pts',(-1.64577474805962,2.63013246788686,7.16327004125268));
#26731=CARTESIAN_POINT('Ctrl Pts',(-0.702838155545203,2.86171778330323,
7.11050592834945));
#26732=CARTESIAN_POINT('Ctrl Pts',(0.24009843696921,3.0933030987196,7.05774181544623));
#26733=CARTESIAN_POINT('Ctrl Pts',(1.30873698105206,2.81307284555698,7.004977702543));
#26734=CARTESIAN_POINT('Ctrl Pts',(2.01669202827731,2.14857241145066,6.95221358963978));
#26735=CARTESIAN_POINT('Ctrl Pts',(2.72464707550255,1.48407197734434,6.89944947673655));
#26736=CARTESIAN_POINT('Ctrl Pts',(3.07191862587017,0.435301362294284,6.84668536383332));
#26737=CARTESIAN_POINT('Ctrl Pts',(2.90044778314584,-0.520396773057355,
6.7939212509301));
#26738=CARTESIAN_POINT('Ctrl Pts',(2.72897694042151,-1.476094908409,6.74115713802687));
#26739=CARTESIAN_POINT('Ctrl Pts',(2.03876370460524,-2.33872056406225,6.68839302512365));
#26740=CARTESIAN_POINT('Ctrl Pts',(1.14395515196615,-2.7156540196524,6.63562891222042));
#26741=CARTESIAN_POINT('Ctrl Pts',(0.249146599327066,-3.09258747524255,
6.58286479931719));
#26742=CARTESIAN_POINT('Ctrl Pts',(-0.850257270134833,-2.98382873076961,
6.53010068641397));
#26743=CARTESIAN_POINT('Ctrl Pts',(-1.65386832517493,-2.43887878074069,
6.47733657351074));
#26744=CARTESIAN_POINT('Ctrl Pts',(-2.44157958840789,-1.90471090083939,
6.42561642137036));
#26745=CARTESIAN_POINT('Ctrl Pts',(-2.94508702235829,-0.95144152531619,
6.37389626922998));
#26746=CARTESIAN_POINT('Ctrl Pts',(-2.94670914091441,0.000353147988772619,
6.3221761170896));
#26747=CARTESIAN_POINT('Ctrl Pts',(-2.94677477477595,5.75751945360796E-5,
6.17782388291039));
#26748=CARTESIAN_POINT('Ctrl Pts',(-2.94649434161591,-0.96839442583636,
6.23045232310485));
#26749=CARTESIAN_POINT('Ctrl Pts',(-2.42260291217609,-1.93710661038694,
6.28308076329931));
#26750=CARTESIAN_POINT('Ctrl Pts',(-1.61187977882684,-2.46684691122469,
6.33570920349377));
#26751=CARTESIAN_POINT('Ctrl Pts',(-0.798551155483845,-2.99828968359228,
6.38850678018955));
#26752=CARTESIAN_POINT('Ctrl Pts',(0.303455765245771,-3.08793451569159,
6.44130435688534));
#26753=CARTESIAN_POINT('Ctrl Pts',(1.19198508678719,-2.69493258870913,6.49410193358112));
#26754=CARTESIAN_POINT('Ctrl Pts',(2.0805144083286,-2.30193066172667,6.5468995102769));
#26755=CARTESIAN_POINT('Ctrl Pts',(2.75556613068181,-1.42628197566246,6.59969708697268));
#26756=CARTESIAN_POINT('Ctrl Pts',(2.90953673839141,-0.466996865899832,
6.65249466366846));
#26757=CARTESIAN_POINT('Ctrl Pts',(3.063507346101,0.492288243862799,6.70529224036424));
#26758=CARTESIAN_POINT('Ctrl Pts',(2.69639683916696,1.53520977732385,6.75808981706003));
#26759=CARTESIAN_POINT('Ctrl Pts',(1.97548792905307,2.18653551239746,6.81088739375581));
#26760=CARTESIAN_POINT('Ctrl Pts',(1.25457901893917,2.83786124747105,6.86368497045159));
#26761=CARTESIAN_POINT('Ctrl Pts',(0.179871705645437,3.09759118415722,6.91648254714737));
#26762=CARTESIAN_POINT('Ctrl Pts',(-0.758917835447689,2.84737314447,6.96928012384315));
#26763=CARTESIAN_POINT('Ctrl Pts',(-1.69770737654082,2.59715510478277,7.02207770053893));
#26764=CARTESIAN_POINT('Ctrl Pts',(-2.50057914543333,1.83698908872215,7.07487527723471));
#26765=CARTESIAN_POINT('Ctrl Pts',(-2.80168535536551,0.913262982026531,
7.1276728539305));
#26766=CARTESIAN_POINT('Ctrl Pts',(-2.89702297756577,0.620788606966313,
7.14438986359046));
#26767=CARTESIAN_POINT('Ctrl Pts',(-2.94205804349871,0.3119171506092,7.16110687325043));
#26768=CARTESIAN_POINT('Ctrl Pts',(-2.9396928876012,0.00237510757666561,
7.17782388291039));
#26769=CARTESIAN_POINT('Origin',(0.,0.,0.));
#26770=CARTESIAN_POINT('',(-2.93902884880934,-0.00212417613307953,8.3221761170896));
#26771=CARTESIAN_POINT('',(-2.93851596067447,-0.00187194491636513,8.17782388291039));
#26772=CARTESIAN_POINT('',(-2.942,-3.60291088309151E-16,0.));
#26773=CARTESIAN_POINT('Ctrl Pts',(-2.93902884880934,-0.00212417613307953,
8.3221761170896));
#26774=CARTESIAN_POINT('Ctrl Pts',(-2.93472032584333,0.63782764634564,8.2876348444988));
#26775=CARTESIAN_POINT('Ctrl Pts',(-2.72915033143689,1.28029955423599,8.25309357190799));
#26776=CARTESIAN_POINT('Ctrl Pts',(-2.34392897127172,1.78589112820386,8.21855229931719));
#26777=CARTESIAN_POINT('Ctrl Pts',(-1.75547748075246,2.55821620168318,8.16578818641397));
#26778=CARTESIAN_POINT('Ctrl Pts',(-0.747816469944497,3.01113630499568,
8.11302407351074));
#26779=CARTESIAN_POINT('Ctrl Pts',(0.220422229727873,2.93850713540157,8.06025996060752));
#26780=CARTESIAN_POINT('Ctrl Pts',(1.18866092940026,2.86587796580745,8.00749584770429));
#26781=CARTESIAN_POINT('Ctrl Pts',(2.11747731793707,2.26769952330669,7.95473173480106));
#26782=CARTESIAN_POINT('Ctrl Pts',(2.58412529643943,1.41622971175793,7.90196762189784));
#26783=CARTESIAN_POINT('Ctrl Pts',(3.05077327494178,0.564759900209195,7.84920350899461));
#26784=CARTESIAN_POINT('Ctrl Pts',(3.05525284340971,-0.540001280387511,
7.79643939609139));
#26785=CARTESIAN_POINT('Ctrl Pts',(2.59552514882778,-1.3952273456203,7.74367528318817));
#26786=CARTESIAN_POINT('Ctrl Pts',(2.13579745424584,-2.25045341085309,7.69091117028494));
#26787=CARTESIAN_POINT('Ctrl Pts',(1.21186249661401,-2.85614436072195,7.63814705738171));
#26788=CARTESIAN_POINT('Ctrl Pts',(0.244244616152473,-2.93662301149546,
7.58538294447848));
#26789=CARTESIAN_POINT('Ctrl Pts',(-0.723373264309057,-3.01710166226897,
7.53261883157526));
#26790=CARTESIAN_POINT('Ctrl Pts',(-1.7346740676003,-2.57236801394714,7.47985471867203));
#26791=CARTESIAN_POINT('Ctrl Pts',(-2.32936932908925,-1.80484034553266,
7.42709060576881));
#26792=CARTESIAN_POINT('Ctrl Pts',(-2.72352706147006,-1.29613112097227,
7.3921191095424));
#26793=CARTESIAN_POINT('Ctrl Pts',(-2.93467421776558,-0.645621767401394,
7.357147613316));
#26794=CARTESIAN_POINT('Ctrl Pts',(-2.93921061841706,0.00219993862087403,
7.3221761170896));
#26795=CARTESIAN_POINT('Ctrl Pts',(-2.9396928876012,0.00237510757666561,
7.17782388291039));
#26796=CARTESIAN_POINT('Ctrl Pts',(-2.93458813695223,-0.665714022071069,
7.21390444994621));
#26797=CARTESIAN_POINT('Ctrl Pts',(-2.70867788182517,-1.33692696049954,
7.24998501698203));
#26798=CARTESIAN_POINT('Ctrl Pts',(-2.29114255557572,-1.85314756423755,
7.28606558401784));
#26799=CARTESIAN_POINT('Ctrl Pts',(-1.68015289488189,-2.60854580647539,
7.33886316071362));
#26800=CARTESIAN_POINT('Ctrl Pts',(-0.658832922522417,-3.03205609362045,
7.3916607374094));
#26801=CARTESIAN_POINT('Ctrl Pts',(0.307428409071859,-2.9306958010181,7.44445831410518));
#26802=CARTESIAN_POINT('Ctrl Pts',(1.27368974066613,-2.82933550841574,7.49725589080096));
#26803=CARTESIAN_POINT('Ctrl Pts',(2.18489243149519,-2.20310463606597,7.55005346749675));
#26804=CARTESIAN_POINT('Ctrl Pts',(2.62582511077046,-1.33736030764222,7.60285104419253));
#26805=CARTESIAN_POINT('Ctrl Pts',(3.06675779004572,-0.471615979218467,
7.65564862088831));
#26806=CARTESIAN_POINT('Ctrl Pts',(3.03742045776721,0.633641805279265,7.70844619758409));
#26807=CARTESIAN_POINT('Ctrl Pts',(2.5511813733499,1.47477581519432,7.76124377427987));
#26808=CARTESIAN_POINT('Ctrl Pts',(2.0649422889326,2.31590982510937,7.81404135097565));
#26809=CARTESIAN_POINT('Ctrl Pts',(1.12180145237649,2.89292006044175,7.86683892767144));
#26810=CARTESIAN_POINT('Ctrl Pts',(0.151523616940655,2.94287796184599,7.91963650436722));
#26811=CARTESIAN_POINT('Ctrl Pts',(-0.818754218495187,2.99283586325022,
7.972434081063));
#26812=CARTESIAN_POINT('Ctrl Pts',(-1.81616905281075,2.51574143072631,8.02523165775878));
#26813=CARTESIAN_POINT('Ctrl Pts',(-2.38622488333927,1.72899419054607,8.07802923445456));
#26814=CARTESIAN_POINT('Ctrl Pts',(-2.74538607196463,1.2333075247876,8.11129411727317));
#26815=CARTESIAN_POINT('Ctrl Pts',(-2.93490389706639,0.614701853345732,
8.14455900009178));
#26816=CARTESIAN_POINT('Ctrl Pts',(-2.93851596067447,-0.00187194491636513,
8.17782388291039));
#26817=CARTESIAN_POINT('Origin',(0.,0.,0.));
#26818=CARTESIAN_POINT('',(-2.94665746643035,-0.000496894171833351,9.3221761170896));
#26819=CARTESIAN_POINT('',(-2.94636616095733,-0.000987191619394096,9.17782388291039));
#26820=CARTESIAN_POINT('',(-2.942,-3.60291088309151E-16,0.));
#26821=CARTESIAN_POINT('Ctrl Pts',(-2.94665746643035,-0.000496894171833351,
9.3221761170896));
#26822=CARTESIAN_POINT('Ctrl Pts',(-2.94443817053572,0.943424973374663,
9.27088618858482));
#26823=CARTESIAN_POINT('Ctrl Pts',(-2.45042926639946,1.88934479557273,9.21959626008003));
#26824=CARTESIAN_POINT('Ctrl Pts',(-1.67359187304369,2.42538664683515,9.16830633157526));
#26825=CARTESIAN_POINT('Ctrl Pts',(-0.874426478873733,2.9768355099044,9.11554221867203));
#26826=CARTESIAN_POINT('Ctrl Pts',(0.224059267942015,3.09450622303989,9.06277810576881));
#26827=CARTESIAN_POINT('Ctrl Pts',(1.12189511505486,2.72484155410552,9.01001399286558));
#26828=CARTESIAN_POINT('Ctrl Pts',(2.01973096216771,2.35517688517114,8.95724987996236));
#26829=CARTESIAN_POINT('Ctrl Pts',(2.71691690957765,1.49817683416691,8.90448576705913));
#26830=CARTESIAN_POINT('Ctrl Pts',(2.89613228646949,0.54390065584916,8.8517216541559));
#26831=CARTESIAN_POINT('Ctrl Pts',(3.07534766336132,-0.410375522468571,
8.79895754125268));
#26832=CARTESIAN_POINT('Ctrl Pts',(2.73659246973507,-1.46192782809981,8.74619342834945));
#26833=CARTESIAN_POINT('Ctrl Pts',(2.03404942496847,-2.13214752795147,8.69342931544623));
#26834=CARTESIAN_POINT('Ctrl Pts',(1.33150638020187,-2.80236722780314,8.640665202543));
#26835=CARTESIAN_POINT('Ctrl Pts',(0.265175484294899,-3.09125432187523,
8.58790108963977));
#26836=CARTESIAN_POINT('Ctrl Pts',(-0.679608128765257,-2.86732330501468,
8.53513697673655));
#26837=CARTESIAN_POINT('Ctrl Pts',(-1.62439174182541,-2.64339228815413,
8.48237286383332));
#26838=CARTESIAN_POINT('Ctrl Pts',(-2.44762807203876,-1.90664316036094,
8.4296087509301));
#26839=CARTESIAN_POINT('Ctrl Pts',(-2.77462525203015,-0.992403574641266,
8.37684463802687));
#26840=CARTESIAN_POINT('Ctrl Pts',(-2.88755840044724,-0.676657870578698,
8.35862179771445));
#26841=CARTESIAN_POINT('Ctrl Pts',(-2.94130188393814,-0.339741727368865,
8.34039895740202));
#26842=CARTESIAN_POINT('Ctrl Pts',(-2.93902884880934,-0.00212417613307953,
8.3221761170896));
#26843=CARTESIAN_POINT('Ctrl Pts',(-2.93851596067447,-0.00187194491636513,
8.17782388291039));
#26844=CARTESIAN_POINT('Ctrl Pts',(-2.94063691607077,-0.363915825239363,
8.19735657678756));
#26845=CARTESIAN_POINT('Ctrl Pts',(-2.87865977372572,-0.725259139831482,
8.21688927066473));
#26846=CARTESIAN_POINT('Ctrl Pts',(-2.74929213038533,-1.06060496256188,
8.23642196454191));
#26847=CARTESIAN_POINT('Ctrl Pts',(-2.39960672016141,-1.96705682765307,
8.28921954123769));
#26848=CARTESIAN_POINT('Ctrl Pts',(-1.55753907297209,-2.6835605099989,8.34201711793347));
#26849=CARTESIAN_POINT('Ctrl Pts',(-0.606797518045518,-2.88362391391516,
8.39481469462925));
#26850=CARTESIAN_POINT('Ctrl Pts',(0.343944036881066,-3.08368731783141,
8.44761227132503));
#26851=CARTESIAN_POINT('Ctrl Pts',(1.40335949954491,-2.7673104433181,8.50040984802081));
#26852=CARTESIAN_POINT('Ctrl Pts',(2.0887007932398,-2.07865800485049,8.55320742471659));
#26853=CARTESIAN_POINT('Ctrl Pts',(2.77404208693468,-1.39000556638288,8.60600500141238));
#26854=CARTESIAN_POINT('Ctrl Pts',(3.08530921166061,-0.329077563960986,
8.65880257810816));
#26855=CARTESIAN_POINT('Ctrl Pts',(2.88066583304364,0.62068870067415,8.71160015480394));
#26856=CARTESIAN_POINT('Ctrl Pts',(2.67602245442666,1.5704549653093,8.76439773149972));
#26857=CARTESIAN_POINT('Ctrl Pts',(1.95546857246677,2.4090594921577,8.8171953081955));
#26858=CARTESIAN_POINT('Ctrl Pts',(1.04734185348866,2.75437200587366,8.86999288489128));
#26859=CARTESIAN_POINT('Ctrl Pts',(0.139215134510575,3.09968451958961,8.92279046158706));
#26860=CARTESIAN_POINT('Ctrl Pts',(-0.956484421485707,2.95170502017316,
8.97558803828284));
#26861=CARTESIAN_POINT('Ctrl Pts',(-1.74047502001417,2.37786391736706,9.02838561497862));
#26862=CARTESIAN_POINT('Ctrl Pts',(-2.48014405062107,1.83646394008204,9.07819837095588));
#26863=CARTESIAN_POINT('Ctrl Pts',(-2.94235176373734,0.915992015346281,
9.12801112693314));
#26864=CARTESIAN_POINT('Ctrl Pts',(-2.94636616095733,-0.000987191619394096,
9.17782388291039));
#26865=CARTESIAN_POINT('Origin',(0.,0.,0.));
#26866=CARTESIAN_POINT('',(-2.94039988794905,0.00253112492490451,10.3221761170896));
#26867=CARTESIAN_POINT('',(-2.94130383534194,0.00264460613430074,10.1778238829104));
#26868=CARTESIAN_POINT('',(-2.942,-3.60291088309151E-16,0.));
#26869=CARTESIAN_POINT('Ctrl Pts',(-2.94039988794905,0.00253112492490451,
10.3221761170896));
#26870=CARTESIAN_POINT('Ctrl Pts',(-2.94274634020493,0.285190445035712,
10.3069016455741));
#26871=CARTESIAN_POINT('Ctrl Pts',(-2.90528029294341,0.56724066031149,10.2916271740585));
#26872=CARTESIAN_POINT('Ctrl Pts',(-2.82546634051429,0.836749725297203,
10.276352702543));
#26873=CARTESIAN_POINT('Ctrl Pts',(-2.54975713558759,1.76774146002846,10.2235885896398));
#26874=CARTESIAN_POINT('Ctrl Pts',(-1.76871589896699,2.54908128327144,10.1708244767365));
#26875=CARTESIAN_POINT('Ctrl Pts',(-0.837829613801701,2.82514631168034,
10.1180603638333));
#26876=CARTESIAN_POINT('Ctrl Pts',(0.0930566713635576,3.10121134008923,
10.0652962509301));
#26877=CARTESIAN_POINT('Ctrl Pts',(1.17378800507349,2.87200157366407,10.0125321380269));
#26878=CARTESIAN_POINT('Ctrl Pts',(1.91247496663932,2.24184068259591,9.95976802512365));
#26879=CARTESIAN_POINT('Ctrl Pts',(2.65116192820514,1.61167979152774,9.90700391222042));
#26880=CARTESIAN_POINT('Ctrl Pts',(3.04780451762686,0.580567775816567,9.8542397993172));
#26881=CARTESIAN_POINT('Ctrl Pts',(2.92187285902738,-0.382189926402199,
9.80147568641397));
#26882=CARTESIAN_POINT('Ctrl Pts',(2.79594120042789,-1.34494762862098,9.74871157351074));
#26883=CARTESIAN_POINT('Ctrl Pts',(2.14743529380718,-2.23935101734735,9.69594746060752));
#26884=CARTESIAN_POINT('Ctrl Pts',(1.27151933471594,-2.65831689713767,9.64318334770429));
#26885=CARTESIAN_POINT('Ctrl Pts',(0.395603375624702,-3.077282776928,9.59041923480107));
#26886=CARTESIAN_POINT('Ctrl Pts',(-0.707722635937064,-3.02081114778227,
9.53765512189783));
#26887=CARTESIAN_POINT('Ctrl Pts',(-1.53628542551181,-2.51460478714333,
9.48489100899461));
#26888=CARTESIAN_POINT('Ctrl Pts',(-2.36484821508653,-2.0083984265044,9.43212689609138));
#26889=CARTESIAN_POINT('Ctrl Pts',(-2.91864778267424,-1.05245733437228,
9.37936278318816));
#26890=CARTESIAN_POINT('Ctrl Pts',(-2.94562504570603,-0.0818732818047256,
9.32659867028494));
#26891=CARTESIAN_POINT('Ctrl Pts',(-2.94637876747043,-0.054755989597048,
9.32512448588649));
#26892=CARTESIAN_POINT('Ctrl Pts',(-2.9467212538342,-0.0276272671525533,
9.32365030148805));
#26893=CARTESIAN_POINT('Ctrl Pts',(-2.94665746643035,-0.000496894171833351,
9.3221761170896));
#26894=CARTESIAN_POINT('Ctrl Pts',(-2.94636616095733,-0.000987191619394096,
9.17782388291039));
#26895=CARTESIAN_POINT('Ctrl Pts',(-2.946606706893,-0.0559333290436887,
9.18080870362892));
#26896=CARTESIAN_POINT('Ctrl Pts',(-2.94520210810221,-0.110866925852438,
9.18379352434745));
#26897=CARTESIAN_POINT('Ctrl Pts',(-2.94211348083954,-0.165705674832853,
9.18677834506597));
#26898=CARTESIAN_POINT('Ctrl Pts',(-2.88747970207578,-1.13573145803076,
9.23957592176175));
#26899=CARTESIAN_POINT('Ctrl Pts',(-2.30593050348768,-2.07608031823082,
9.29237349845753));
#26900=CARTESIAN_POINT('Ctrl Pts',(-1.46246273194259,-2.55825973319532,
9.34517107515332));
#26901=CARTESIAN_POINT('Ctrl Pts',(-0.618994960397504,-3.04043914815982,
9.3979686518491));
#26902=CARTESIAN_POINT('Ctrl Pts',(0.486391384104583,-3.06444911788875,
9.45076622854488));
#26903=CARTESIAN_POINT('Ctrl Pts',(1.35000048945615,-2.61934892354526,9.50356380524066));
#26904=CARTESIAN_POINT('Ctrl Pts',(2.21360959480774,-2.17424872920176,9.55636138193644));
#26905=CARTESIAN_POINT('Ctrl Pts',(2.8354414610088,-1.26003837078583,9.60915895863223));
#26906=CARTESIAN_POINT('Ctrl Pts',(2.93214347709368,-0.293299734992319,
9.66195653532801));
#26907=CARTESIAN_POINT('Ctrl Pts',(3.02884549317855,0.673438900801169,9.71475411202378));
#26908=CARTESIAN_POINT('Ctrl Pts',(2.60041765914726,1.69270581397223,9.76755168871956));
#26909=CARTESIAN_POINT('Ctrl Pts',(1.84208339789187,2.30004757777328,9.82034926541534));
#26910=CARTESIAN_POINT('Ctrl Pts',(1.08374913663646,2.90738934157434,9.87314684211112));
#26911=CARTESIAN_POINT('Ctrl Pts',(-0.00449155184308325,3.10280595600537,
9.92594441880692));
#26912=CARTESIAN_POINT('Ctrl Pts',(-0.926755685023515,2.79725115159261,
9.9787419955027));
#26913=CARTESIAN_POINT('Ctrl Pts',(-1.84901981820395,2.49169634717984,10.0315395721985));
#26914=CARTESIAN_POINT('Ctrl Pts',(-2.60530739608529,1.6851701239233,10.0843371488943));
#26915=CARTESIAN_POINT('Ctrl Pts',(-2.85099783635035,0.745185508403901,
10.13713472559));
#26916=CARTESIAN_POINT('Ctrl Pts',(-2.91411270892398,0.503714944202581,
10.1506977780301));
#26917=CARTESIAN_POINT('Ctrl Pts',(-2.94353259565806,0.253437282769067,
10.1642608304703));
#26918=CARTESIAN_POINT('Ctrl Pts',(-2.94130383534194,0.00264460613430074,
10.1778238829104));
#26919=CARTESIAN_POINT('Origin',(0.,0.,0.));
#26920=CARTESIAN_POINT('',(-2.93811988821084,-0.00158572391977807,11.3221761170896));
#26921=CARTESIAN_POINT('',(-2.9376139453736,-0.001087489077759,11.1778238829104));
#26922=CARTESIAN_POINT('',(-2.942,-3.60291088309151E-16,0.));
#26923=CARTESIAN_POINT('Ctrl Pts',(-2.93811988821084,-0.00158572391977807,
11.3221761170896));
#26924=CARTESIAN_POINT('Ctrl Pts',(-2.93519577795759,0.592173285545134,
11.2901529896601));
#26925=CARTESIAN_POINT('Ctrl Pts',(-2.76052119328951,1.18751446039404,11.2581298622306));
#26926=CARTESIAN_POINT('Ctrl Pts',(-2.42602614988553,1.6726647196123,11.2261067348011));
#26927=CARTESIAN_POINT('Ctrl Pts',(-1.87488278406078,2.47204083016763,11.1733426218978));
#26928=CARTESIAN_POINT('Ctrl Pts',(-0.889846893775436,2.97226240860755,
11.1205785089946));
#26929=CARTESIAN_POINT('Ctrl Pts',(0.0807473991431609,2.94565612414208,
11.0678143960914));
#26930=CARTESIAN_POINT('Ctrl Pts',(1.05134169206174,2.91904983967661,11.0150502831882));
#26931=CARTESIAN_POINT('Ctrl Pts',(2.00749438761357,2.36561569230577,10.9622861702849));
#26932=CARTESIAN_POINT('Ctrl Pts',(2.51401740451069,1.53724644542814,10.9095220573817));
#26933=CARTESIAN_POINT('Ctrl Pts',(3.02054042140782,0.70887719855049,10.8567579444785));
#26934=CARTESIAN_POINT('Ctrl Pts',(3.07743375965022,-0.394427147833989,
10.8039938315753));
#26935=CARTESIAN_POINT('Ctrl Pts',(2.65880270302471,-1.27050318006396,10.751229718672));
#26936=CARTESIAN_POINT('Ctrl Pts',(2.2401716463992,-2.14657921229393,10.6984656057688));
#26937=CARTESIAN_POINT('Ctrl Pts',(1.34601619490581,-2.79542693036942,10.6457014928656));
#26938=CARTESIAN_POINT('Ctrl Pts',(0.383306696605943,-2.92172656497852,
10.5929373799624));
#26939=CARTESIAN_POINT('Ctrl Pts',(-0.579402801693943,-3.04802619958762,
10.5401732670591));
#26940=CARTESIAN_POINT('Ctrl Pts',(-1.6106663468003,-2.65177775073031,10.4874091541559));
#26941=CARTESIAN_POINT('Ctrl Pts',(-2.24110953273706,-1.91333170319189,
10.4346450412527));
#26942=CARTESIAN_POINT('Ctrl Pts',(-2.68904824819375,-1.38865544156027,
10.397155399865));
#26943=CARTESIAN_POINT('Ctrl Pts',(-2.93464075883505,-0.691227512489607,
10.3596657584773));
#26944=CARTESIAN_POINT('Ctrl Pts',(-2.94039988794905,0.00253112492490451,
10.3221761170896));
#26945=CARTESIAN_POINT('Ctrl Pts',(-2.94130383534194,0.00264460613430074,
10.1778238829104));
#26946=CARTESIAN_POINT('Ctrl Pts',(-2.93485658822933,-0.722835988887616,
10.217058407166));
#26947=CARTESIAN_POINT('Ctrl Pts',(-2.66357332332191,-1.45262623338011,
10.2562929314217));
#26948=CARTESIAN_POINT('Ctrl Pts',(-2.17698883749842,-1.98600345070618,
10.2955274556774));
#26949=CARTESIAN_POINT('Ctrl Pts',(-1.52219609573261,-2.70376478651468,
10.3483250323732));
#26950=CARTESIAN_POINT('Ctrl Pts',(-0.477517309552185,-3.06584445034943,
10.4011226090689));
#26951=CARTESIAN_POINT('Ctrl Pts',(0.481014564589377,-2.90725215512216,
10.4539201857647));
#26952=CARTESIAN_POINT('Ctrl Pts',(1.43954643873093,-2.7486598598949,10.5067177624605));
#26953=CARTESIAN_POINT('Ctrl Pts',(2.3119314008336,-2.06939560560563,10.5595153391563));
#26954=CARTESIAN_POINT('Ctrl Pts',(2.70064630965162,-1.17898244896802,10.6123129158521));
#26955=CARTESIAN_POINT('Ctrl Pts',(3.08936121846965,-0.288569292330407,
10.6651104925479));
#26956=CARTESIAN_POINT('Ctrl Pts',(2.99440607400299,0.812992766655582,10.7179080692436));
#26957=CARTESIAN_POINT('Ctrl Pts',(2.45904946631867,1.62375054334323,10.7707056459394));
#26958=CARTESIAN_POINT('Ctrl Pts',(1.92369285863434,2.43450832003088,10.8235032226352));
#26959=CARTESIAN_POINT('Ctrl Pts',(0.947934787732336,2.95446181442022,10.876300799331));
#26960=CARTESIAN_POINT('Ctrl Pts',(-0.023597167633587,2.94668174027824,
10.9290983760268));
#26961=CARTESIAN_POINT('Ctrl Pts',(-0.995129122999497,2.93890166613627,
10.9818959527225));
#26962=CARTESIAN_POINT('Ctrl Pts',(-1.96243496282931,2.40338802346302,11.0346935294183));
#26963=CARTESIAN_POINT('Ctrl Pts',(-2.48473857027235,1.58416045342967,11.0874911061141));
#26964=CARTESIAN_POINT('Ctrl Pts',(-2.78261294345243,1.11694771463552,11.1176020317129));
#26965=CARTESIAN_POINT('Ctrl Pts',(-2.93574936512043,0.557456399077179,
11.1477129573116));
#26966=CARTESIAN_POINT('Ctrl Pts',(-2.9376139453736,-0.001087489077759,
11.1778238829104));
#26967=CARTESIAN_POINT('Origin',(0.,0.,0.));
#26968=CARTESIAN_POINT('',(-2.9460560275736,-0.00128820797444335,12.3221761170896));
#26969=CARTESIAN_POINT('',(-2.94523166487087,-0.00185944496279741,12.1778238829104));
#26970=CARTESIAN_POINT('',(-2.942,-3.60291088309151E-16,0.));
#26971=CARTESIAN_POINT('Ctrl Pts',(-2.9460560275736,-0.00128820797444335,
12.3221761170896));
#26972=CARTESIAN_POINT('Ctrl Pts',(-2.94111144504364,0.896779189536789,
12.2734043337461));
#26973=CARTESIAN_POINT('Ctrl Pts',(-2.50046702038657,1.79904631809884,12.2246325504026));
#26974=CARTESIAN_POINT('Ctrl Pts',(-1.78678689418432,2.3432461968251,12.1758607670591));
#26975=CARTESIAN_POINT('Ctrl Pts',(-1.01468679502424,2.93199284241738,12.1230966541559));
#26976=CARTESIAN_POINT('Ctrl Pts',(0.0769784812166023,3.10165208129682,
12.0703325412527));
#26977=CARTESIAN_POINT('Ctrl Pts',(0.991342985003044,2.77500436580727,12.0175684283495));
#26978=CARTESIAN_POINT('Ctrl Pts',(1.90570748878951,2.4483566503177,11.9648043154462));
#26979=CARTESIAN_POINT('Ctrl Pts',(2.64277122012159,1.62540198045911,11.912040202543));
#26980=CARTESIAN_POINT('Ctrl Pts',(2.86706333577767,0.680704027315496,11.8592760896398));
#26981=CARTESIAN_POINT('Ctrl Pts',(3.09135545143376,-0.263993925828108,
11.8065119767365));
#26982=CARTESIAN_POINT('Ctrl Pts',(2.80287595141388,-1.33043516225671,11.7537478638333));
#26983=CARTESIAN_POINT('Ctrl Pts',(2.13292482649212,-2.03323432705079,11.7009837509301));
#26984=CARTESIAN_POINT('Ctrl Pts',(1.46297370157037,-2.73603349184485,11.6482196380269));
#26985=CARTESIAN_POINT('Ctrl Pts',(0.411550951746749,-3.07519058500439,
11.5954555251236));
#26986=CARTESIAN_POINT('Ctrl Pts',(-0.542793656558674,-2.89633996460426,
11.5426914122204));
#26987=CARTESIAN_POINT('Ctrl Pts',(-1.49713826486415,-2.71748934420412,
11.4899272993172));
#26988=CARTESIAN_POINT('Ctrl Pts',(-2.35440473165143,-2.02063101024426,
11.437163186414));
#26989=CARTESIAN_POINT('Ctrl Pts',(-2.72441254436296,-1.12293652192895,
11.3843990735107));
#26990=CARTESIAN_POINT('Ctrl Pts',(-2.86985849704456,-0.770062810659939,
11.363658088037));
#26991=CARTESIAN_POINT('Ctrl Pts',(-2.94001379842994,-0.386156125961379,
11.3429171025633));
#26992=CARTESIAN_POINT('Ctrl Pts',(-2.93811988821084,-0.00158572391977807,
11.3221761170896));
#26993=CARTESIAN_POINT('Ctrl Pts',(-2.9376139453736,-0.001087489077759,
11.1778238829104));
#26994=CARTESIAN_POINT('Ctrl Pts',(-2.93901878699851,-0.421914483298863,
11.2005105340074));
#26995=CARTESIAN_POINT('Ctrl Pts',(-2.85455180894317,-0.842203655580439,
11.2231971851044));
#26996=CARTESIAN_POINT('Ctrl Pts',(-2.68141846901601,-1.22208227989338,
11.2458838362014));
#26997=CARTESIAN_POINT('Ctrl Pts',(-2.27849338526037,-2.10615594578964,
11.2986814128972));
#26998=CARTESIAN_POINT('Ctrl Pts',(-1.39534184269282,-2.77136178018875,
11.351478989593));
#26999=CARTESIAN_POINT('Ctrl Pts',(-0.434393033296842,-2.91458278273799,
11.4042765662888));
#27000=CARTESIAN_POINT('Ctrl Pts',(0.526555776099161,-3.05780378528724,
11.4570741429846));
#27001=CARTESIAN_POINT('Ctrl Pts',(1.56530185232359,-2.6790399559866,11.5098717196804));
#27002=CARTESIAN_POINT('Ctrl Pts',(2.20851562057241,-1.95088412226283,11.5626692963761));
#27003=CARTESIAN_POINT('Ctrl Pts',(2.8517293888212,-1.22272828853909,11.6154668730719));
#27004=CARTESIAN_POINT('Ctrl Pts',(3.09941084909442,-0.145180450392246,
11.6682644497677));
#27005=CARTESIAN_POINT('Ctrl Pts',(2.83869800079219,0.790748863488276,11.7210620264635));
#27006=CARTESIAN_POINT('Ctrl Pts',(2.57798515248995,1.72667817736883,11.7738596031593));
#27007=CARTESIAN_POINT('Ctrl Pts',(1.80887799561223,2.52098896698305,11.8266571798551));
#27008=CARTESIAN_POINT('Ctrl Pts',(0.881838661257381,2.81173446120386,11.8794547565508));
#27009=CARTESIAN_POINT('Ctrl Pts',(-0.0452006730974654,3.10247995542467,
11.9322523332466));
#27010=CARTESIAN_POINT('Ctrl Pts',(-1.13017218492944,2.88966015425208,11.9850499099424));
#27011=CARTESIAN_POINT('Ctrl Pts',(-1.87868257050012,2.27025150679581,12.0378474866382));
#27012=CARTESIAN_POINT('Ctrl Pts',(-2.54016360114299,1.72286154613935,12.0845062853956));
#27013=CARTESIAN_POINT('Ctrl Pts',(-2.93887569608656,0.857934401938529,
12.131165084153));
#27014=CARTESIAN_POINT('Ctrl Pts',(-2.94523166487087,-0.00185944496279741,
12.1778238829104));
#27015=CARTESIAN_POINT('Origin',(0.,0.,0.));
#27016=CARTESIAN_POINT('',(-2.94174180320762,0.00264834375568943,13.3221761170896));
#27017=CARTESIAN_POINT('',(-2.94305001533088,0.00255625401320253,13.1778238829104));
#27018=CARTESIAN_POINT('',(-2.942,-3.60291088309151E-16,0.));
#27019=CARTESIAN_POINT('Ctrl Pts',(-2.94174180320762,0.00264834375568943,
13.3221761170896));
#27020=CARTESIAN_POINT('Ctrl Pts',(-2.94387102475549,0.238434505128271,
13.3094197907354));
#27021=CARTESIAN_POINT('Ctrl Pts',(-2.91788746839781,0.47375723479733,13.2966634643811));
#27022=CARTESIAN_POINT('Ctrl Pts',(-2.86198621303624,0.701744298554981,
13.2839071380269));
#27023=CARTESIAN_POINT('Ctrl Pts',(-2.63076132372094,1.64476933872116,13.2311430251236));
#27024=CARTESIAN_POINT('Ctrl Pts',(-1.88767285741819,2.4622880626259,13.1783789122204));
#27025=CARTESIAN_POINT('Ctrl Pts',(-0.970933785112477,2.78221094259426,
13.1256147993172));
#27026=CARTESIAN_POINT('Ctrl Pts',(-0.0541947128067906,3.10213382256261,
13.072850686414));
#27027=CARTESIAN_POINT('Ctrl Pts',(1.03619496550185,2.92446085859461,13.0200865735107));
#27028=CARTESIAN_POINT('Ctrl Pts',(1.80394988224929,2.33005900493893,12.9673224606075));
#27029=CARTESIAN_POINT('Ctrl Pts',(2.57170479899673,1.73565715128324,12.9145583477043));
#27030=CARTESIAN_POINT('Ctrl Pts',(3.01682495418297,0.724526407939868,12.8617942348011));
#27031=CARTESIAN_POINT('Ctrl Pts',(2.93671615215365,-0.243122162387507,
12.8090301218978));
#27032=CARTESIAN_POINT('Ctrl Pts',(2.85660735012433,-1.21077073271488,12.7562660089946));
#27033=CARTESIAN_POINT('Ctrl Pts',(2.25126959087945,-2.13493713002626,12.7035018960914));
#27034=CARTESIAN_POINT('Ctrl Pts',(1.39621930521764,-2.59499167549757,12.6507377831882));
#27035=CARTESIAN_POINT('Ctrl Pts',(0.541169019555798,-3.0550462209689,12.5979736702849));
#27036=CARTESIAN_POINT('Ctrl Pts',(-0.563593792522998,-3.05098891460014,
12.5452095573817));
#27037=CARTESIAN_POINT('Ctrl Pts',(-1.41524190404595,-2.58466641894008,
12.4924454444785));
#27038=CARTESIAN_POINT('Ctrl Pts',(-2.26689001556888,-2.11834392328004,
12.4396813315753));
#27039=CARTESIAN_POINT('Ctrl Pts',(-2.86542342653597,-1.18975623832874,
12.386917218672));
#27040=CARTESIAN_POINT('Ctrl Pts',(-2.93842267097986,-0.221545369700522,
12.3341531057688));
#27041=CARTESIAN_POINT('Ctrl Pts',(-2.94394606605647,-0.148286924552967,
12.3301607762091));
#27042=CARTESIAN_POINT('Ctrl Pts',(-2.94646077805926,-0.0748016366810879,
12.3261684466493));
#27043=CARTESIAN_POINT('Ctrl Pts',(-2.9460560275736,-0.00128820797444335,
12.3221761170896));
#27044=CARTESIAN_POINT('Ctrl Pts',(-2.94523166487087,-0.00185944496279741,
12.1778238829104));
#27045=CARTESIAN_POINT('Ctrl Pts',(-2.94606790330798,-0.11498030618232,
12.1839626608488));
#27046=CARTESIAN_POINT('Ctrl Pts',(-2.94011246232577,-0.228012310092633,
12.1901014387871));
#27047=CARTESIAN_POINT('Ctrl Pts',(-2.92707021611942,-0.34022059713689,
12.1962402167255));
#27048=CARTESIAN_POINT('Ctrl Pts',(-2.81489821685867,-1.30528655987343,
12.2490377934213));
#27049=CARTESIAN_POINT('Ctrl Pts',(-2.17850495902776,-2.20942099160657,
12.3018353701171));
#27050=CARTESIAN_POINT('Ctrl Pts',(-1.30787830109555,-2.64063334341081,
12.3546329468129));
#27051=CARTESIAN_POINT('Ctrl Pts',(-0.437251643163329,-3.07184569521506,
12.4074305235086));
#27052=CARTESIAN_POINT('Ctrl Pts',(0.667608414870202,-3.0301359670904,12.4602281002044));
#27053=CARTESIAN_POINT('Ctrl Pts',(1.50324587595541,-2.53451019750022,12.5130256769002));
#27054=CARTESIAN_POINT('Ctrl Pts',(2.3388833370406,-2.03888442791006,12.565823253596));
#27055=CARTESIAN_POINT('Ctrl Pts',(2.90529820117748,-1.0893426168544,12.6186208302918));
#27056=CARTESIAN_POINT('Ctrl Pts',(2.94438994414644,-0.118566275217254,
12.6714184069876));
#27057=CARTESIAN_POINT('Ctrl Pts',(2.9834816871154,0.852210066419907,12.7242159836833));
#27058=CARTESIAN_POINT('Ctrl Pts',(2.49525030891641,1.84422093863856,12.7770135603791));
#27059=CARTESIAN_POINT('Ctrl Pts',(1.70217015235411,2.40543278377184,12.8298111370749));
#27060=CARTESIAN_POINT('Ctrl Pts',(0.909089995791835,2.9666446289051,12.8826087137707));
#27061=CARTESIAN_POINT('Ctrl Pts',(-0.188838939133739,3.09705744695301,
12.9354062904664));
#27062=CARTESIAN_POINT('Ctrl Pts',(-1.09131898793251,2.7372455080587,12.9882038671622));
#27063=CARTESIAN_POINT('Ctrl Pts',(-1.99379903673132,2.37743356916437,13.041001443858));
#27064=CARTESIAN_POINT('Ctrl Pts',(-2.70083019940331,1.52739687332778,13.0937990205538));
#27065=CARTESIAN_POINT('Ctrl Pts',(-2.89023676115095,0.574475038014031,
13.1465965972496));
#27066=CARTESIAN_POINT('Ctrl Pts',(-2.92757845484148,0.386605542063277,
13.1570056924699));
#27067=CARTESIAN_POINT('Ctrl Pts',(-2.94480084734965,0.194737053204087,
13.1674147876901));
#27068=CARTESIAN_POINT('Ctrl Pts',(-2.94305001533088,0.00255625401320253,
13.1778238829104));
#27069=CARTESIAN_POINT('Origin',(0.,0.,0.));
#27070=CARTESIAN_POINT('',(-2.93751466932027,-0.000920155716999105,14.3221761170896));
#27071=CARTESIAN_POINT('',(-2.93723567126517,-0.000168200420414877,14.1778238829104));
#27072=CARTESIAN_POINT('',(-2.942,-3.60291088309151E-16,0.));
#27073=CARTESIAN_POINT('Ctrl Pts',(-2.93751466932027,-0.000920155716999105,
14.3221761170896));
#27074=CARTESIAN_POINT('Ctrl Pts',(-2.93597025204609,0.546430712607314,
14.2926711348214));
#27075=CARTESIAN_POINT('Ctrl Pts',(-2.78929401088964,1.09455044560389,14.2631661525532));
#27076=CARTESIAN_POINT('Ctrl Pts',(-2.50265848527962,1.55567048253069,14.2336611702849));
#27077=CARTESIAN_POINT('Ctrl Pts',(-1.99006474440319,2.38029696320978,14.1808970573817));
#27078=CARTESIAN_POINT('Ctrl Pts',(-1.02987285703515,2.92669322244838,14.1281329444785));
#27079=CARTESIAN_POINT('Ctrl Pts',(-0.0591093222587219,2.94616975617191,
14.0753688315753));
#27080=CARTESIAN_POINT('Ctrl Pts',(0.91165421251771,2.96564628989543,14.022604718672));
#27081=CARTESIAN_POINT('Ctrl Pts',(1.89298939470253,2.45820309810388,13.9698406057688));
#27082=CARTESIAN_POINT('Ctrl Pts',(2.43824646110908,1.6548003925117,13.9170764928656));
#27083=CARTESIAN_POINT('Ctrl Pts',(2.98350352751563,0.851397686919529,13.8643123799624));
#27084=CARTESIAN_POINT('Ctrl Pts',(3.09268247814392,-0.247964532473289,
13.8115482670591));
#27085=CARTESIAN_POINT('Ctrl Pts',(2.71609106377438,-1.14291709123984,13.7587841541559));
#27086=CARTESIAN_POINT('Ctrl Pts',(2.33949964940482,-2.03786965000643,13.7060200412527));
#27087=CARTESIAN_POINT('Ctrl Pts',(1.47713787003741,-2.72841254814676,13.6532559283495));
#27088=CARTESIAN_POINT('Ctrl Pts',(0.521505344074129,-2.90024866524679,
13.6004918154462));
#27089=CARTESIAN_POINT('Ctrl Pts',(-0.434127181889136,-3.07208478234682,
13.547727702543));
#27090=CARTESIAN_POINT('Ctrl Pts',(-1.48303045444825,-2.72521411840656,
13.4949635896398));
#27091=CARTESIAN_POINT('Ctrl Pts',(-2.14780143456386,-2.01751310822262,
13.4421994767365));
#27092=CARTESIAN_POINT('Ctrl Pts',(-2.65185644493049,-1.48090689240571,
13.4021916901876));
#27093=CARTESIAN_POINT('Ctrl Pts',(-2.93506390560319,-0.736850015994192,
13.3621839036386));
#27094=CARTESIAN_POINT('Ctrl Pts',(-2.94174180320762,0.00264834375568943,
13.3221761170896));
#27095=CARTESIAN_POINT('Ctrl Pts',(-2.94305001533088,0.00255625401320253,
13.1778238829104));
#27096=CARTESIAN_POINT('Ctrl Pts',(-2.93592018233154,-0.780052807971912,
13.2202123643859));
#27097=CARTESIAN_POINT('Ctrl Pts',(-2.61415254645348,-1.56784099153657,
13.2626008458614));
#27098=CARTESIAN_POINT('Ctrl Pts',(-2.05514306890902,-2.111842103739,13.3049893273369));
#27099=CARTESIAN_POINT('Ctrl Pts',(-1.35886085409615,-2.78943043538737,
13.3577869040327));
#27100=CARTESIAN_POINT('Ctrl Pts',(-0.294514463647097,-3.08880012389325,
13.4105844807285));
#27101=CARTESIAN_POINT('Ctrl Pts',(0.652901130166797,-2.87353618718061,
13.4633820574243));
#27102=CARTESIAN_POINT('Ctrl Pts',(1.60031672398072,-2.65827225046796,13.5161796341201));
#27103=CARTESIAN_POINT('Ctrl Pts',(2.43080152115949,-1.92837468853676,13.5689772108158));
#27104=CARTESIAN_POINT('Ctrl Pts',(2.76592519601784,-1.01643883969637,13.6217747875116));
#27105=CARTESIAN_POINT('Ctrl Pts',(3.10104887087618,-0.104502990856014,
13.6745723642074));
#27106=CARTESIAN_POINT('Ctrl Pts',(2.94081142341417,0.989471144893501,13.7273699409032));
#27107=CARTESIAN_POINT('Ctrl Pts',(2.35822889153647,1.7669880022038,13.780167517599));
#27108=CARTESIAN_POINT('Ctrl Pts',(1.77564635965879,2.54450485951408,13.8329650942947));
#27109=CARTESIAN_POINT('Ctrl Pts',(0.770718743365416,3.00556443838513,13.8857626709905));
#27110=CARTESIAN_POINT('Ctrl Pts',(-0.198634575296267,2.94007387837555,
13.9385602476863));
#27111=CARTESIAN_POINT('Ctrl Pts',(-1.16798789395799,2.87458331836597,13.9913578243821));
#27112=CARTESIAN_POINT('Ctrl Pts',(-2.10176691498804,2.28254261947571,14.0441554010779));
#27113=CARTESIAN_POINT('Ctrl Pts',(-2.57447282101243,1.43372933243287,14.0969529777737));
#27114=CARTESIAN_POINT('Ctrl Pts',(-2.81582325712524,1.00034896972683,14.1239099461526));
#27115=CARTESIAN_POINT('Ctrl Pts',(-2.9369793805535,0.500032141317613,14.1508669145315));
#27116=CARTESIAN_POINT('Ctrl Pts',(-2.93723567126517,-0.000168200420414877,
14.1778238829104));
#27117=CARTESIAN_POINT('Origin',(0.,0.,0.));
#27118=CARTESIAN_POINT('',(-2.94505309192038,-0.00193896756046696,15.3221761170896));
#27119=CARTESIAN_POINT('',(-2.94366018875525,-0.00243623744087094,15.1778238829104));
#27120=CARTESIAN_POINT('',(-2.942,-3.60291088309151E-16,0.));
#27121=CARTESIAN_POINT('Ctrl Pts',(-2.94505309192038,-0.00193896756046696,
15.3221761170896));
#27122=CARTESIAN_POINT('Ctrl Pts',(-2.9385470358389,0.850524388417163,15.2759224789074));
#27123=CARTESIAN_POINT('Ctrl Pts',(-2.547538609851,1.70819207565318,15.2296688407252));
#27124=CARTESIAN_POINT('Ctrl Pts',(-1.89595701623,2.25582737299276,15.183415202543));
#27125=CARTESIAN_POINT('Ctrl Pts',(-1.15266143727356,2.88054559612564,15.1306510896398));
#27126=CARTESIAN_POINT('Ctrl Pts',(-0.0702757065020065,3.101811187844,15.0778869767365));
#27127=CARTESIAN_POINT('Ctrl Pts',(0.858557765212819,2.81891622927623,15.0251228638333));
#27128=CARTESIAN_POINT('Ctrl Pts',(1.78739123692767,2.53602127070844,14.9723587509301));
#27129=CARTESIAN_POINT('Ctrl Pts',(2.56267244958579,1.74896576185448,14.9195946380269));
#27130=CARTESIAN_POINT('Ctrl Pts',(2.83153606576082,0.815974051442588,14.8668305251236));
#27131=CARTESIAN_POINT('Ctrl Pts',(3.10039968193584,-0.11701765896928,14.8140664122204));
#27132=CARTESIAN_POINT('Ctrl Pts',(2.86284570162781,-1.19594557093908,14.7613022993172));
#27133=CARTESIAN_POINT('Ctrl Pts',(2.22699562201281,-1.92974108203173,14.708538186414));
#27134=CARTESIAN_POINT('Ctrl Pts',(1.59114554239781,-2.66353659312438,14.6557740735107));
#27135=CARTESIAN_POINT('Ctrl Pts',(0.556999363475848,-3.05219970333988,
14.6030099606075));
#27136=CARTESIAN_POINT('Ctrl Pts',(-0.404756492565064,-2.91883235658634,
14.5502458477043));
#27137=CARTESIAN_POINT('Ctrl Pts',(-1.36651234860599,-2.78546500983279,
14.4974817348011));
#27138=CARTESIAN_POINT('Ctrl Pts',(-2.25587788176586,-2.13006720611019,
14.4447176218978));
#27139=CARTESIAN_POINT('Ctrl Pts',(-2.66806285115338,-1.25093995318909,
14.3919535089946));
#27140=CARTESIAN_POINT('Ctrl Pts',(-2.84975952946865,-0.86340883600752,
14.3686943783596));
#27141=CARTESIAN_POINT('Ctrl Pts',(-2.93873215194095,-0.432403395862752,
14.3454352477246));
#27142=CARTESIAN_POINT('Ctrl Pts',(-2.93751466932027,-0.000920155716999105,
14.3221761170896));
#27143=CARTESIAN_POINT('Ctrl Pts',(-2.93723567126517,-0.000168200420414877,
14.1778238829104));
#27144=CARTESIAN_POINT('Ctrl Pts',(-2.93748134829393,-0.479653909982754,
14.2036644912273));
#27145=CARTESIAN_POINT('Ctrl Pts',(-2.82663341825378,-0.959032581146549,
14.2295050995441));
#27146=CARTESIAN_POINT('Ctrl Pts',(-2.6040704337075,-1.37924156009726,14.255345707861));
#27147=CARTESIAN_POINT('Ctrl Pts',(-2.14932934935944,-2.23781329038918,
14.3081432845568));
#27148=CARTESIAN_POINT('Ctrl Pts',(-1.22821438964454,-2.84937087577762,
14.3609408612526));
#27149=CARTESIAN_POINT('Ctrl Pts',(-0.260453688517605,-2.9352434278857,
14.4137384379483));
#27150=CARTESIAN_POINT('Ctrl Pts',(0.707307012609348,-3.02111597999379,
14.4665360146441));
#27151=CARTESIAN_POINT('Ctrl Pts',(1.72171345514836,-2.58130349882152,14.5193335913399));
#27152=CARTESIAN_POINT('Ctrl Pts',(2.32052700242268,-1.81621709490922,14.5721311680357));
#27153=CARTESIAN_POINT('Ctrl Pts',(2.91934054969697,-1.05113069099694,14.6249287447315));
#27154=CARTESIAN_POINT('Ctrl Pts',(3.10256120170658,0.0392296356553336,
14.6777263214272));
#27155=CARTESIAN_POINT('Ctrl Pts',(2.78670007190605,0.958015038527095,14.730523898123));
#27156=CARTESIAN_POINT('Ctrl Pts',(2.4708389421055,1.87680044139888,14.7833214748188));
#27157=CARTESIAN_POINT('Ctrl Pts',(1.65589603049478,2.62401092049012,14.8361190515146));
#27158=CARTESIAN_POINT('Ctrl Pts',(0.713219629658999,2.85916209136071,14.8889166282104));
#27159=CARTESIAN_POINT('Ctrl Pts',(-0.229456771176758,3.09431326223129,
14.9417142049061));
#27160=CARTESIAN_POINT('Ctrl Pts',(-1.2998666612376,2.81740512488122,14.9945117816019));
#27161=CARTESIAN_POINT('Ctrl Pts',(-2.0102520891451,2.15461751661924,15.0473093582977));
#27162=CARTESIAN_POINT('Ctrl Pts',(-2.59560481564969,1.60848506746078,15.0908141998353));
#27163=CARTESIAN_POINT('Ctrl Pts',(-2.93651363712562,0.800354074714661,
15.1343190413728));
#27164=CARTESIAN_POINT('Ctrl Pts',(-2.94366018875525,-0.00243623744087094,
15.1778238829104));
#27165=CARTESIAN_POINT('Origin',(0.,0.,0.));
#27166=CARTESIAN_POINT('',(-2.94313738502513,0.00253302137586425,16.3221761170896));
#27167=CARTESIAN_POINT('',(-2.94471111638464,0.00210180365940244,16.1778238829104));
#27168=CARTESIAN_POINT('',(-2.942,-3.60291088309151E-16,0.));
#27169=CARTESIAN_POINT('Ctrl Pts',(-2.94313738502513,0.00253302137586425,
16.3221761170896));
#27170=CARTESIAN_POINT('Ctrl Pts',(-2.94485185925312,0.191543887392068,
16.3119379358966));
#27171=CARTESIAN_POINT('Ctrl Pts',(-2.9281926935312,0.380253813087586,16.3016997547037));
#27172=CARTESIAN_POINT('Ctrl Pts',(-2.89205921107313,0.565158123055661,
16.2914615735107));
#27173=CARTESIAN_POINT('Ctrl Pts',(-2.70583949957629,1.51809221394305,16.2386974606075));
#27174=CARTESIAN_POINT('Ctrl Pts',(-2.00237766161548,2.36994831590605,16.1859333477043));
#27175=CARTESIAN_POINT('Ctrl Pts',(-1.10185083601191,2.73300839513725,16.1331692348011));
#27176=CARTESIAN_POINT('Ctrl Pts',(-0.201324010408316,3.09606847436846,
16.0804051218978));
#27177=CARTESIAN_POINT('Ctrl Pts',(0.896267802838059,2.97033253086785,16.0276410089946));
#27178=CARTESIAN_POINT('Ctrl Pts',(1.69136123542551,2.41302865700962,15.9748768960914));
#27179=CARTESIAN_POINT('Ctrl Pts',(2.48645466801294,1.85572478315141,15.9221127831882));
#27180=CARTESIAN_POINT('Ctrl Pts',(2.97904971994149,0.866852978935614,15.8693486702849));
#27181=CARTESIAN_POINT('Ctrl Pts',(2.94494422784077,-0.103506742820716,
15.8165845573817));
#27182=CARTESIAN_POINT('Ctrl Pts',(2.91083873574005,-1.07386646457706,15.7638204444785));
#27183=CARTESIAN_POINT('Ctrl Pts',(2.35003269961009,-2.0257141038739,15.7110563315753));
#27184=CARTESIAN_POINT('Ctrl Pts',(1.51777416489894,-2.52582100099134,15.658292218672));
#27185=CARTESIAN_POINT('Ctrl Pts',(0.685515630187792,-3.02592789810876,
15.6055281057688));
#27186=CARTESIAN_POINT('Ctrl Pts',(-0.418195403104536,-3.07429405304675,
15.5527639928656));
#27187=CARTESIAN_POINT('Ctrl Pts',(-1.2910104219294,-2.64890585572412,15.4999998799623));
#27188=CARTESIAN_POINT('Ctrl Pts',(-2.16382544075429,-2.22351765840148,
15.4472357670591));
#27189=CARTESIAN_POINT('Ctrl Pts',(-2.80574444511171,-1.3243751088182,15.3944716541559));
#27190=CARTESIAN_POINT('Ctrl Pts',(-2.92460123371974,-0.360718406752851,
15.3417075412527));
#27191=CARTESIAN_POINT('Ctrl Pts',(-2.93926677200092,-0.241814434842101,
15.3351970665317));
#27192=CARTESIAN_POINT('Ctrl Pts',(-2.94596885801613,-0.121928255923654,
15.3286865918106));
#27193=CARTESIAN_POINT('Ctrl Pts',(-2.94505309192038,-0.00193896756046696,
15.3221761170896));
#27194=CARTESIAN_POINT('Ctrl Pts',(-2.94366018875525,-0.00243623744087094,
15.1778238829104));
#27195=CARTESIAN_POINT('Ctrl Pts',(-2.94518670877559,-0.173914111966714,
15.1871166180686));
#27196=CARTESIAN_POINT('Ctrl Pts',(-2.93148500754538,-0.345148312857129,
15.1964093532268));
#27197=CARTESIAN_POINT('Ctrl Pts',(-2.90168460531916,-0.513533403029899,
15.2057020883851));
#27198=CARTESIAN_POINT('Ctrl Pts',(-2.7323707278315,-1.47022963524309,15.2584996650808));
#27199=CARTESIAN_POINT('Ctrl Pts',(-2.04338200710198,-2.33495502049558,
15.3112972417766));
#27200=CARTESIAN_POINT('Ctrl Pts',(-1.14867268627487,-2.7136766875585,15.3640948184724));
#27201=CARTESIAN_POINT('Ctrl Pts',(-0.25396336544776,-3.09239835462142,
15.4168923951682));
#27202=CARTESIAN_POINT('Ctrl Pts',(0.846466555476943,-2.98511630349478,
15.469689971864));
#27203=CARTESIAN_POINT('Ctrl Pts',(1.65117977763893,-2.44071617499708,15.5224875485597));
#27204=CARTESIAN_POINT('Ctrl Pts',(2.45589299980093,-1.89631604649936,15.5752851252555));
#27205=CARTESIAN_POINT('Ctrl Pts',(2.9648895232002,-0.914797840630574,15.6280827019513));
#27206=CARTESIAN_POINT('Ctrl Pts',(2.94623286851971,0.0565861200307141,
15.6808802786471));
#27207=CARTESIAN_POINT('Ctrl Pts',(2.92757621383922,1.02797008069197,15.7336778553429));
#27208=CARTESIAN_POINT('Ctrl Pts',(2.38126638107898,1.98921979614572,15.7864754320387));
#27209=CARTESIAN_POINT('Ctrl Pts',(1.55624255416387,2.50231876814311,15.8392730087344));
#27210=CARTESIAN_POINT('Ctrl Pts',(0.731218727248764,3.01541774014049,15.8920705854302));
#27211=CARTESIAN_POINT('Ctrl Pts',(-0.372519093821215,3.08036596868152,
15.944868162126));
#27212=CARTESIAN_POINT('Ctrl Pts',(-1.25202628558859,2.66756823456797,15.9976657388218));
#27213=CARTESIAN_POINT('Ctrl Pts',(-2.13153347735599,2.2547705004544,16.0504633155176));
#27214=CARTESIAN_POINT('Ctrl Pts',(-2.78681003982076,1.36422680368623,16.1032608922133));
#27215=CARTESIAN_POINT('Ctrl Pts',(-2.91926348480717,0.401734749454156,
16.1560584689091));
#27216=CARTESIAN_POINT('Ctrl Pts',(-2.93746447209008,0.269474651268154,
16.1633136069095));
#27217=CARTESIAN_POINT('Ctrl Pts',(-2.94579316360478,0.135855976077432,
16.17056874491));
#27218=CARTESIAN_POINT('Ctrl Pts',(-2.94471111638464,0.00210180365940244,
16.1778238829104));
#27219=CARTESIAN_POINT('Origin',(0.,0.,0.));
#27220=CARTESIAN_POINT('',(-2.93725002901676,-0.0001812803941037,17.3221761170896));
#27221=CARTESIAN_POINT('',(-2.93741720373741,0.000771801339816214,17.1778238829104));
#27222=CARTESIAN_POINT('',(-2.942,-3.60291088309151E-16,0.));
#27223=CARTESIAN_POINT('Ctrl Pts',(-2.93725002901676,-0.0001812803941037,
17.3221761170896));
#27224=CARTESIAN_POINT('Ctrl Pts',(-2.93697279781615,0.500567342066419,
17.2951892799827));
#27225=CARTESIAN_POINT('Ctrl Pts',(-2.81551854411511,1.00144216616236,17.2682024428757));
#27226=CARTESIAN_POINT('Ctrl Pts',(-2.57365375306511,1.43517165229615,17.2412156057688));
#27227=CARTESIAN_POINT('Ctrl Pts',(-2.10076465191889,2.28319068784079,17.1884514928656));
#27228=CARTESIAN_POINT('Ctrl Pts',(-1.16757891458186,2.87453141365988,17.1356873799624));
#27229=CARTESIAN_POINT('Ctrl Pts',(-0.198832686731451,2.94004703408661,
17.0829232670591));
#27230=CARTESIAN_POINT('Ctrl Pts',(0.769913541118934,3.00556265451333,17.0301591541559));
#27231=CARTESIAN_POINT('Ctrl Pts',(1.7742202594827,2.54525316954771,16.9773950412527));
#27232=CARTESIAN_POINT('Ctrl Pts',(2.35698303829202,1.76862666853625,16.9246309283495));
#27233=CARTESIAN_POINT('Ctrl Pts',(2.93974581710134,0.992000167524792,16.8718668154462));
#27234=CARTESIAN_POINT('Ctrl Pts',(3.1009646563562,-0.10094334953251,16.819102702543));
#27235=CARTESIAN_POINT('Ctrl Pts',(2.76726124086461,-1.01275643457747,16.7663385896398));
#27236=CARTESIAN_POINT('Ctrl Pts',(2.43355782537301,-1.92456951962244,16.7135744767365));
#27237=CARTESIAN_POINT('Ctrl Pts',(1.60493215513494,-2.65525217265506,16.6608103638333));
#27238=CARTESIAN_POINT('Ctrl Pts',(0.658529223760488,-2.87223771613265,
16.6080462509301));
#27239=CARTESIAN_POINT('Ctrl Pts',(-0.28787370761399,-3.08922325961025,
16.5552821380269));
#27240=CARTESIAN_POINT('Ctrl Pts',(-1.35205390012486,-2.79251169353279,
16.5025180251236));
#27241=CARTESIAN_POINT('Ctrl Pts',(-2.04965520386386,-2.11714987058814,
16.4497539122204));
#27242=CARTESIAN_POINT('Ctrl Pts',(-2.61189616218738,-1.57283311471008,
16.4072279805101));
#27243=CARTESIAN_POINT('Ctrl Pts',(-2.93601604066088,-0.782554000353691,
16.3647020487999));
#27244=CARTESIAN_POINT('Ctrl Pts',(-2.94313738502513,0.00253302137586425,
16.3221761170896));
#27245=CARTESIAN_POINT('Ctrl Pts',(-2.94471111638464,0.00210180365940244,
16.1778238829104));
#27246=CARTESIAN_POINT('Ctrl Pts',(-2.93791881702584,-0.837508855329917,
16.2233663216058));
#27247=CARTESIAN_POINT('Ctrl Pts',(-2.56030500077532,-1.68245865812038,
16.2689087603011));
#27248=CARTESIAN_POINT('Ctrl Pts',(-1.9260357734749,-2.23021889165449,16.3144511989965));
#27249=CARTESIAN_POINT('Ctrl Pts',(-1.19072428964819,-2.86524006683513,
16.3672487756922));
#27250=CARTESIAN_POINT('Ctrl Pts',(-0.110470994486742,-3.10084200550047,
16.420046352388));
#27251=CARTESIAN_POINT('Ctrl Pts',(0.822480772671947,-2.82966702812486,
16.4728439290838));
#27252=CARTESIAN_POINT('Ctrl Pts',(1.75543253983062,-2.55849205074926,16.5256415057796));
#27253=CARTESIAN_POINT('Ctrl Pts',(2.54108277898654,-1.78054015733275,16.5784390824754));
#27254=CARTESIAN_POINT('Ctrl Pts',(2.82143111474126,-0.850303800757864,
16.6312366591711));
#27255=CARTESIAN_POINT('Ctrl Pts',(3.10177945049598,0.0799325558170201,
16.6840342358669));
#27256=CARTESIAN_POINT('Ctrl Pts',(2.8768258828495,1.16245337555027,16.7368318125627));
#27257=CARTESIAN_POINT('Ctrl Pts',(2.24907588729453,1.90398208157484,16.7896293892585));
#27258=CARTESIAN_POINT('Ctrl Pts',(1.62132589173955,2.64551078759941,16.8424269659543));
#27259=CARTESIAN_POINT('Ctrl Pts',(0.590779468276065,3.0460473799153,16.8952245426501));
#27260=CARTESIAN_POINT('Ctrl Pts',(-0.372970147291156,2.92307772968038,
16.9480221193458));
#27261=CARTESIAN_POINT('Ctrl Pts',(-1.33671976285836,2.80010807944546,17.0008196960416));
#27262=CARTESIAN_POINT('Ctrl Pts',(-2.23367257052931,2.15363218665976,17.0536172727374));
#27263=CARTESIAN_POINT('Ctrl Pts',(-2.65511055711324,1.27823234158675,17.1064148494332));
#27264=CARTESIAN_POINT('Ctrl Pts',(-2.84510967687048,0.883571192629371,
17.1302178605922));
#27265=CARTESIAN_POINT('Ctrl Pts',(-2.93845923718072,0.442380686112001,
17.1540208717513));
#27266=CARTESIAN_POINT('Ctrl Pts',(-2.93741720373741,0.000771801339816214,
17.1778238829104));
#27267=CARTESIAN_POINT('Origin',(0.,0.,0.));
#27268=CARTESIAN_POINT('',(-2.94374845943093,-0.00235935217182681,18.3221761170896));
#27269=CARTESIAN_POINT('',(-2.94191884508495,-0.00265442804262754,18.1778238829104));
#27270=CARTESIAN_POINT('',(-2.942,-3.60291088309151E-16,0.));
#27271=CARTESIAN_POINT('Ctrl Pts',(-2.94374845943093,-0.00235935217182681,
18.3221761170896));
#27272=CARTESIAN_POINT('Ctrl Pts',(-2.93663601505887,0.804593723390554,
18.2784406240687));
#27273=CARTESIAN_POINT('Ctrl Pts',(-2.59170604511532,1.61685233182154,18.2347051310478));
#27274=CARTESIAN_POINT('Ctrl Pts',(-2.00087556349472,2.16331231972268,18.1909696380269));
#27275=CARTESIAN_POINT('Ctrl Pts',(-1.28807586499836,2.82258181703745,18.1382055251236));
#27276=CARTESIAN_POINT('Ctrl Pts',(-0.21737042847422,3.09498407768528,18.0854414122204));
#27277=CARTESIAN_POINT('Ctrl Pts',(0.723848642366025,2.85648596639017,18.0326772993172));
#27278=CARTESIAN_POINT('Ctrl Pts',(1.66506771320627,2.61798785509506,17.979913186414));
#27279=CARTESIAN_POINT('Ctrl Pts',(2.47680041836259,1.86858937185697,17.9271490735107));
#27280=CARTESIAN_POINT('Ctrl Pts',(2.78962522811136,0.949401968316567,17.8743849606075));
#27281=CARTESIAN_POINT('Ctrl Pts',(3.10245003786014,0.0302145647761227,
17.8216208477043));
#27282=CARTESIAN_POINT('Ctrl Pts',(2.91636695220134,-1.05876175906663,17.7688567348011));
#27283=CARTESIAN_POINT('Ctrl Pts',(2.31605267190429,-1.82189879882254,17.7160926218978));
#27284=CARTESIAN_POINT('Ctrl Pts',(1.71573839160727,-2.58503583857842,17.6633285089946));
#27285=CARTESIAN_POINT('Ctrl Pts',(0.701192916672019,-3.02233359424745,
17.6105643960914));
#27286=CARTESIAN_POINT('Ctrl Pts',(-0.26580902510543,-2.93475092606069,
17.5578002831882));
#27287=CARTESIAN_POINT('Ctrl Pts',(-1.23281096688288,-2.84716825787392,
17.5050361702849));
#27288=CARTESIAN_POINT('Ctrl Pts',(-2.15226937550254,-2.23470516583136,
17.4522720573817));
#27289=CARTESIAN_POINT('Ctrl Pts',(-2.60570234733465,-1.376124947175,17.3995079444785));
#27290=CARTESIAN_POINT('Ctrl Pts',(-2.82722159833554,-0.956675858167516,
17.3737306686822));
#27291=CARTESIAN_POINT('Ctrl Pts',(-2.93751483459916,-0.478486140449837,
17.3479533928859));
#27292=CARTESIAN_POINT('Ctrl Pts',(-2.93725002901676,-0.0001812803941037,
17.3221761170896));
#27293=CARTESIAN_POINT('Ctrl Pts',(-2.93741720373741,0.000771801339816214,
17.1778238829104));
#27294=CARTESIAN_POINT('Ctrl Pts',(-2.93614789764997,-0.537154163806018,
17.2068184484471));
#27295=CARTESIAN_POINT('Ctrl Pts',(-2.79482226555546,-1.07570091009264,
17.2358130139838));
#27296=CARTESIAN_POINT('Ctrl Pts',(-2.51752135312617,-1.53152748460635,
17.2648075795205));
#27297=CARTESIAN_POINT('Ctrl Pts',(-2.01257099705827,-2.36156366836612,
17.3176051562163));
#27298=CARTESIAN_POINT('Ctrl Pts',(-1.05674711942554,-2.91731223852532,
17.3704027329121));
#27299=CARTESIAN_POINT('Ctrl Pts',(-0.0855940111972479,-2.94553288784212,
17.4232003096079));
#27300=CARTESIAN_POINT('Ctrl Pts',(0.885559097031044,-2.97375353715892,
17.4759978863037));
#27301=CARTESIAN_POINT('Ctrl Pts',(1.87204143585492,-2.47444626563332,17.5287954629994));
#27302=CARTESIAN_POINT('Ctrl Pts',(2.42433904935325,-1.6751326720045,17.5815930396952));
#27303=CARTESIAN_POINT('Ctrl Pts',(2.97663666285158,-0.875819078375684,
17.634390616391));
#27304=CARTESIAN_POINT('Ctrl Pts',(3.09474955102439,0.223500837356317,17.6871881930868));
#27305=CARTESIAN_POINT('Ctrl Pts',(2.72485599198232,1.12189607224172,17.7399857697826));
#27306=CARTESIAN_POINT('Ctrl Pts',(2.35496243294025,2.02029130712709,17.7927833464783));
#27307=CARTESIAN_POINT('Ctrl Pts',(1.49706242668327,2.71776186116588,17.8455809231741));
#27308=CARTESIAN_POINT('Ctrl Pts',(0.542080129465371,2.89648759437067,17.8983784998699));
#27309=CARTESIAN_POINT('Ctrl Pts',(-0.412902167752565,3.07521332757547,
17.9511760765657));
#27310=CARTESIAN_POINT('Ctrl Pts',(-1.46496675593142,2.73519423994629,18.0039736532615));
#27311=CARTESIAN_POINT('Ctrl Pts',(-2.13471789678605,2.03136999411808,18.0567712299573));
#27312=CARTESIAN_POINT('Ctrl Pts',(-2.64657947259283,1.49346783078479,18.097122114275));
#27313=CARTESIAN_POINT('Ctrl Pts',(-2.93513642830927,0.743071513225126,
18.1374729985927));
#27314=CARTESIAN_POINT('Ctrl Pts',(-2.94191884508495,-0.00265442804262754,
18.1778238829104));
#27315=CARTESIAN_POINT('Origin',(0.,0.,-1.84858989190501));
#27316=CARTESIAN_POINT('',(-2.37315955426761,-0.00190203722427915,18.651410108095));
#27317=CARTESIAN_POINT('',(-2.375045185697,0.00109621558353243,18.848589891905));
#27318=CARTESIAN_POINT('',(-2.37175,-1.78696459712734E-13,-1.84858989190501));
#27319=CARTESIAN_POINT('',(-2.34668236863849,0.343918483395781,19.62825));
#27320=CARTESIAN_POINT('Ctrl Pts',(-2.37315955426761,-0.00190203722427911,
18.651410108095));
#27321=CARTESIAN_POINT('Ctrl Pts',(-2.37434322924264,-0.13619766213342,
18.6604387279773));
#27322=CARTESIAN_POINT('Ctrl Pts',(-2.30301174794614,-1.05408217035119,
18.7222314607628));
#27323=CARTESIAN_POINT('Ctrl Pts',(-1.10630348664728,-2.57293846871273,
18.8367883064516));
#27324=CARTESIAN_POINT('Ctrl Pts',(1.55510431037697,-2.32895732784023,18.9950806451613));
#27325=CARTESIAN_POINT('Ctrl Pts',(2.799454735287,0.0339291128273711,19.153372983871));
#27326=CARTESIAN_POINT('Ctrl Pts',(1.49831225734699,2.36808646144409,19.3116653225806));
#27327=CARTESIAN_POINT('Ctrl Pts',(-1.17239605887113,2.54234418499522,19.4699576612903));
#27328=CARTESIAN_POINT('Ctrl Pts',(-2.23266420913401,1.1219063425307,19.5754858870968));
#27329=CARTESIAN_POINT('Ctrl Pts',(-2.34668236863853,0.34391848339548,19.62825));
#27330=CARTESIAN_POINT('',(-0.439445221993725,2.33068358199196,19.62825));
#27331=CARTESIAN_POINT('Origin',(0.,0.,19.62825));
#27332=CARTESIAN_POINT('Ctrl Pts',(-2.375045185697,0.0010962155835324,18.848589891905));
#27333=CARTESIAN_POINT('Ctrl Pts',(-2.3709070095079,-0.721840983553584,
18.8972862878202));
#27334=CARTESIAN_POINT('Ctrl Pts',(-1.63279314114456,-2.23594095261586,
18.9987802604312));
#27335=CARTESIAN_POINT('Ctrl Pts',(0.939403752255799,-2.63798173542721,
19.153071809738));
#27336=CARTESIAN_POINT('Ctrl Pts',(2.72681418428107,-0.648558891555657,
19.3114645398253));
#27337=CARTESIAN_POINT('Ctrl Pts',(2.02326260265721,1.93590572399224,19.4698572699127));
#27338=CARTESIAN_POINT('Ctrl Pts',(0.333728659905137,2.4764638032096,19.5754524233042));
#27339=CARTESIAN_POINT('Ctrl Pts',(-0.439445221994122,2.33068358199189,
19.62825));
#27340=CARTESIAN_POINT('Origin',(0.,0.,-1.84858989190501));
#27341=CARTESIAN_POINT('',(-2.36792071934755,-0.000146142683553414,17.651410108095));
#27342=CARTESIAN_POINT('',(-2.37168457540117,-0.00213991832454075,17.848589891905));
#27343=CARTESIAN_POINT('',(-2.37175,-1.78696459712734E-13,-1.84858989190501));
#27344=CARTESIAN_POINT('Ctrl Pts',(-2.36792071934755,-0.000146142683553653,
17.651410108095));
#27345=CARTESIAN_POINT('Ctrl Pts',(-2.36813419747129,-0.385740823797463,
17.6771873838913));
#27346=CARTESIAN_POINT('Ctrl Pts',(-2.09721693494845,-1.56033551046507,
17.7557287725908));
#27347=CARTESIAN_POINT('Ctrl Pts',(-0.252615203963521,-2.78904848883903,
17.8870342741935));
#27348=CARTESIAN_POINT('Ctrl Pts',(2.20107095869216,-1.73144044804223,18.0453266129032));
#27349=CARTESIAN_POINT('Ctrl Pts',(2.65111435612032,0.902257304582571,18.2036189516129));
#27350=CARTESIAN_POINT('Ctrl Pts',(0.687932462726838,2.71468339494958,18.3619112903226));
#27351=CARTESIAN_POINT('Ctrl Pts',(-1.75387752254126,2.09345318786399,18.51117500915));
#27352=CARTESIAN_POINT('Ctrl Pts',(-2.36742572016178,0.648638736727164,
18.6076746150741));
#27353=CARTESIAN_POINT('Ctrl Pts',(-2.37315955426761,-0.00190203722427911,
18.651410108095));
#27354=CARTESIAN_POINT('Ctrl Pts',(-2.37168457540117,-0.0021399183245409,
17.848589891905));
#27355=CARTESIAN_POINT('Ctrl Pts',(-2.37337117352649,-0.187581187441035,
17.8610365842831));
#27356=CARTESIAN_POINT('Ctrl Pts',(-2.26891520043147,-1.15776718319138,
17.9262808533569));
#27357=CARTESIAN_POINT('Ctrl Pts',(-0.936670484863442,-2.63980707365487,
18.0443226991266));
#27358=CARTESIAN_POINT('Ctrl Pts',(1.70458375322942,-2.22265690947637,18.2027154292139));
#27359=CARTESIAN_POINT('Ctrl Pts',(2.7924295091237,0.220067221674903,18.3611081593012));
#27360=CARTESIAN_POINT('Ctrl Pts',(1.33528471034559,2.46230981068379,18.5195008893886));
#27361=CARTESIAN_POINT('Ctrl Pts',(-1.33854848928615,2.46038562697746,18.6778936194759));
#27362=CARTESIAN_POINT('Ctrl Pts',(-2.34578650854474,0.906342840260155,
18.7875899536481));
#27363=CARTESIAN_POINT('Ctrl Pts',(-2.37539370037317,0.0619815458209781,
18.8444887111244));
#27364=CARTESIAN_POINT('Ctrl Pts',(-2.375045185697,0.0010962155835324,18.848589891905));
#27365=CARTESIAN_POINT('Origin',(0.,0.,-1.84858989190501));
#27366=CARTESIAN_POINT('',(-2.37266692485838,0.00204204400000237,16.651410108095));
#27367=CARTESIAN_POINT('',(-2.36805549047049,0.000622202524476756,16.848589891905));
#27368=CARTESIAN_POINT('',(-2.37175,-1.78696459712734E-13,-1.84858989190501));
#27369=CARTESIAN_POINT('Ctrl Pts',(-2.37266692485838,0.00204204400000234,
16.651410108095));
#27370=CARTESIAN_POINT('Ctrl Pts',(-2.36692591585228,-0.630870989238285,
16.6939360398053));
#27371=CARTESIAN_POINT('Ctrl Pts',(-1.78142766618931,-2.05845093397981,
16.7892260844188));
#27372=CARTESIAN_POINT('Ctrl Pts',(0.625834434246847,-2.72963661550809,
16.9372802419355));
#27373=CARTESIAN_POINT('Ctrl Pts',(2.62987209575649,-0.962474906809746,
17.0955725806452));
#27374=CARTESIAN_POINT('Ctrl Pts',(2.23996307264014,1.6808175336192,17.2538649193548));
#27375=CARTESIAN_POINT('Ctrl Pts',(-0.188960577202794,2.79407962162107,
17.4121572580645));
#27376=CARTESIAN_POINT('Ctrl Pts',(-2.07834764953227,1.59681365622726,17.5446723209779));
#27377=CARTESIAN_POINT('Ctrl Pts',(-2.36769722407223,0.403542010042759,
17.6244232709881));
#27378=CARTESIAN_POINT('Ctrl Pts',(-2.36792071934755,-0.000146142683553653,
17.651410108095));
#27379=CARTESIAN_POINT('Ctrl Pts',(-2.36805549047049,0.000622202524476895,
16.848589891905));
#27380=CARTESIAN_POINT('Ctrl Pts',(-2.36703221490523,-0.433037181511712,
16.8775844574417));
#27381=CARTESIAN_POINT('Ctrl Pts',(-2.04563496603972,-1.65777921929151,
16.9593765996742));
#27382=CARTESIAN_POINT('Ctrl Pts',(-0.0813612164248821,-2.79987490584551,
17.0939663186025));
#27383=CARTESIAN_POINT('Ctrl Pts',(2.3044540321531,-1.59229636617095,17.2523590486898));
#27384=CARTESIAN_POINT('Ctrl Pts',(2.59011097558326,1.0664174443023,17.4107517787772));
#27385=CARTESIAN_POINT('Ctrl Pts',(0.515273103550636,2.75325543193802,17.5691445088645));
#27386=CARTESIAN_POINT('Ctrl Pts',(-1.82920922018932,1.99553698989753,17.7150905465738));
#27387=CARTESIAN_POINT('Ctrl Pts',(-2.36621679940268,0.599041421309039,
17.8082390075873));
#27388=CARTESIAN_POINT('Ctrl Pts',(-2.37168457540117,-0.0021399183245409,
17.848589891905));
#27389=CARTESIAN_POINT('Origin',(0.,0.,-1.84858989190501));
#27390=CARTESIAN_POINT('',(-2.37421130889265,-0.00156313606789179,15.651410108095));
#27391=CARTESIAN_POINT('',(-2.37393561872375,0.00169440952702007,15.848589891905));
#27392=CARTESIAN_POINT('',(-2.37175,-1.78696459712734E-13,-1.84858989190501));
#27393=CARTESIAN_POINT('Ctrl Pts',(-2.37421130889265,-0.00156313606789185,
15.651410108095));
#27394=CARTESIAN_POINT('Ctrl Pts',(-2.37494957137993,-0.0982948133878638,
15.657920582816));
#27395=CARTESIAN_POINT('Ctrl Pts',(-2.32575783841749,-0.97823113259622,
15.7171951704403));
#27396=CARTESIAN_POINT('Ctrl Pts',(-1.22691420480089,-2.5173927084595,15.8292338709677));
#27397=CARTESIAN_POINT('Ctrl Pts',(1.44241955782089,-2.40041878462448,15.9875262096774));
#27398=CARTESIAN_POINT('Ctrl Pts',(2.7987333404768,-0.0983678276200387,
16.1458185483871));
#27399=CARTESIAN_POINT('Ctrl Pts',(1.60738835637255,2.29322636168875,16.3041108870968));
#27400=CARTESIAN_POINT('Ctrl Pts',(-1.0471460247291,2.59731972402479,16.4624032258064));
#27401=CARTESIAN_POINT('Ctrl Pts',(-2.29140475539041,1.09058640184897,16.5781696328059));
#27402=CARTESIAN_POINT('Ctrl Pts',(-2.37404908129966,0.154416796370487,
16.641171926902));
#27403=CARTESIAN_POINT('Ctrl Pts',(-2.37266692485838,0.00204204400000234,
16.651410108095));
#27404=CARTESIAN_POINT('Ctrl Pts',(-2.37393561872375,0.00169440952702,15.848589891905));
#27405=CARTESIAN_POINT('Ctrl Pts',(-2.36845987569029,-0.675173904700622,
15.8941323306004));
#27406=CARTESIAN_POINT('Ctrl Pts',(-1.71112283332055,-2.14603323350396,
15.9924723459915));
#27407=CARTESIAN_POINT('Ctrl Pts',(0.781808691918871,-2.68973858755105,
16.1436099380784));
#27408=CARTESIAN_POINT('Ctrl Pts',(2.68190993738254,-0.808255851442284,
16.3020026681657));
#27409=CARTESIAN_POINT('Ctrl Pts',(2.137857975385,1.80982921402577,16.4603953982531));
#27410=CARTESIAN_POINT('Ctrl Pts',(-0.354526606378597,2.77853009386107,
16.6187881283404));
#27411=CARTESIAN_POINT('Ctrl Pts',(-2.1267152976418,1.50123071247663,16.7481862928911));
#27412=CARTESIAN_POINT('Ctrl Pts',(-2.36889554581355,0.356633715936655,
16.824786880746));
#27413=CARTESIAN_POINT('Ctrl Pts',(-2.36805549047049,0.000622202524476895,
16.848589891905));
#27414=CARTESIAN_POINT('Origin',(0.,0.,-1.84858989190501));
#27415=CARTESIAN_POINT('',(-2.36813406422853,-0.000741801265089943,14.651410108095));
#27416=CARTESIAN_POINT('',(-2.3730883931612,-0.00196401976579913,14.848589891905));
#27417=CARTESIAN_POINT('',(-2.37175,-1.78696459712734E-13,-1.84858989190501));
#27418=CARTESIAN_POINT('Ctrl Pts',(-2.36813406422853,-0.000741801265090151,
14.651410108095));
#27419=CARTESIAN_POINT('Ctrl Pts',(-2.36911556130725,-0.348590331114078,
14.67466923873));
#27420=CARTESIAN_POINT('Ctrl Pts',(-2.13467349016726,-1.48428584342291,
14.7506924822682));
#27421=CARTESIAN_POINT('Ctrl Pts',(-0.384661101133316,-2.77391787153297,
14.8794798387097));
#27422=CARTESIAN_POINT('Ctrl Pts',(2.11642951734883,-1.833933100982,15.0377721774193));
#27423=CARTESIAN_POINT('Ctrl Pts',(2.69095567587589,0.775462488971503,15.196064516129));
#27424=CARTESIAN_POINT('Ctrl Pts',(0.815932002060255,2.67896239018596,15.3543568548387));
#27425=CARTESIAN_POINT('Ctrl Pts',(-1.69415942334001,2.16583952768063,15.5061387188274));
#27426=CARTESIAN_POINT('Ctrl Pts',(-2.36896632639394,0.68566662754189,15.6051564699128));
#27427=CARTESIAN_POINT('Ctrl Pts',(-2.37421130889265,-0.00156313606789185,
15.651410108095));
#27428=CARTESIAN_POINT('Ctrl Pts',(-2.3730883931612,-0.00196401976579899,
14.848589891905));
#27429=CARTESIAN_POINT('Ctrl Pts',(-2.3743190266956,-0.140204213139865,
14.8578826270632));
#27430=CARTESIAN_POINT('Ctrl Pts',(-2.30051483718045,-1.06255693428419,
14.9199729389172));
#27431=CARTESIAN_POINT('Ctrl Pts',(-1.09187025049414,-2.57948402526614,
15.034860827467));
#27432=CARTESIAN_POINT('Ctrl Pts',(1.56952811621541,-2.32002154590554,15.1932535575544));
#27433=CARTESIAN_POINT('Ctrl Pts',(2.80054018729513,0.0537879083119886,
15.3516462876417));
#27434=CARTESIAN_POINT('Ctrl Pts',(1.47928558581743,2.37857786000547,15.510039017729));
#27435=CARTESIAN_POINT('Ctrl Pts',(-1.19011296325406,2.53565565848489,15.6684317478164));
#27436=CARTESIAN_POINT('Ctrl Pts',(-2.31923158661152,1.00114407889721,15.7812820392084));
#27437=CARTESIAN_POINT('Ctrl Pts',(-2.37480793194414,0.109522913413036,
15.8413347539046));
#27438=CARTESIAN_POINT('Ctrl Pts',(-2.37393561872375,0.00169440952702,15.848589891905));
#27439=CARTESIAN_POINT('Origin',(0.,0.,-1.84858989190501));
#27440=CARTESIAN_POINT('',(-2.3715418496797,0.00213501335906034,13.651410108095));
#27441=CARTESIAN_POINT('',(-2.3679091445694,-0.000135598010815169,13.848589891905));
#27442=CARTESIAN_POINT('',(-2.37175,-1.78696459712734E-13,-1.84858989190501));
#27443=CARTESIAN_POINT('Ctrl Pts',(-2.3715418496797,0.00213501335906002,
13.651410108095));
#27444=CARTESIAN_POINT('Ctrl Pts',(-2.36615833382539,-0.594025841412108,
13.691417894644));
#27445=CARTESIAN_POINT('Ctrl Pts',(-1.83673527245257,-1.98495272027885,
13.7841897940962));
#27446=CARTESIAN_POINT('Ctrl Pts',(0.495613593829615,-2.7562568251976,13.9297258064516));
#27447=CARTESIAN_POINT('Ctrl Pts',(2.58124229901106,-1.08617342751133,14.0880181451613));
#27448=CARTESIAN_POINT('Ctrl Pts',(2.31719215337611,1.57264269469624,14.246310483871));
#27449=CARTESIAN_POINT('Ctrl Pts',(-0.0561746566308962,2.79989802113906,
14.4046028225806));
#27450=CARTESIAN_POINT('Ctrl Pts',(-2.03718260390642,1.67260737626565,14.5396360306553));
#27451=CARTESIAN_POINT('Ctrl Pts',(-2.36688900247802,0.440515650110908,
14.6219051258268));
#27452=CARTESIAN_POINT('Ctrl Pts',(-2.36813406422853,-0.000741801265090151,
14.651410108095));
#27453=CARTESIAN_POINT('Ctrl Pts',(-2.3679091445694,-0.000135598010815204,
13.848589891905));
#27454=CARTESIAN_POINT('Ctrl Pts',(-2.36810720184093,-0.386682243712472,
13.8744305002219));
#27455=CARTESIAN_POINT('Ctrl Pts',(-2.09616001129468,-1.5627590796402,13.9530686852345));
#27456=CARTESIAN_POINT('Ctrl Pts',(-0.247574124043378,-2.79009418007158,
14.084504446943));
#27457=CARTESIAN_POINT('Ctrl Pts',(2.20577578767506,-1.72640425598558,14.2428971770303));
#27458=CARTESIAN_POINT('Ctrl Pts',(2.64889636694473,0.910640718254001,14.4012899071176));
#27459=CARTESIAN_POINT('Ctrl Pts',(0.677950564144521,2.71777510348644,14.559682637205));
#27460=CARTESIAN_POINT('Ctrl Pts',(-1.75896225721554,2.08736146800612,14.7087826321341));
#27461=CARTESIAN_POINT('Ctrl Pts',(-2.36732706283238,0.645220862237953,
14.8050850503675));
#27462=CARTESIAN_POINT('Ctrl Pts',(-2.3730883931612,-0.00196401976579899,
14.848589891905));
#27463=CARTESIAN_POINT('Origin',(0.,0.,-1.84858989190501));
#27464=CARTESIAN_POINT('',(-2.37501984479867,-0.00103851368575368,12.651410108095));
#27465=CARTESIAN_POINT('',(-2.37259649009551,0.00206077343817647,12.848589891905));
#27466=CARTESIAN_POINT('',(-2.37175,-1.78696459712734E-13,-1.84858989190501));
#27467=CARTESIAN_POINT('Ctrl Pts',(-2.37501984479867,-0.00103851368575395,
12.651410108095));
#27468=CARTESIAN_POINT('Ctrl Pts',(-2.37534614220328,-0.0603027810327914,
12.6554024376547));
#27469=CARTESIAN_POINT('Ctrl Pts',(-2.3465255250126,-0.902503139782818,
12.7121588801177));
#27470=CARTESIAN_POINT('Ctrl Pts',(-1.3449778303753,-2.45634263828104,12.8216794354839));
#27471=CARTESIAN_POINT('Ctrl Pts',(1.3268996674641,-2.46615526545311,12.9799717741935));
#27472=CARTESIAN_POINT('Ctrl Pts',(2.79091377061401,-0.231051608597259,
13.1382641129033));
#27473=CARTESIAN_POINT('Ctrl Pts',(1.71438719543081,2.21437599900773,13.2965564516129));
#27474=CARTESIAN_POINT('Ctrl Pts',(-0.922728766019108,2.64407945137796,
13.4548487903226));
#27475=CARTESIAN_POINT('Ctrl Pts',(-2.26566734580998,1.16662759494473,13.5731333424833));
#27476=CARTESIAN_POINT('Ctrl Pts',(-2.37325836266616,0.192218571562817,
13.6386537817407));
#27477=CARTESIAN_POINT('Ctrl Pts',(-2.3715418496797,0.00213501335906002,
13.651410108095));
#27478=CARTESIAN_POINT('Ctrl Pts',(-2.37259649009551,0.00206077343817663,
12.848589891905));
#27479=CARTESIAN_POINT('Ctrl Pts',(-2.36684863781259,-0.628854604795339,
12.8909783733805));
#27480=CARTESIAN_POINT('Ctrl Pts',(-1.7843511132665,-2.05499140547376,12.9861644315518));
#27481=CARTESIAN_POINT('Ctrl Pts',(0.620614844457064,-2.73143839311951,
13.1341480664189));
#27482=CARTESIAN_POINT('Ctrl Pts',(2.62914881900703,-0.966175433387754,
13.2925407965062));
#27483=CARTESIAN_POINT('Ctrl Pts',(2.24161329961403,1.67960956640559,13.4509335265936));
#27484=CARTESIAN_POINT('Ctrl Pts',(-0.18881199672574,2.79468576238185,13.6093262566809));
#27485=CARTESIAN_POINT('Ctrl Pts',(-2.0787303718274,1.59642731960111,13.7418783784514));
#27486=CARTESIAN_POINT('Ctrl Pts',(-2.36770253087283,0.403110547644307,
13.8216329235261));
#27487=CARTESIAN_POINT('Ctrl Pts',(-2.3679091445694,-0.000135598010815204,
13.848589891905));
#27488=CARTESIAN_POINT('Origin',(0.,0.,-1.84858989190501));
#27489=CARTESIAN_POINT('',(-2.36862197310131,-0.00127836189895874,11.651410108095));
#27490=CARTESIAN_POINT('',(-2.37435526891825,-0.00149902739337487,11.848589891905));
#27491=CARTESIAN_POINT('',(-2.37175,-1.78696459712734E-13,-1.84858989190501));
#27492=CARTESIAN_POINT('Ctrl Pts',(-2.36862197310131,-0.00127836189895824,
11.651410108095));
#27493=CARTESIAN_POINT('Ctrl Pts',(-2.37014878532502,-0.31130720317775,
11.6721510935687));
#27494=CARTESIAN_POINT('Ctrl Pts',(-2.16971320797384,-1.40813889625016,
11.7456561919456));
#27495=CARTESIAN_POINT('Ctrl Pts',(-0.515844982015253,-2.75254218412146,
11.8719254032258));
#27496=CARTESIAN_POINT('Ctrl Pts',(2.02702915825758,-1.93228810284904,12.0302177419355));
#27497=CARTESIAN_POINT('Ctrl Pts',(2.72471908433383,0.646908364689661,12.1885100806452));
#27498=CARTESIAN_POINT('Ctrl Pts',(0.942124687882267,2.63723066744667,12.3468024193548));
#27499=CARTESIAN_POINT('Ctrl Pts',(-1.6314871656873,2.2372573077083,12.5011024285048));
#27500=CARTESIAN_POINT('Ctrl Pts',(-2.37103367429718,0.72295582691495,12.6026383247515));
#27501=CARTESIAN_POINT('Ctrl Pts',(-2.37501984479867,-0.00103851368575395,
12.651410108095));
#27502=CARTESIAN_POINT('Ctrl Pts',(-2.37435526891825,-0.00149902739337513,
11.848589891905));
#27503=CARTESIAN_POINT('Ctrl Pts',(-2.3750294186508,-0.09269358979894,11.8547286698434));
#27504=CARTESIAN_POINT('Ctrl Pts',(-2.32893572485017,-0.967534360360412,
11.9136650244775));
#27505=CARTESIAN_POINT('Ctrl Pts',(-1.24320306842743,-2.51005271084502,
12.0253989558075));
#27506=CARTESIAN_POINT('Ctrl Pts',(1.42890961951376,-2.40917740729671,12.1837916858948));
#27507=CARTESIAN_POINT('Ctrl Pts',(2.79878839655315,-0.112703113920128,
12.3421844159822));
#27508=CARTESIAN_POINT('Ctrl Pts',(1.61799699147824,2.28648293589416,12.5005771460695));
#27509=CARTESIAN_POINT('Ctrl Pts',(-1.03735272104025,2.60188735588576,12.6589698761568));
#27510=CARTESIAN_POINT('Ctrl Pts',(-2.28969978642726,1.09623807519608,12.7749741247687));
#27511=CARTESIAN_POINT('Ctrl Pts',(-2.37400795707056,0.156991028530352,
12.8381807966847));
#27512=CARTESIAN_POINT('Ctrl Pts',(-2.37259649009551,0.00206077343817663,
12.848589891905));
#27513=CARTESIAN_POINT('Origin',(0.,0.,-1.84858989190501));
#27514=CARTESIAN_POINT('',(-2.3704600388318,0.00204051513951079,10.651410108095));
#27515=CARTESIAN_POINT('',(-2.36821409753223,-0.000876700279052733,10.848589891905));
#27516=CARTESIAN_POINT('',(-2.37175,-1.78696459712734E-13,-1.84858989190501));
#27517=CARTESIAN_POINT('Ctrl Pts',(-2.3704600388318,0.00204051513951101,
10.651410108095));
#27518=CARTESIAN_POINT('Ctrl Pts',(-2.36581720590312,-0.557246380947459,
10.6888997494827));
#27519=CARTESIAN_POINT('Ctrl Pts',(-1.88917186759772,-1.91081278379687,
10.7791535037736));
#27520=CARTESIAN_POINT('Ctrl Pts',(0.364276246834986,-2.77666838798409,
10.9221713709677));
#27521=CARTESIAN_POINT('Ctrl Pts',(2.52679819661009,-1.20742510924963,11.0804637096774));
#27522=CARTESIAN_POINT('Ctrl Pts',(2.38920121328945,1.46092507790601,11.2387560483871));
#27523=CARTESIAN_POINT('Ctrl Pts',(0.0767384440762257,2.79940988996594,
11.3970483870968));
#27524=CARTESIAN_POINT('Ctrl Pts',(-1.99342445870054,1.74813839309205,11.5345997403327));
#27525=CARTESIAN_POINT('Ctrl Pts',(-2.36626464526543,0.477391906863246,
11.6193869806655));
#27526=CARTESIAN_POINT('Ctrl Pts',(-2.36862197310131,-0.00127836189895824,
11.651410108095));
#27527=CARTESIAN_POINT('Ctrl Pts',(-2.36821409753223,-0.000876700279052144,
10.848589891905));
#27528=CARTESIAN_POINT('Ctrl Pts',(-2.36934663768308,-0.34013449210219,
10.871276543002));
#27529=CARTESIAN_POINT('Ctrl Pts',(-2.14277840224568,-1.46748838032652,
10.9467607707948));
#27530=CARTESIAN_POINT('Ctrl Pts',(-0.412912081686591,-2.77045521410563,
11.0750425752834));
#27531=CARTESIAN_POINT('Ctrl Pts',(2.09930342438264,-1.85441193183801,11.2334353053708));
#27532=CARTESIAN_POINT('Ctrl Pts',(2.69832297238025,0.751645938785551,11.3918280354581));
#27533=CARTESIAN_POINT('Ctrl Pts',(0.838231300737091,2.67269279323914,11.5502207655454));
#27534=CARTESIAN_POINT('Ctrl Pts',(-1.68408275985356,2.17793475487982,11.7024747176944));
#27535=CARTESIAN_POINT('Ctrl Pts',(-2.3692312821868,0.691640352752269,11.8019310931476));
#27536=CARTESIAN_POINT('Ctrl Pts',(-2.37435526891825,-0.00149902739337513,
11.848589891905));
#27537=CARTESIAN_POINT('Origin',(0.,0.,-1.84858989190501));
#27538=CARTESIAN_POINT('',(-2.37550470632433,-0.000400580813136427,9.65141010809499));
#27539=CARTESIAN_POINT('',(-2.371188773444,0.00213200020334231,9.84858989190502));
#27540=CARTESIAN_POINT('',(-2.37175,-1.78696459712734E-13,-1.84858989190501));
#27541=CARTESIAN_POINT('Ctrl Pts',(-2.37550470632433,-0.000400580813136008,
9.65141010809499));
#27542=CARTESIAN_POINT('Ctrl Pts',(-2.3755561297693,-0.022272253864447,
9.65288429249344));
#27543=CARTESIAN_POINT('Ctrl Pts',(-2.36539776597002,-0.826927449365476,
9.70712258979511));
#27544=CARTESIAN_POINT('Ctrl Pts',(-1.46001177080394,-2.38975943348956,
9.81412499999998));
#27545=CARTESIAN_POINT('Ctrl Pts',(1.20839081375242,-2.52633651006299,9.97241733870969));
#27546=CARTESIAN_POINT('Ctrl Pts',(2.77680741881119,-0.363214922151578,
10.1307096774193));
#27547=CARTESIAN_POINT('Ctrl Pts',(1.81752421541791,2.13053754888476,10.2890020161291));
#27548=CARTESIAN_POINT('Ctrl Pts',(-0.796232964112916,2.68488316090261,
10.4472943548387));
#27549=CARTESIAN_POINT('Ctrl Pts',(-2.23781112805667,1.24275389167182,10.5680970521607));
#27550=CARTESIAN_POINT('Ctrl Pts',(-2.37235167654013,0.229911773627901,
10.6361356365795));
#27551=CARTESIAN_POINT('Ctrl Pts',(-2.3704600388318,0.00204051513951101,
10.651410108095));
#27552=CARTESIAN_POINT('Ctrl Pts',(-2.371188773444,0.00213200020334229,
9.84858989190502));
#27553=CARTESIAN_POINT('Ctrl Pts',(-2.36599120092886,-0.582728163373476,
9.88782441616068));
#27554=CARTESIAN_POINT('Ctrl Pts',(-1.85298786413136,-1.96277949353793,
9.97985651711213));
#27555=CARTESIAN_POINT('Ctrl Pts',(0.457228155062243,-2.76348708967243,
10.1246861947593));
#27556=CARTESIAN_POINT('Ctrl Pts',(2.56709800604834,-1.12068118031423,10.2830789248467));
#27557=CARTESIAN_POINT('Ctrl Pts',(2.33744824681434,1.54345527114731,10.441471654934));
#27558=CARTESIAN_POINT('Ctrl Pts',(-0.0224302759543461,2.80096686222604,
10.5998643850214));
#27559=CARTESIAN_POINT('Ctrl Pts',(-2.02678859651666,1.69132688976849,10.7355704640117));
#27560=CARTESIAN_POINT('Ctrl Pts',(-2.36671093022588,0.44940421975213,10.8184789663063));
#27561=CARTESIAN_POINT('Ctrl Pts',(-2.36821409753223,-0.000876700279052144,
10.848589891905));
#27562=CARTESIAN_POINT('Origin',(0.,0.,-1.84858989190501));
#27563=CARTESIAN_POINT('',(-2.36935474920583,-0.00171244552815533,8.65141010809499));
#27564=CARTESIAN_POINT('',(-2.37526986480305,-0.00079584354989698,8.84858989190502));
#27565=CARTESIAN_POINT('',(-2.37175,-1.78696459712734E-13,-1.84858989190501));
#27566=CARTESIAN_POINT('Ctrl Pts',(-2.36935474920583,-0.00171244552815496,
8.65141010809499));
#27567=CARTESIAN_POINT('Ctrl Pts',(-2.37118720028221,-0.27388934122613,
8.66963294840741));
#27568=CARTESIAN_POINT('Ctrl Pts',(-2.2024097115759,-1.33194990712133,8.74061990162306));
#27569=CARTESIAN_POINT('Ctrl Pts',(-0.645866875421753,-2.72496614659181,
8.86437096774193));
#27570=CARTESIAN_POINT('Ctrl Pts',(1.93306273270264,-2.02629045111372,9.02266330645161));
#27571=CARTESIAN_POINT('Ctrl Pts',(2.75234481681179,0.516897020892659,9.18095564516129));
#27572=CARTESIAN_POINT('Ctrl Pts',(1.06619515253284,2.58955834411081,9.33924798387097));
#27573=CARTESIAN_POINT('Ctrl Pts',(-1.56575926891701,2.3076211823316,9.49606613818219));
#27574=CARTESIAN_POINT('Ctrl Pts',(-2.37371557816729,0.760560224541533,
9.60012017959021));
#27575=CARTESIAN_POINT('Ctrl Pts',(-2.37550470632433,-0.000400580813136008,
9.65141010809499));
#27576=CARTESIAN_POINT('Ctrl Pts',(-2.37526986480305,-0.000795843549896919,
8.84858989190502));
#27577=CARTESIAN_POINT('Ctrl Pts',(-2.37546378554503,-0.0450917311895661,
8.85157471262355));
#27578=CARTESIAN_POINT('Ctrl Pts',(-2.35430174920285,-0.872735026693859,
8.90735711003785));
#27579=CARTESIAN_POINT('Ctrl Pts',(-1.39014322226223,-2.43175251663614,
9.01593708414793));
#27580=CARTESIAN_POINT('Ctrl Pts',(1.2832422936176,-2.48982081613093,9.17432981423527));
#27581=CARTESIAN_POINT('Ctrl Pts',(2.78714752338885,-0.278795917178183,
9.33272254432263));
#27582=CARTESIAN_POINT('Ctrl Pts',(1.75099145741626,2.18630908076216,9.49111527440996));
#27583=CARTESIAN_POINT('Ctrl Pts',(-0.880927155331511,2.6589256904937,9.64950800449731));
#27584=CARTESIAN_POINT('Ctrl Pts',(-2.25694217263034,1.19150479465494,9.76866621032899));
#27585=CARTESIAN_POINT('Ctrl Pts',(-2.37298553152687,0.2043133499004,9.83502683946489));
#27586=CARTESIAN_POINT('Ctrl Pts',(-2.371188773444,0.00213200020334229,
9.84858989190502));
#27587=CARTESIAN_POINT('Origin',(0.,0.,-1.84858989190501));
#27588=CARTESIAN_POINT('',(-2.36950128627827,0.0017735229177115,7.65141010809498));
#27589=CARTESIAN_POINT('',(-2.36894127455122,-0.00150910447186903,7.84858989190502));
#27590=CARTESIAN_POINT('',(-2.37175,-1.78696459712734E-13,-1.84858989190501));
#27591=CARTESIAN_POINT('Ctrl Pts',(-2.36950128627827,0.00177352291771137,
7.65141010809498));
#27592=CARTESIAN_POINT('Ctrl Pts',(-2.36584417946481,-0.520480430603125,
7.68638160432139));
#27593=CARTESIAN_POINT('Ctrl Pts',(-1.93879965313242,-1.83613375809405,
7.77411721345102));
#27594=CARTESIAN_POINT('Ctrl Pts',(0.23211833466387,-2.79082525421268,7.91461693548387));
#27595=CARTESIAN_POINT('Ctrl Pts',(2.4666622528453,-1.32595695677747,8.07290927419355));
#27596=CARTESIAN_POINT('Ctrl Pts',(2.45582838148514,1.34591659530986,8.23120161290321));
#27597=CARTESIAN_POINT('Ctrl Pts',(0.209478684497901,2.79261583494391,8.38949395161291));
#27598=CARTESIAN_POINT('Ctrl Pts',(-1.94700227603872,1.8233279802371,8.52956345001015));
#27599=CARTESIAN_POINT('Ctrl Pts',(-2.36588135038034,0.51419704970092,8.61686883550418));
#27600=CARTESIAN_POINT('Ctrl Pts',(-2.36935474920583,-0.00171244552815496,
8.65141010809499));
#27601=CARTESIAN_POINT('Ctrl Pts',(-2.36894127455122,-0.0015091044718692,
7.84858989190502));
#27602=CARTESIAN_POINT('Ctrl Pts',(-2.37065112362024,-0.29337775612239,
7.86812258578219));
#27603=CARTESIAN_POINT('Ctrl Pts',(-2.18563237695357,-1.37208652926944,
7.94045285635514));
#27604=CARTESIAN_POINT('Ctrl Pts',(-0.576791078891976,-2.74102727674834,
8.06558070362385));
#27605=CARTESIAN_POINT('Ctrl Pts',(1.9854134998704,-1.97586733236324,8.22397343371122));
#27606=CARTESIAN_POINT('Ctrl Pts',(2.73821547444757,0.589995335628766,8.38236616379854));
#27607=CARTESIAN_POINT('Ctrl Pts',(0.995550277773485,2.61816693986326,8.54075889388591));
#27608=CARTESIAN_POINT('Ctrl Pts',(-1.60447071736692,2.26702158872423,8.69616680325471));
#27609=CARTESIAN_POINT('Ctrl Pts',(-2.37203358111632,0.738444616722348,
8.79877713592776));
#27610=CARTESIAN_POINT('Ctrl Pts',(-2.37526986480305,-0.000795843549896919,
8.84858989190502));
#27611=CARTESIAN_POINT('Origin',(0.,0.,-1.84858989190501));
#27612=CARTESIAN_POINT('',(-2.37554636470555,0.000284697057196372,6.65141010809498));
#27613=CARTESIAN_POINT('',(-2.36989007687564,0.00191473874719905,6.84858989190502));
#27614=CARTESIAN_POINT('',(-2.37175,-1.78696459712734E-13,-1.84858989190501));
#27615=CARTESIAN_POINT('Ctrl Pts',(-2.37554636470555,0.000284697057196357,
6.65141010809498));
#27616=CARTESIAN_POINT('Ctrl Pts',(-2.37423866256909,-0.767022922389114,
6.70313026023536));
#27617=CARTESIAN_POINT('Ctrl Pts',(-1.55422096328597,-2.31952782580344,
6.80761452527896));
#27618=CARTESIAN_POINT('Ctrl Pts',(1.087159950493,-2.58082695330052,6.96486290322581));
#27619=CARTESIAN_POINT('Ctrl Pts',(2.75644605727123,-0.494560061258782,
7.12315524193547));
#27620=CARTESIAN_POINT('Ctrl Pts',(1.91656709780378,2.04189987033018,7.28144758064516));
#27621=CARTESIAN_POINT('Ctrl Pts',(-0.667943575474826,2.7196389283911,7.43973991935484));
#27622=CARTESIAN_POINT('Ctrl Pts',(-2.20776674506755,1.31893238938929,7.56306076183811));
#27623=CARTESIAN_POINT('Ctrl Pts',(-2.37136193013682,0.267483183802526,
7.63361749141816));
#27624=CARTESIAN_POINT('Ctrl Pts',(-2.36950128627827,0.00177352291771137,
7.65141010809498));
#27625=CARTESIAN_POINT('Ctrl Pts',(-2.36989007687564,0.00191473874719891,
6.84858989190502));
#27626=CARTESIAN_POINT('Ctrl Pts',(-2.36577478375809,-0.53667818893527,
6.88467045894083));
#27627=CARTESIAN_POINT('Ctrl Pts',(-1.91714943575642,-1.86961076393625,
6.97354860267242));
#27628=CARTESIAN_POINT('Ctrl Pts',(0.292225921295444,-2.78577143561543,
7.11522432309981));
#27629=CARTESIAN_POINT('Ctrl Pts',(2.49597675267592,-1.27122717508287,7.27361705318714));
#27630=CARTESIAN_POINT('Ctrl Pts',(2.42502418520658,1.40184741742138,7.43200978327449));
#27631=CARTESIAN_POINT('Ctrl Pts',(0.144030698698804,2.79735118252968,7.59040251336184));
#27632=CARTESIAN_POINT('Ctrl Pts',(-1.9707500505419,1.78578599745412,7.729262549572));
#27633=CARTESIAN_POINT('Ctrl Pts',(-2.36602933985975,0.495553745979654,
7.8153250090864));
#27634=CARTESIAN_POINT('Ctrl Pts',(-2.36894127455122,-0.0015091044718692,
7.84858989190502));
#27635=CARTESIAN_POINT('Origin',(0.,0.,-1.84858989190501));
#27636=CARTESIAN_POINT('',(-2.37028552428411,-0.00200651108796764,5.65141010809498));
#27637=CARTESIAN_POINT('',(-2.3755997202681,4.64207010002296E-5,5.84858989190501));
#27638=CARTESIAN_POINT('',(-2.37175,-1.78696459712734E-13,-1.84858989190501));
#27639=CARTESIAN_POINT('Ctrl Pts',(-2.37028552428411,-0.00200651108796798,
5.65141010809498));
#27640=CARTESIAN_POINT('Ctrl Pts',(-2.37218747443614,-0.236339757801373,
5.66711480324611));
#27641=CARTESIAN_POINT('Ctrl Pts',(-2.23283499221027,-1.25576625306762,
5.73558361130047));
#27642=CARTESIAN_POINT('Ctrl Pts',(-0.774433895304387,-2.6912518764775,
5.85681653225807));
#27643=CARTESIAN_POINT('Ctrl Pts',(1.83474190859146,-2.11572839695838,6.01510887096773));
#27644=CARTESIAN_POINT('Ctrl Pts',(2.77377064377508,0.385721319828002,6.17340120967742));
#27645=CARTESIAN_POINT('Ctrl Pts',(1.18786391621721,2.53605280650616,6.3316935483871));
#27646=CARTESIAN_POINT('Ctrl Pts',(-1.47934336288373,2.37784098196877,6.48998588709676));
#27647=CARTESIAN_POINT('Ctrl Pts',(-2.36843670110272,0.814031196077336,
6.59655807366607));
#27648=CARTESIAN_POINT('Ctrl Pts',(-2.37557276040749,0.0157726454599615,
6.65036614733214));
#27649=CARTESIAN_POINT('Ctrl Pts',(-2.37554636470555,0.000284697057196357,
6.65141010809498));
#27650=CARTESIAN_POINT('Ctrl Pts',(-2.37559927670797,4.64153524631309E-5,
5.84858989190501));
#27651=CARTESIAN_POINT('Ctrl Pts',(-2.37537320011125,-0.780689829870116,
5.90121833209947));
#27652=CARTESIAN_POINT('Ctrl Pts',(-1.52932552826367,-2.34509161690763,
6.00664434898972));
#27653=CARTESIAN_POINT('Ctrl Pts',(1.13304083122442,-2.56166683144901,6.16486794257572));
#27654=CARTESIAN_POINT('Ctrl Pts',(2.76565869916243,-0.443903638546721,
6.32326067266308));
#27655=CARTESIAN_POINT('Ctrl Pts',(1.87779906814186,2.07841024349223,6.48165340275042));
#27656=CARTESIAN_POINT('Ctrl Pts',(-0.721388970917745,2.70656912588725,
6.64004613283776));
#27657=CARTESIAN_POINT('Ctrl Pts',(-2.22082549341992,1.28688950604137,6.7623582958893));
#27658=CARTESIAN_POINT('Ctrl Pts',(-2.37179679288516,0.251458022419059,
6.83187288224505));
#27659=CARTESIAN_POINT('Ctrl Pts',(-2.36989007687564,0.00191473874719891,
6.84858989190502));
#27660=CARTESIAN_POINT('Origin',(0.,0.,-1.84858989190501));
#27661=CARTESIAN_POINT('',(-2.36873091192997,0.00136091434597342,4.65141010809498));
#27662=CARTESIAN_POINT('',(-2.37001948420046,-0.00195088435344298,4.84858989190502));
#27663=CARTESIAN_POINT('',(-2.37175,-1.78696459712734E-13,-1.84858989190501));
#27664=CARTESIAN_POINT('Ctrl Pts',(-2.36873091192997,0.00136091434597342,
4.65141010809498));
#27665=CARTESIAN_POINT('Ctrl Pts',(-2.36618048682385,-0.483684235607871,
4.6838634591601));
#27666=CARTESIAN_POINT('Ctrl Pts',(-1.98568385961058,-1.76101097954328,
4.76908092312844));
#27667=CARTESIAN_POINT('Ctrl Pts',(0.099437554957728,-2.79869553427603,
4.9070625));
#27668=CARTESIAN_POINT('Ctrl Pts',(2.40096992936847,-1.44150196638533,5.06535483870968));
#27669=CARTESIAN_POINT('Ctrl Pts',(2.51692357424149,1.22787631390688,5.22364717741935));
#27670=CARTESIAN_POINT('Ctrl Pts',(0.341747055246021,2.77953116030023,5.38193951612902));
#27671=CARTESIAN_POINT('Ctrl Pts',(-1.8978479262878,1.89808937168119,5.52452715968758));
#27672=CARTESIAN_POINT('Ctrl Pts',(-2.36579736551696,0.550965297634364,
5.61435069034289));
#27673=CARTESIAN_POINT('Ctrl Pts',(-2.37028552428411,-0.00200651108796798,
5.65141010809498));
#27674=CARTESIAN_POINT('Ctrl Pts',(-2.37001948420046,-0.00195088435344316,
4.84858989190502));
#27675=CARTESIAN_POINT('Ctrl Pts',(-2.37193026582578,-0.24641085904258,
4.86496862856234));
#27676=CARTESIAN_POINT('Ctrl Pts',(-2.22486407851201,-1.27665550423204,
4.93414494191544));
#27677=CARTESIAN_POINT('Ctrl Pts',(-0.738632074782922,-2.7019143470289,
5.05611883196433));
#27678=CARTESIAN_POINT('Ctrl Pts',(1.86450842642192,-2.09034131384488,5.21451156205166));
#27679=CARTESIAN_POINT('Ctrl Pts',(2.76843291921558,0.426260075974678,5.37290429213902));
#27680=CARTESIAN_POINT('Ctrl Pts',(1.14935163317956,2.55439020196149,5.53129702222635));
#27681=CARTESIAN_POINT('Ctrl Pts',(-1.51718895457673,2.35458194945041,5.68968975231371));
#27682=CARTESIAN_POINT('Ctrl Pts',(-2.37446221325061,0.788309337875694,
5.79545404220658));
#27683=CARTESIAN_POINT('Ctrl Pts',(-2.37560000326959,0.00255553392953162,
5.84842075540369));
#27684=CARTESIAN_POINT('Ctrl Pts',(-2.37559927670797,4.64153524631309E-5,
5.84858989190501));
#27685=CARTESIAN_POINT('Origin',(0.,0.,-1.84858989190501));
#27686=CARTESIAN_POINT('',(-2.37512893756715,0.000936004496838188,3.65141010809498));
#27687=CARTESIAN_POINT('',(-2.36884487406159,0.0014490806830475,3.84858989190502));
#27688=CARTESIAN_POINT('',(-2.37175,-1.78696459712734E-13,-1.84858989190501));
#27689=CARTESIAN_POINT('Ctrl Pts',(-2.37512893756715,0.000936004496838207,
3.65141010809498));
#27690=CARTESIAN_POINT('Ctrl Pts',(-2.37144701194991,-0.729355776449451,
3.70061211507407));
#27691=CARTESIAN_POINT('Ctrl Pts',(-1.62047524979812,-2.24935719258021,
3.80257823495639));
#27692=CARTESIAN_POINT('Ctrl Pts',(0.963480161046465,-2.62950385116291,
3.95730846774193));
#27693=CARTESIAN_POINT('Ctrl Pts',(2.72987555186367,-0.62479115878066,4.11560080645161));
#27694=CARTESIAN_POINT('Ctrl Pts',(2.01129273950979,1.94866262755053,4.27389314516129));
#27695=CARTESIAN_POINT('Ctrl Pts',(-0.538149583533225,2.74826846342811,
4.43218548387097));
#27696=CARTESIAN_POINT('Ctrl Pts',(-2.17546335777147,1.39512363286222,4.55802447151553));
#27697=CARTESIAN_POINT('Ctrl Pts',(-2.37032708228576,0.304923911636404,
4.63109934625687));
#27698=CARTESIAN_POINT('Ctrl Pts',(-2.36873091192997,0.00136091434597342,
4.65141010809498));
#27699=CARTESIAN_POINT('Ctrl Pts',(-2.36884487406159,0.0014490806830475,
3.84858989190502));
#27700=CARTESIAN_POINT('Ctrl Pts',(-2.36608421378806,-0.490609372151221,
3.88151650172098));
#27701=CARTESIAN_POINT('Ctrl Pts',(-1.97696067069986,-1.77568073879797,
3.96724068823273));
#27702=CARTESIAN_POINT('Ctrl Pts',(0.126191152782097,-2.79821269277661,
4.10576245144026));
#27703=CARTESIAN_POINT('Ctrl Pts',(2.41603635476259,-1.41728148685534,4.26415518152759));
#27704=CARTESIAN_POINT('Ctrl Pts',(2.50403167886292,1.25528635446798,4.42254791161495));
#27705=CARTESIAN_POINT('Ctrl Pts',(0.309982763347203,2.78385149874581,4.58094064170228));
#27706=CARTESIAN_POINT('Ctrl Pts',(-1.91047842319259,1.87964319012959,4.72295463513232));
#27707=CARTESIAN_POINT('Ctrl Pts',(-2.36577077736693,0.541616601972229,
4.81217105186656));
#27708=CARTESIAN_POINT('Ctrl Pts',(-2.37001948420046,-0.00195088435344316,
4.84858989190502));
#27709=CARTESIAN_POINT('Origin',(0.,0.,-1.84858989190501));
#27710=CARTESIAN_POINT('',(-2.37135157935354,-0.0021318991616305,2.65141010809498));
#27711=CARTESIAN_POINT('',(-2.37519554933426,0.000880106332527136,2.84858989190502));
#27712=CARTESIAN_POINT('',(-2.37175,-1.78696459712734E-13,-1.84858989190501));
#27713=CARTESIAN_POINT('Ctrl Pts',(-2.37135157935354,-0.00213189916163091,
2.65141010809498));
#27714=CARTESIAN_POINT('Ctrl Pts',(-2.37311082894275,-0.198666550155835,
2.66459665808482));
#27715=CARTESIAN_POINT('Ctrl Pts',(-2.26106011094342,-1.17962859930864,
2.7305473209779));
#27716=CARTESIAN_POINT('Ctrl Pts',(-0.901256421879981,-2.65147525836599,
2.84926209677419));
#27717=CARTESIAN_POINT('Ctrl Pts',(1.73228815673516,-2.20040050466946,3.00755443548387));
#27718=CARTESIAN_POINT('Ctrl Pts',(2.78894830461411,0.253676763035589,3.16584677419355));
#27719=CARTESIAN_POINT('Ctrl Pts',(1.30685690747379,2.47683457209687,3.32413911290322));
#27720=CARTESIAN_POINT('Ctrl Pts',(-1.36485315638996,2.44535486220292,3.4824314516129));
#27721=CARTESIAN_POINT('Ctrl Pts',(-2.34988246062014,0.889580033391542,
3.59152178334349));
#27722=CARTESIAN_POINT('Ctrl Pts',(-2.37539550004821,0.0538073574959181,
3.64784800217084));
#27723=CARTESIAN_POINT('Ctrl Pts',(-2.37512893756715,0.000936004496838207,
3.65141010809498));
#27724=CARTESIAN_POINT('Ctrl Pts',(-2.37519554933426,0.00088010633252705,
2.84858989190502));
#27725=CARTESIAN_POINT('Ctrl Pts',(-2.37168702189121,-0.733401409280994,
2.89806437487963));
#27726=CARTESIAN_POINT('Ctrl Pts',(-1.61323878014562,-2.25754538560165,
3.00033643455002));
#27727=CARTESIAN_POINT('Ctrl Pts',(0.978835944215164,-2.62446160086853,
3.15540607091619));
#27728=CARTESIAN_POINT('Ctrl Pts',(2.73439785209926,-0.607442893388946,
3.31379880100354));
#27729=CARTESIAN_POINT('Ctrl Pts',(1.99797176831316,1.9631676666159,3.47219153109088));
#27730=CARTESIAN_POINT('Ctrl Pts',(-0.559301870866465,2.7446493220368,3.63058426117822));
#27731=CARTESIAN_POINT('Ctrl Pts',(-2.18121205708018,1.38232176842859,3.7560503814496));
#27732=CARTESIAN_POINT('Ctrl Pts',(-2.37051091223462,0.29840273834331,3.8287189250252));
#27733=CARTESIAN_POINT('Ctrl Pts',(-2.36884487406159,0.0014490806830475,
3.84858989190502));
#27734=CARTESIAN_POINT('Origin',(0.,0.,-1.84858989190501));
#27735=CARTESIAN_POINT('',(-2.36819810156307,0.000841410002426573,1.65141010809498));
#27736=CARTESIAN_POINT('',(-2.37133740986255,-0.00213858212026324,1.84858989190502));
#27737=CARTESIAN_POINT('',(-2.37175,-1.78696459712734E-13,-1.84858989190501));
#27738=CARTESIAN_POINT('Ctrl Pts',(-2.36819810156307,0.000841410002426421,
1.65141010809498));
#27739=CARTESIAN_POINT('Ctrl Pts',(-2.36676749726595,-0.446820888278083,
1.6813453139988));
#27740=CARTESIAN_POINT('Ctrl Pts',(-2.02989303093846,-1.68553679022923,
1.76404463280585));
#27741=CARTESIAN_POINT('Ctrl Pts',(-0.0334666860564693,-2.80025859792997,
1.89950806451613));
#27742=CARTESIAN_POINT('Ctrl Pts',(2.32986892611582,-1.55380138209287,2.0578004032258));
#27743=CARTESIAN_POINT('Ctrl Pts',(2.57234931467855,1.10707092589757,2.21609274193548));
#27744=CARTESIAN_POINT('Ctrl Pts',(0.473245533627712,2.76018492369889,2.37438508064516));
#27745=CARTESIAN_POINT('Ctrl Pts',(-1.84589567906405,1.97232864399116,2.51949086936499));
#27746=CARTESIAN_POINT('Ctrl Pts',(-2.36607144077667,0.587739031473957,
2.6118325451816));
#27747=CARTESIAN_POINT('Ctrl Pts',(-2.37135157935354,-0.00213189916163091,
2.65141010809498));
#27748=CARTESIAN_POINT('Ctrl Pts',(-2.37133740986255,-0.00213858212026316,
1.84858989190502));
#27749=CARTESIAN_POINT('Ctrl Pts',(-2.37310428453163,-0.199245954569927,
1.86181467134249));
#27750=CARTESIAN_POINT('Ctrl Pts',(-2.26061413178437,-1.18128083118873,
1.92783702747574));
#27751=CARTESIAN_POINT('Ctrl Pts',(-0.897863084978552,-2.65325422541087,
2.04665696030478));
#27752=CARTESIAN_POINT('Ctrl Pts',(1.7370153276097,-2.19742960924133,2.20504969039212));
#27753=CARTESIAN_POINT('Ctrl Pts',(2.78886857766781,0.261018802222555,2.36344242047947));
#27754=CARTESIAN_POINT('Ctrl Pts',(1.29909191311228,2.48158786740548,2.52183515056681));
#27755=CARTESIAN_POINT('Ctrl Pts',(-1.37460948338166,2.44056701717432,2.68022788065416));
#27756=CARTESIAN_POINT('Ctrl Pts',(-2.35172378535123,0.882891152726273,
2.78914612776689));
#27757=CARTESIAN_POINT('Ctrl Pts',(-2.37543120951332,0.0502002032269103,
2.84526679818384));
#27758=CARTESIAN_POINT('Ctrl Pts',(-2.37519554933426,0.00088010633252705,
2.84858989190502));
#27759=CARTESIAN_POINT('Origin',(0.,0.,-1.84858989190501));
#27760=CARTESIAN_POINT('',(-2.37433784198147,0.00164420209662431,0.651410108094979));
#27761=CARTESIAN_POINT('',(-2.36815429608613,0.000817443606317692,0.848589891905017));
#27762=CARTESIAN_POINT('',(-2.37175,-1.78696459712734E-13,-1.84858989190501));
#27763=CARTESIAN_POINT('Ctrl Pts',(-2.37433784198147,0.00164420209662409,
0.651410108094979));
#27764=CARTESIAN_POINT('Ctrl Pts',(-2.36924246624065,-0.691823527182799,
0.698093969912781));
#27765=CARTESIAN_POINT('Ctrl Pts',(-1.6837126199259,-2.17836324814241,0.797541944633808));
#27766=CARTESIAN_POINT('Ctrl Pts',(0.837655777364047,-2.67211687161305,
0.949754032258061));
#27767=CARTESIAN_POINT('Ctrl Pts',(2.69714227944592,-0.753688528678065,
1.10804637096774));
#27768=CARTESIAN_POINT('Ctrl Pts',(2.10149481948277,1.85107442631988,1.26633870967742));
#27769=CARTESIAN_POINT('Ctrl Pts',(-0.407147056663944,2.77068707131458,
1.42463104838709));
#27770=CARTESIAN_POINT('Ctrl Pts',(-2.14082823127596,1.47128617579538,1.55298818119295));
#27771=CARTESIAN_POINT('Ctrl Pts',(-2.36928909564398,0.342233448775053,
1.62858120109558));
#27772=CARTESIAN_POINT('Ctrl Pts',(-2.36819810156307,0.000841410002426421,
1.65141010809498));
#27773=CARTESIAN_POINT('Ctrl Pts',(-2.36815429608612,0.000817443606317657,
0.848589891905016));
#27774=CARTESIAN_POINT('Ctrl Pts',(-2.36680126784445,-0.444438138072723,
0.878362544501135));
#27775=CARTESIAN_POINT('Ctrl Pts',(-2.03256363798364,-1.68119575265189,
0.960932773793035));
#27776=CARTESIAN_POINT('Ctrl Pts',(-0.0402824848387021,-2.80074754850057,
1.09630057978071));
#27777=CARTESIAN_POINT('Ctrl Pts',(2.32755559974952,-1.55833818967747,1.25469330986806));
#27778=CARTESIAN_POINT('Ctrl Pts',(2.57419348860935,1.10429523958194,1.4130860399554));
#27779=CARTESIAN_POINT('Ctrl Pts',(0.474838546093255,2.76051273114501,1.57147877004275));
#27780=CARTESIAN_POINT('Ctrl Pts',(-1.84584231488806,1.97272007570003,1.71664672069262));
#27781=CARTESIAN_POINT('Ctrl Pts',(-2.36605035207901,0.587670126973683,
1.80901709464671));
#27782=CARTESIAN_POINT('Ctrl Pts',(-2.37133740986255,-0.00213858212026316,
1.84858989190502));
#27783=CARTESIAN_POINT('Origin',(0.,0.,19.5));
#27784=CARTESIAN_POINT('',(-2.86978283437093,0.00124690900571957,19.1339652973708));
#27785=CARTESIAN_POINT('Ctrl Pts',(-0.439445221994122,2.33068358199189,
19.62825));
#27786=CARTESIAN_POINT('Ctrl Pts',(-0.359496399915194,2.34930837340854,
19.6247608600375));
#27787=CARTESIAN_POINT('Ctrl Pts',(-0.278741728044194,2.36340753905626,
19.6212859488617));
#27788=CARTESIAN_POINT('Ctrl Pts',(-0.197506041411201,2.3731670460491,19.6178205395779));
#27789=CARTESIAN_POINT('Ctrl Pts',(-0.114116696920991,2.38318528956266,
19.6142632580364));
#27790=CARTESIAN_POINT('Ctrl Pts',(-0.0302197403964261,2.3886307553927,
19.6107159888789));
#27791=CARTESIAN_POINT('Ctrl Pts',(0.0538488183862894,2.38965232235862,
19.6071736192084));
#27792=CARTESIAN_POINT('Ctrl Pts',(0.0937194843833986,2.39013681449078,
19.6054936018509));
#27793=CARTESIAN_POINT('Ctrl Pts',(0.133628895976177,2.38962550572521,19.6038146865157));
#27794=CARTESIAN_POINT('Ctrl Pts',(0.173541591315785,2.3881303051021,19.6021363277883));
#27795=CARTESIAN_POINT('Ctrl Pts',(0.197736469304413,2.38722392189904,19.6011189150506));
#27796=CARTESIAN_POINT('Ctrl Pts',(0.221932555405085,2.38595593679589,19.600101706851));
#27797=CARTESIAN_POINT('Ctrl Pts',(0.246121926732615,2.38432855965558,19.5990845816929));
#27798=CARTESIAN_POINT('Ctrl Pts',(0.261966760970886,2.3832625740753,19.5984183312429));
#27799=CARTESIAN_POINT('Ctrl Pts',(0.27780950980444,2.38204221833013,19.5977520828035));
#27800=CARTESIAN_POINT('Ctrl Pts',(0.293631569537354,2.38066972871238,19.5970864910922));
#27801=CARTESIAN_POINT('Ctrl Pts',(0.379373845864251,2.37323198760618,19.5934795429833));
#27802=CARTESIAN_POINT('Ctrl Pts',(0.464621179595313,2.36132408278005,19.5898871205887));
#27803=CARTESIAN_POINT('Ctrl Pts',(0.549021293139782,2.3451096637313,19.5863039889554));
#27804=CARTESIAN_POINT('Ctrl Pts',(0.634164428857974,2.32875249993515,19.5826893129777));
#27805=CARTESIAN_POINT('Ctrl Pts',(0.718446312182276,2.30801251387993,19.5790840920651));
#27806=CARTESIAN_POINT('Ctrl Pts',(0.801504492173054,2.28300464467492,19.5754829517853));
#27807=CARTESIAN_POINT('Ctrl Pts',(0.853054825935946,2.26748342804869,19.5732478921756));
#27808=CARTESIAN_POINT('Ctrl Pts',(0.904133707598755,2.25031714023312,19.5710144044686));
#27809=CARTESIAN_POINT('Ctrl Pts',(0.954651843583393,2.23152350140498,19.5687812037332));
#27810=CARTESIAN_POINT('Ctrl Pts',(0.966661711293098,2.22705561850094,19.5682502964684));
#27811=CARTESIAN_POINT('Ctrl Pts',(0.978637539548016,2.22249655100818,19.5677195079304));
#27812=CARTESIAN_POINT('Ctrl Pts',(0.990570080353664,2.21784986361285,19.5671891810056));
#27813=CARTESIAN_POINT('Ctrl Pts',(1.07233004187525,2.18601146566952,19.5635554612747));
#27814=CARTESIAN_POINT('Ctrl Pts',(1.15216830046977,2.15002310442033,19.5599385463906));
#27815=CARTESIAN_POINT('Ctrl Pts',(1.22972588848851,2.11003339454853,19.5563331219261));
#27816=CARTESIAN_POINT('Ctrl Pts',(1.30689380941087,2.07024460214374,19.5527458119404));
#27817=CARTESIAN_POINT('Ctrl Pts',(1.3818048666458,2.02649428366031,19.5491698772035));
#27818=CARTESIAN_POINT('Ctrl Pts',(1.45409265027459,1.97887925509432,19.5456000829893));
#27819=CARTESIAN_POINT('Ctrl Pts',(1.51414958607928,1.93932052787409,19.542634285849));
#27820=CARTESIAN_POINT('Ctrl Pts',(1.57239588882887,1.89709330508863,19.5396727271079));
#27821=CARTESIAN_POINT('Ctrl Pts',(1.6286075594529,1.85222888403246,19.5367124049177));
#27822=CARTESIAN_POINT('Ctrl Pts',(1.65671339476491,1.82979667350437,19.5352322438226));
#27823=CARTESIAN_POINT('Ctrl Pts',(1.68431033399215,1.80670482947816,19.5337523918653));
#27824=CARTESIAN_POINT('Ctrl Pts',(1.71136870094884,1.78295531352429,19.5322724738146));
#27825=CARTESIAN_POINT('Ctrl Pts',(1.72505548280361,1.77094222919672,19.5315238951751));
#27826=CARTESIAN_POINT('Ctrl Pts',(1.7386044467155,1.7587608538397,19.5307752996251));
#27827=CARTESIAN_POINT('Ctrl Pts',(1.75201162231319,1.74641131895379,19.5300266386024));
#27828=CARTESIAN_POINT('Ctrl Pts',(1.76374413009413,1.73560434375724,19.5293714915723));
#27829=CARTESIAN_POINT('Ctrl Pts',(1.77536978940808,1.72466678187038,19.5287161918229));
#27830=CARTESIAN_POINT('Ctrl Pts',(1.78686993494738,1.71361443483951,19.5280616263465));
#27831=CARTESIAN_POINT('Ctrl Pts',(1.78820879329981,1.71232770963368,19.5279854211844));
#27832=CARTESIAN_POINT('Ctrl Pts',(1.7895459973299,1.71103938648239,19.527909223385));
#27833=CARTESIAN_POINT('Ctrl Pts',(1.79088154369118,1.70974946659003,19.5278330328994));
#27834=CARTESIAN_POINT('Ctrl Pts',(1.8509299108473,1.65175254072928,19.5244073830022));
#27835=CARTESIAN_POINT('Ctrl Pts',(1.90762953422213,1.59053155433168,19.5209965182257));
#27836=CARTESIAN_POINT('Ctrl Pts',(1.96096030440938,1.52647851758989,19.5175959868336));
#27837=CARTESIAN_POINT('Ctrl Pts',(2.01585595410063,1.46054597893928,19.514095673986));
#27838=CARTESIAN_POINT('Ctrl Pts',(2.06718257934786,1.39161216589875,19.5106063098428));
#27839=CARTESIAN_POINT('Ctrl Pts',(2.11488498779521,1.32006098590835,19.5071230391759));
#27840=CARTESIAN_POINT('Ctrl Pts',(2.16100614932092,1.25088159566155,19.5037552325118));
#27841=CARTESIAN_POINT('Ctrl Pts',(2.20373946041229,1.17925459387015,19.5003931220444));
#27842=CARTESIAN_POINT('Ctrl Pts',(2.24300118618815,1.10549836563141,19.4970323195431));
#27843=CARTESIAN_POINT('Ctrl Pts',(2.26017819121508,1.07323001577696,19.4955619684488));
#27844=CARTESIAN_POINT('Ctrl Pts',(2.27669026031943,1.04055381937119,19.4940918677074));
#27845=CARTESIAN_POINT('Ctrl Pts',(2.29252817853264,1.00749527125662,19.4926216498475));
#27846=CARTESIAN_POINT('Ctrl Pts',(2.300517169549,0.99081981932247,19.4918800399264));
#27847=CARTESIAN_POINT('Ctrl Pts',(2.30833460670403,0.974047072136536,19.4911384002056));
#27848=CARTESIAN_POINT('Ctrl Pts',(2.31597916990764,0.957180253262817,19.4903966835216));
#27849=CARTESIAN_POINT('Ctrl Pts',(2.32148143469363,0.945040160877076,19.4898628241652));
#27850=CARTESIAN_POINT('Ctrl Pts',(2.32689374255309,0.932852048460756,19.4893289576981));
#27851=CARTESIAN_POINT('Ctrl Pts',(2.332210604538,0.92062911548402,19.4887955857665));
#27852=CARTESIAN_POINT('Ctrl Pts',(2.36777326752894,0.838874116492736,19.4852280441781));
#27853=CARTESIAN_POINT('Ctrl Pts',(2.39913263839588,0.755425618458568,19.4816765201166));
#27854=CARTESIAN_POINT('Ctrl Pts',(2.4262333303409,0.670689801398847,19.4781359905495));
#27855=CARTESIAN_POINT('Ctrl Pts',(2.45364753630358,0.584973719093478,19.4745545024102));
#27856=CARTESIAN_POINT('Ctrl Pts',(2.47670437210413,0.497939463359003,19.4709842646162));
#27857=CARTESIAN_POINT('Ctrl Pts',(2.49530163963731,0.409978999236876,19.4674200777839));
#27858=CARTESIAN_POINT('Ctrl Pts',(2.51280420413611,0.327196209028843,19.4640656919955));
#27859=CARTESIAN_POINT('Ctrl Pts',(2.52635662496927,0.243592136482556,19.4607166657717));
#27860=CARTESIAN_POINT('Ctrl Pts',(2.53583313283201,0.159481833132225,19.457368664907));
#27861=CARTESIAN_POINT('Ctrl Pts',(2.53950882122587,0.126857656557172,19.4560700633441));
#27862=CARTESIAN_POINT('Ctrl Pts',(2.5425708637383,0.0941572581992666,19.4547716160424));
#27863=CARTESIAN_POINT('Ctrl Pts',(2.5450101915364,0.0613989272386214,19.4534730700835));
#27864=CARTESIAN_POINT('Ctrl Pts',(2.54664995154104,0.0393781881769477,
19.4526001641423));
#27865=CARTESIAN_POINT('Ctrl Pts',(2.54800830074101,0.0173312706195899,
19.4517272136201));
#27866=CARTESIAN_POINT('Ctrl Pts',(2.54908222580259,-0.00473625006357956,
19.4508541416904));
#27867=CARTESIAN_POINT('Ctrl Pts',(2.5497978073951,-0.0194403594638387,
19.450272393276));
#27868=CARTESIAN_POINT('Ctrl Pts',(2.55038670103113,-0.0341462169389561,
19.4496908837209));
#27869=CARTESIAN_POINT('Ctrl Pts',(2.55084824252384,-0.048844767938526,
19.4491098818334));
#27870=CARTESIAN_POINT('Ctrl Pts',(2.55374081608822,-0.140963549732027,
19.4454686258957));
#27871=CARTESIAN_POINT('Ctrl Pts',(2.55164005327307,-0.232884185733536,
19.4418437427226));
#27872=CARTESIAN_POINT('Ctrl Pts',(2.54444222542436,-0.324196175898947,
19.4382298881162));
#27873=CARTESIAN_POINT('Ctrl Pts',(2.53724439757566,-0.415508166064358,
19.4346160335098));
#27874=CARTESIAN_POINT('Ctrl Pts',(2.524949863139,-0.506212566736429,19.4310132074699));
#27875=CARTESIAN_POINT('Ctrl Pts',(2.50739898915578,-0.595905850588752,
19.4274160657988));
#27876=CARTESIAN_POINT('Ctrl Pts',(2.49041552541174,-0.682699399209003,
19.4239352177673));
#27877=CARTESIAN_POINT('Ctrl Pts',(2.46850979008406,-0.768546973818678,
19.4204596925007));
#27878=CARTESIAN_POINT('Ctrl Pts',(2.44195100957766,-0.853189635279847,
19.4169846475493));
#27879=CARTESIAN_POINT('Ctrl Pts',(2.43105026163653,-0.887930248367561,
19.4155583550624));
#27880=CARTESIAN_POINT('Ctrl Pts',(2.4193650665621,-0.922467728725974,19.4141321434892));
#27881=CARTESIAN_POINT('Ctrl Pts',(2.40691167793065,-0.956783357203964,
19.4127056780113));
#27882=CARTESIAN_POINT('Ctrl Pts',(2.40227529198214,-0.969559036370352,
19.4121746061325));
#27883=CARTESIAN_POINT('Ctrl Pts',(2.39753142734847,-0.982306537607564,
19.4116433912781));
#27884=CARTESIAN_POINT('Ctrl Pts',(2.39268420846545,-0.995016186464471,
19.4111123792872));
#27885=CARTESIAN_POINT('Ctrl Pts',(2.36008996603969,-1.08047991029981,19.4075416856628));
#27886=CARTESIAN_POINT('Ctrl Pts',(2.32289371031631,-1.16406508789994,19.4039871869403));
#27887=CARTESIAN_POINT('Ctrl Pts',(2.28145232389539,-1.2455084624321,19.4004438616248));
#27888=CARTESIAN_POINT('Ctrl Pts',(2.2401496080627,-1.3266793122823,19.3969123929349));
#27889=CARTESIAN_POINT('Ctrl Pts',(2.19462948656474,-1.40572341239688,19.3933920230006));
#27890=CARTESIAN_POINT('Ctrl Pts',(2.14519002651603,-1.48236812476013,19.3898777805668));
#27891=CARTESIAN_POINT('Ctrl Pts',(2.09545800359527,-1.5594663897543,19.3863427422575));
#27892=CARTESIAN_POINT('Ctrl Pts',(2.0417595663806,-1.63413758358452,19.3828139041835));
#27893=CARTESIAN_POINT('Ctrl Pts',(1.98435092675475,-1.70608041179627,19.3792862063132));
#27894=CARTESIAN_POINT('Ctrl Pts',(1.96385857271652,-1.73176083055963,19.3780269736581));
#27895=CARTESIAN_POINT('Ctrl Pts',(1.94289307887375,-1.75709333013408,19.376767886285));
#27896=CARTESIAN_POINT('Ctrl Pts',(1.92146486206384,-1.7820631761771,19.3755087140512));
#27897=CARTESIAN_POINT('Ctrl Pts',(1.90808270355052,-1.79765712133665,19.3747223470577));
#27898=CARTESIAN_POINT('Ctrl Pts',(1.89452006441996,-1.81310961476765,19.3739359469673));
#27899=CARTESIAN_POINT('Ctrl Pts',(1.88077936786051,-1.82841694049769,19.3731494577247));
#27900=CARTESIAN_POINT('Ctrl Pts',(1.8684512417402,-1.84215064325055,19.3724438211121));
#27901=CARTESIAN_POINT('Ctrl Pts',(1.85597675343054,-1.85577058254818,19.3717379474738));
#27902=CARTESIAN_POINT('Ctrl Pts',(1.84337723420589,-1.86925344146862,19.3710328821673));
#27903=CARTESIAN_POINT('Ctrl Pts',(1.77710288751082,-1.94017421634914,19.3673241896579));
#27904=CARTESIAN_POINT('Ctrl Pts',(1.70728117389982,-2.00741106239547,19.3636324635521));
#27905=CARTESIAN_POINT('Ctrl Pts',(1.63425481305677,-2.07065048051062,19.3599520680256));
#27906=CARTESIAN_POINT('Ctrl Pts',(1.56435178486444,-2.1311851528719,19.3564290827738));
#27907=CARTESIAN_POINT('Ctrl Pts',(1.4915113914409,-2.1880576143788,19.3529164796116));
#27908=CARTESIAN_POINT('Ctrl Pts',(1.4159918760443,-2.24096200122539,19.3494093153588));
#27909=CARTESIAN_POINT('Ctrl Pts',(1.34164349717693,-2.29304596093249,19.3459565392752));
#27910=CARTESIAN_POINT('Ctrl Pts',(1.26469778687837,-2.34128460563477,19.3425090347186));
#27911=CARTESIAN_POINT('Ctrl Pts',(1.18537076960009,-2.38534634059117,19.3390620849337));
#27912=CARTESIAN_POINT('Ctrl Pts',(1.15499487450069,-2.40221845660982,19.3377421791983));
#27913=CARTESIAN_POINT('Ctrl Pts',(1.12426954458043,-2.41847765262325,19.3364223548077));
#27914=CARTESIAN_POINT('Ctrl Pts',(1.0932060081487,-2.43410342660017,19.3351023469319));
#27915=CARTESIAN_POINT('Ctrl Pts',(1.07852356668983,-2.44148907994231,19.3344784341201));
#27916=CARTESIAN_POINT('Ctrl Pts',(1.06376556159054,-2.44873320670299,19.3338544803166));
#27917=CARTESIAN_POINT('Ctrl Pts',(1.04893314692695,-2.45583355114468,19.3332304575567));
#27918=CARTESIAN_POINT('Ctrl Pts',(1.03777451577937,-2.46117523868798,19.3327609965847));
#27919=CARTESIAN_POINT('Ctrl Pts',(1.02657507642648,-2.46643486915688,19.3322915524202));
#27920=CARTESIAN_POINT('Ctrl Pts',(1.01534417119219,-2.47160761026341,19.3318224792748));
#27921=CARTESIAN_POINT('Ctrl Pts',(0.976776596263432,-2.48937110092166,
19.3302116550977));
#27922=CARTESIAN_POINT('Ctrl Pts',(0.937809807627497,-2.50612368700867,
19.3286040154222));
#27923=CARTESIAN_POINT('Ctrl Pts',(0.898469638803505,-2.52183800942761,
19.3269990986982));
#27924=CARTESIAN_POINT('Ctrl Pts',(0.815541152704475,-2.55496356549997,
19.3236159583045));
#27925=CARTESIAN_POINT('Ctrl Pts',(0.730955270809804,-2.58347870238839,
19.3202449176199));
#27926=CARTESIAN_POINT('Ctrl Pts',(0.645080730189636,-2.60751906959201,
19.3168816532826));
#27927=CARTESIAN_POINT('Ctrl Pts',(0.556937627094779,-2.63219451530112,
19.3134295410143));
#27928=CARTESIAN_POINT('Ctrl Pts',(0.467436139325503,-2.65215578598813,
19.3099856213784));
#27929=CARTESIAN_POINT('Ctrl Pts',(0.376952220119887,-2.66749996206646,
19.3065452192493));
#27930=CARTESIAN_POINT('Ctrl Pts',(0.28814825433163,-2.68255925325844,19.3031686927278));
#27931=CARTESIAN_POINT('Ctrl Pts',(0.198397148537396,-2.69317110363349,
19.2997955543113));
#27932=CARTESIAN_POINT('Ctrl Pts',(0.108044784410401,-2.69938115345377,
19.2964213844691));
#27933=CARTESIAN_POINT('Ctrl Pts',(0.0846755836239938,-2.700987352722,19.2955486718037));
#27934=CARTESIAN_POINT('Ctrl Pts',(0.0612661467540061,-2.70229884783018,
19.2946758901386));
#27935=CARTESIAN_POINT('Ctrl Pts',(0.037822458411094,-2.7033159368433,19.2938029630042));
#27936=CARTESIAN_POINT('Ctrl Pts',(0.0220310773589827,-2.70400103553319,
19.2932149699884));
#27937=CARTESIAN_POINT('Ctrl Pts',(0.00623212385897853,-2.70455216083962,
19.2926272077515));
#27938=CARTESIAN_POINT('Ctrl Pts',(-0.00956443944047891,-2.70496967952273,
19.2920399533629));
#27939=CARTESIAN_POINT('Ctrl Pts',(-0.103598710039189,-2.70745509765341,
19.2885441272746));
#27940=CARTESIAN_POINT('Ctrl Pts',(-0.197635930615719,-2.70521413060483,
19.2850629827735));
#27941=CARTESIAN_POINT('Ctrl Pts',(-0.291281950672319,-2.69836938342123,
19.2815917980052));
#27942=CARTESIAN_POINT('Ctrl Pts',(-0.38606363263148,-2.69144162877396,
19.2780785175632));
#27943=CARTESIAN_POINT('Ctrl Pts',(-0.480445514899326,-2.67979776357681,
19.2745754398856));
#27944=CARTESIAN_POINT('Ctrl Pts',(-0.574027890122098,-2.66351219296258,
19.2710776692377));
#27945=CARTESIAN_POINT('Ctrl Pts',(-0.667261159572748,-2.64728737509896,
19.2675929469006));
#27946=CARTESIAN_POINT('Ctrl Pts',(-0.759701848049967,-2.62645531011172,
19.2641134920718));
#27947=CARTESIAN_POINT('Ctrl Pts',(-0.850949097824244,-2.60103852864063,
19.2606344636025));
#27948=CARTESIAN_POINT('Ctrl Pts',(-0.888409306005341,-2.59060404510764,
19.2592061999446));
#27949=CARTESIAN_POINT('Ctrl Pts',(-0.925668224932336,-2.57939626873602,
19.2577780081451));
#27950=CARTESIAN_POINT('Ctrl Pts',(-0.962697255759592,-2.56741431371771,
19.2563495532386));
#27951=CARTESIAN_POINT('Ctrl Pts',(-0.978584771163812,-2.56227338805281,
19.2557366665704));
#27952=CARTESIAN_POINT('Ctrl Pts',(-0.994429958507756,-2.55698992710178,
19.2551237314672));
#27953=CARTESIAN_POINT('Ctrl Pts',(-1.01023051820469,-2.55156378128263,
19.254510721472));
#27954=CARTESIAN_POINT('Ctrl Pts',(-1.02485107054566,-2.54654286743652,
19.2539434918995));
#27955=CARTESIAN_POINT('Ctrl Pts',(-1.03942581785439,-2.54140235120542,
19.2533764922911));
#27956=CARTESIAN_POINT('Ctrl Pts',(-1.05394656826891,-2.53614492416381,
19.2528099559783));
#27957=CARTESIAN_POINT('Ctrl Pts',(-1.1442425835919,-2.5034520743346,19.2492869995111));
#27958=CARTESIAN_POINT('Ctrl Pts',(-1.23253047867916,-2.46621543590235,
19.2457788737934));
#27959=CARTESIAN_POINT('Ctrl Pts',(-1.31841054501642,-2.42451396270994,
19.2422807482851));
#27960=CARTESIAN_POINT('Ctrl Pts',(-1.40295505543142,-2.38346100612755,
19.2388370235527));
#27961=CARTESIAN_POINT('Ctrl Pts',(-1.48516695569074,-2.33808077848995,
19.2354029904136));
#27962=CARTESIAN_POINT('Ctrl Pts',(-1.56465265588408,-2.28840031795577,
19.2319740402064));
#27963=CARTESIAN_POINT('Ctrl Pts',(-1.60634279285186,-2.26234298689805,
19.2301755606881));
#27964=CARTESIAN_POINT('Ctrl Pts',(-1.64728266840485,-2.23510188014699,
19.2283784794781));
#27965=CARTESIAN_POINT('Ctrl Pts',(-1.68741284053105,-2.20667575559394,
19.2265821315976));
#27966=CARTESIAN_POINT('Ctrl Pts',(-1.76408500272364,-2.15236518783998,
19.2231500537182));
#27967=CARTESIAN_POINT('Ctrl Pts',(-1.83780366664609,-2.09373114303323,
19.2197206527414));
#27968=CARTESIAN_POINT('Ctrl Pts',(-1.90842406585113,-2.03112180178175,
19.2162892909117));
#27969=CARTESIAN_POINT('Ctrl Pts',(-1.92415367580141,-2.01717653202662,
19.2155250077331));
#27970=CARTESIAN_POINT('Ctrl Pts',(-1.93973411950598,-2.0030293780058,19.2147603912815));
#27971=CARTESIAN_POINT('Ctrl Pts',(-1.95513815612309,-1.98870805072037,
19.2139966607035));
#27972=CARTESIAN_POINT('Ctrl Pts',(-2.02393936909849,-1.92474269455126,
19.2105855035206));
#27973=CARTESIAN_POINT('Ctrl Pts',(-2.08930100738169,-1.85724208008421,
19.2071883480391));
#27974=CARTESIAN_POINT('Ctrl Pts',(-2.15113215444763,-1.78661473678416,
19.2038008153795));
#27975=CARTESIAN_POINT('Ctrl Pts',(-2.21426051930702,-1.714505631447,19.2003422122668));
#27976=CARTESIAN_POINT('Ctrl Pts',(-2.27370921946588,-1.63913657767921,
19.1968936399852));
#27977=CARTESIAN_POINT('Ctrl Pts',(-2.32934945775057,-1.56089671412961,
19.1934504382259));
#27978=CARTESIAN_POINT('Ctrl Pts',(-2.3854816519556,-1.48196507489273,19.189976792609));
#27979=CARTESIAN_POINT('Ctrl Pts',(-2.43773825193628,-1.40011084488009,
19.1865086129037));
#27980=CARTESIAN_POINT('Ctrl Pts',(-2.48594698643214,-1.31569866499581,
19.1830411140891));
#27981=CARTESIAN_POINT('Ctrl Pts',(-2.51310393228564,-1.26814759313163,
19.1810878025463));
#27982=CARTESIAN_POINT('Ctrl Pts',(-2.53897560819788,-1.21978424599781,
19.1791347070703));
#27983=CARTESIAN_POINT('Ctrl Pts',(-2.56352474874957,-1.17067045541336,
19.1771809723));
#27984=CARTESIAN_POINT('Ctrl Pts',(-2.5701220073907,-1.15747177016204,19.1766559317769));
#27985=CARTESIAN_POINT('Ctrl Pts',(-2.57662472903377,-1.14421678676666,
19.1761307625987));
#27986=CARTESIAN_POINT('Ctrl Pts',(-2.58302887965335,-1.13091345079126,
19.1756057150565));
#27987=CARTESIAN_POINT('Ctrl Pts',(-2.62568677355004,-1.04230024847588,
19.172108385953));
#27988=CARTESIAN_POINT('Ctrl Pts',(-2.66385866655196,-0.951788919503196,
19.1686260589889));
#27989=CARTESIAN_POINT('Ctrl Pts',(-2.69741818565158,-0.859782121332853,
19.1651540264633));
#27990=CARTESIAN_POINT('Ctrl Pts',(-2.73103699790175,-0.767612765024542,
19.1616758595307));
#27991=CARTESIAN_POINT('Ctrl Pts',(-2.76002758078427,-0.673941779287795,
19.1582080234452));
#27992=CARTESIAN_POINT('Ctrl Pts',(-2.78421958380913,-0.579144596406193,
19.1547457855091));
#27993=CARTESIAN_POINT('Ctrl Pts',(-2.80790962022943,-0.486314386658796,
19.1513553865116));
#27994=CARTESIAN_POINT('Ctrl Pts',(-2.82699841437237,-0.392403361685435,
19.1479703557585));
#27995=CARTESIAN_POINT('Ctrl Pts',(-2.84127941192308,-0.297748919984249,
19.1445862490817));
#27996=CARTESIAN_POINT('Ctrl Pts',(-2.85260005450855,-0.222715708906352,
19.1419036450113));
#27997=CARTESIAN_POINT('Ctrl Pts',(-2.86089874028508,-0.147214912387106,
19.1392216216156));
#27998=CARTESIAN_POINT('Ctrl Pts',(-2.8660492635332,-0.0714129213286235,
19.1365379651471));
#27999=CARTESIAN_POINT('Ctrl Pts',(-2.86769679090258,-0.0471657043165984,
19.1356795285827));
#28000=CARTESIAN_POINT('Ctrl Pts',(-2.8690199678599,-0.0229179339290668,
19.1348219958471));
#28001=CARTESIAN_POINT('Ctrl Pts',(-2.87001662176841,0.00132468418317613,
19.1339652973708));
#28002=CARTESIAN_POINT('',(0.261007814359831,2.92578301259841,19.058));
#28003=CARTESIAN_POINT('Ctrl Pts',(0.260898964428293,2.92506788491831,19.058));
#28004=CARTESIAN_POINT('Ctrl Pts',(0.163023909524402,2.92122872644259,19.0703782857669));
#28005=CARTESIAN_POINT('Ctrl Pts',(0.0656137074299065,2.912742505651,19.0828007237738));
#28006=CARTESIAN_POINT('Ctrl Pts',(-0.030953795983259,2.89962093163934,
19.0952868597003));
#28007=CARTESIAN_POINT('Ctrl Pts',(-0.130391850521096,2.88610930768639,
19.1081441566308));
#28008=CARTESIAN_POINT('Ctrl Pts',(-0.228937522172488,2.86768264892189,
19.1210689947157));
#28009=CARTESIAN_POINT('Ctrl Pts',(-0.326154050402428,2.8443004424986,19.134082714997));
#28010=CARTESIAN_POINT('Ctrl Pts',(-0.399066446574882,2.82676378768113,
19.143843005208));
#28011=CARTESIAN_POINT('Ctrl Pts',(-0.471230789680895,2.80643850217304,
19.1536532916545));
#28012=CARTESIAN_POINT('Ctrl Pts',(-0.542448327672379,2.78328892000252,
19.1635225775885));
#28013=CARTESIAN_POINT('Ctrl Pts',(-0.595861481165992,2.76592673337463,
19.1709245420391));
#28014=CARTESIAN_POINT('Ctrl Pts',(-0.6487418158016,2.74697554899712,19.1783596937014));
#28015=CARTESIAN_POINT('Ctrl Pts',(-0.700999502826955,2.72641481549739,
19.1858318308225));
#28016=CARTESIAN_POINT('Ctrl Pts',(-0.716250316273543,2.72041439854864,
19.1880124893202));
#28017=CARTESIAN_POINT('Ctrl Pts',(-0.731448062028104,2.71427686698661,
19.1901962978622));
#28018=CARTESIAN_POINT('Ctrl Pts',(-0.746590412830255,2.70800163764602,
19.1923833508571));
#28019=CARTESIAN_POINT('Ctrl Pts',(-0.759834193701528,2.70251320567204,
19.1942961879718));
#28020=CARTESIAN_POINT('Ctrl Pts',(-0.773030676312604,2.69692143623512,
19.1962107991778));
#28021=CARTESIAN_POINT('Ctrl Pts',(-0.786171449556019,2.69122928513894,
19.1981262233848));
#28022=CARTESIAN_POINT('Ctrl Pts',(-0.869595052331544,2.65509292214185,
19.2102862070654));
#28023=CARTESIAN_POINT('Ctrl Pts',(-0.950864331706193,2.61487768287787,
19.2224917235733));
#28024=CARTESIAN_POINT('Ctrl Pts',(-1.02964582077395,2.5705582476779,19.2347617221928));
#28025=CARTESIAN_POINT('Ctrl Pts',(-1.070119428365,2.54778935297729,19.2410653744231));
#28026=CARTESIAN_POINT('Ctrl Pts',(-1.1099359371769,2.52393656066965,19.2473860456799));
#28027=CARTESIAN_POINT('Ctrl Pts',(-1.14904652243468,2.49899242632004,19.2537263053885));
#28028=CARTESIAN_POINT('Ctrl Pts',(-1.22710174167599,2.4492099988107,19.2663799222633));
#28029=CARTESIAN_POINT('Ctrl Pts',(-1.30234807687636,2.39508206632693,19.2791115608326));
#28030=CARTESIAN_POINT('Ctrl Pts',(-1.37457154418326,2.3369356258057,19.291941645948));
#28031=CARTESIAN_POINT('Ctrl Pts',(-1.44877133871285,2.27719806265369,19.3051228142698));
#28032=CARTESIAN_POINT('Ctrl Pts',(-1.5197812312985,2.21321803485081,19.3184078906476));
#28033=CARTESIAN_POINT('Ctrl Pts',(-1.58731554407866,2.14533092033585,19.3318190229539));
#28034=CARTESIAN_POINT('Ctrl Pts',(-1.59783038643963,2.1347611480515,19.3339070865807));
#28035=CARTESIAN_POINT('Ctrl Pts',(-1.60826086139227,2.12409664410853,19.3359982059718));
#28036=CARTESIAN_POINT('Ctrl Pts',(-1.61860576158074,2.11333865957609,19.3380924647195));
#28037=CARTESIAN_POINT('Ctrl Pts',(-1.62822431541569,2.10333602528327,19.3400396793027));
#28038=CARTESIAN_POINT('Ctrl Pts',(-1.63776282721144,2.09325885830216,19.341988383369));
#28039=CARTESIAN_POINT('Ctrl Pts',(-1.64721859595761,2.08311066413915,19.343938216497));
#28040=CARTESIAN_POINT('Ctrl Pts',(-1.70843622698655,2.01741019889329,19.3565616391085));
#28041=CARTESIAN_POINT('Ctrl Pts',(-1.766219100483,1.9487041025178,19.3692383719282));
#28042=CARTESIAN_POINT('Ctrl Pts',(-1.82039858689206,1.87731348025079,19.3819900850371));
#28043=CARTESIAN_POINT('Ctrl Pts',(-1.87433752519525,1.80623982073302,19.3946851826143));
#28044=CARTESIAN_POINT('Ctrl Pts',(-1.92470528964026,1.73250442333618,19.407454596158));
#28045=CARTESIAN_POINT('Ctrl Pts',(-1.97128720650435,1.65640691870135,19.4203197083937));
#28046=CARTESIAN_POINT('Ctrl Pts',(-2.01705756114674,1.58163520450376,19.4329606813117));
#28047=CARTESIAN_POINT('Ctrl Pts',(-2.05917296516592,1.50458207736984,19.4456940473948));
#28048=CARTESIAN_POINT('Ctrl Pts',(-2.09738014456683,1.42552910739471,19.4585400911205));
#28049=CARTESIAN_POINT('Ctrl Pts',(-2.1193437171634,1.3800851444472,19.465924698369));
#28050=CARTESIAN_POINT('Ctrl Pts',(-2.14001485636328,1.33398034007164,19.4733465408239));
#28051=CARTESIAN_POINT('Ctrl Pts',(-2.15933758201886,1.28726947129132,19.4808094718297));
#28052=CARTESIAN_POINT('Ctrl Pts',(-2.16497166515239,1.27364960613157,19.4829854988797));
#28053=CARTESIAN_POINT('Ctrl Pts',(-2.17049154787065,1.2599767962587,19.4851652437125));
#28054=CARTESIAN_POINT('Ctrl Pts',(-2.17588921595073,1.2462696637705,19.4873460678037));
#28055=CARTESIAN_POINT('Ctrl Pts',(-2.20705516631138,1.16712515092234,19.4999380713062));
#28056=CARTESIAN_POINT('Ctrl Pts',(-2.23420478857045,1.0867091474059,19.5125864882835));
#28057=CARTESIAN_POINT('Ctrl Pts',(-2.25715829612839,1.0052897707403,19.5253134008472));
#28058=CARTESIAN_POINT('Ctrl Pts',(-2.27976324370209,0.925106786228536,
19.53784704916));
#28059=CARTESIAN_POINT('Ctrl Pts',(-2.29829861115926,0.843949859450999,
19.5504568271743));
#28060=CARTESIAN_POINT('Ctrl Pts',(-2.31254304095193,0.762077696140832,
19.5631638262184));
#28061=CARTESIAN_POINT('Ctrl Pts',(-2.32637402815749,0.682581860946577,
19.5755020063884));
#28062=CARTESIAN_POINT('Ctrl Pts',(-2.33615945602606,0.602411077429613,
19.5879318458378));
#28063=CARTESIAN_POINT('Ctrl Pts',(-2.3416499618205,0.521815068187646,19.6004726521654));
#28064=CARTESIAN_POINT('Ctrl Pts',(-2.34567646704228,0.462709356579674,
19.6096695502389));
#28065=CARTESIAN_POINT('Ctrl Pts',(-2.34739215247365,0.403375179185436,
19.6189261278148));
#28066=CARTESIAN_POINT('Ctrl Pts',(-2.34668236863853,0.34391848339548,19.62825));
#28067=CARTESIAN_POINT('',(-2.14350474087485,2.01162918712768,19.058));
#28068=CARTESIAN_POINT('Origin',(0.,0.,19.058));
#28069=CARTESIAN_POINT('Ctrl Pts',(-2.87001662176841,0.00132468418317613,
19.1339652973708));
#28070=CARTESIAN_POINT('Ctrl Pts',(-2.8730496525982,0.0751001517771462,
19.1313581808297));
#28071=CARTESIAN_POINT('Ctrl Pts',(-2.87305989114646,0.14882755829897,19.1287587900596));
#28072=CARTESIAN_POINT('Ctrl Pts',(-2.86997577113599,0.222349839512856,
19.126165164497));
#28073=CARTESIAN_POINT('Ctrl Pts',(-2.86597654860783,0.317687233114156,
19.1228019731347));
#28074=CARTESIAN_POINT('Ctrl Pts',(-2.85677656440916,0.412680012263468,
19.1194484757843));
#28075=CARTESIAN_POINT('Ctrl Pts',(-2.84265033724356,0.507029984461914,
19.1161003976653));
#28076=CARTESIAN_POINT('Ctrl Pts',(-2.82824071780026,0.603272751757619,
19.1126851523209));
#28077=CARTESIAN_POINT('Ctrl Pts',(-2.80870497678361,0.6988474329182,19.1092755458241));
#28078=CARTESIAN_POINT('Ctrl Pts',(-2.784279579828,0.793434685907145,19.1058670409239));
#28079=CARTESIAN_POINT('Ctrl Pts',(-2.76987697537351,0.849208714624576,
19.1038571924065));
#28080=CARTESIAN_POINT('Ctrl Pts',(-2.75377324450372,0.90463930914618,19.1018477269091));
#28081=CARTESIAN_POINT('Ctrl Pts',(-2.73600874080969,0.959658848626435,
19.0998377142003));
#28082=CARTESIAN_POINT('Ctrl Pts',(-2.72986209641136,0.978695999901232,
19.0991422355328));
#28083=CARTESIAN_POINT('Ctrl Pts',(-2.72351657272334,0.9976839197633,19.0984466913527));
#28084=CARTESIAN_POINT('Ctrl Pts',(-2.71697368591159,1.01661973836998,19.0977510431258));
#28085=CARTESIAN_POINT('Ctrl Pts',(-2.71223360146931,1.03033805289415,19.0972470711891));
#28086=CARTESIAN_POINT('Ctrl Pts',(-2.70738997743942,1.04402867625674,19.0967430566156));
#28087=CARTESIAN_POINT('Ctrl Pts',(-2.70244828698933,1.05767755042078,19.0962394649656));
#28088=CARTESIAN_POINT('Ctrl Pts',(-2.66878296987175,1.15066064632101,19.0928087416602));
#28089=CARTESIAN_POINT('Ctrl Pts',(-2.6305179809939,1.24186163011973,19.0893919514575));
#28090=CARTESIAN_POINT('Ctrl Pts',(-2.58793978625899,1.33096685230041,19.0859846442085));
#28091=CARTESIAN_POINT('Ctrl Pts',(-2.54484291834037,1.42115752419453,19.0825358302938));
#28092=CARTESIAN_POINT('Ctrl Pts',(-2.49732675054846,1.50920190161696,19.0790967317763));
#28093=CARTESIAN_POINT('Ctrl Pts',(-2.4456353402102,1.59476406879245,19.0756627338873));
#28094=CARTESIAN_POINT('Ctrl Pts',(-2.3941166019357,1.68004042066733,19.0722402070628));
#28095=CARTESIAN_POINT('Ctrl Pts',(-2.33844998117206,1.76285193805007,19.068822746847));
#28096=CARTESIAN_POINT('Ctrl Pts',(-2.27883141277619,1.84284311864553,19.065405784563));
#28097=CARTESIAN_POINT('Ctrl Pts',(-2.23576527783441,1.90062563624645,19.062937503912));
#28098=CARTESIAN_POINT('Ctrl Pts',(-2.19063602623153,1.95693605387978,19.0604694830846));
#28099=CARTESIAN_POINT('Ctrl Pts',(-2.14350474087485,2.01162918712768,19.058));
#28100=CARTESIAN_POINT('',(-2.,-2.44929359829471E-16,20.));
#28101=CARTESIAN_POINT('',(-2.5,-3.06161699786838E-16,19.5));
#28102=CARTESIAN_POINT('Origin',(0.,0.,20.));
#28103=CARTESIAN_POINT('Ctrl Pts',(1.70810875200395,-2.39535560853238,-0.329233991005387));
#28104=CARTESIAN_POINT('Ctrl Pts',(2.50223308968789,-1.82907195255014,-0.276469878102161));
#28105=CARTESIAN_POINT('Ctrl Pts',(3.46973755032763,0.145306414888747,-0.170941652295709));
#28106=CARTESIAN_POINT('Ctrl Pts',(1.76544499098352,2.99434248509872,-0.0126493135860318));
#28107=CARTESIAN_POINT('Ctrl Pts',(-1.54740154846188,3.1089951954401,0.145643025123646));
#28108=CARTESIAN_POINT('Ctrl Pts',(-3.45088210452873,0.39789687314801,0.303935363833323));
#28109=CARTESIAN_POINT('Ctrl Pts',(-2.21346936403042,-2.67765081270084,
0.462227702543001));
#28110=CARTESIAN_POINT('Ctrl Pts',(1.03905693981445,-3.31458536367054,0.620520041252677));
#28111=CARTESIAN_POINT('Ctrl Pts',(3.34562773737951,-0.934901086274263,
0.778812379962355));
#28112=CARTESIAN_POINT('Ctrl Pts',(2.60676621014795,2.2961361704366,0.937104718672033));
#28113=CARTESIAN_POINT('Ctrl Pts',(-0.505039165470731,3.43685521821756,
1.09539705738171));
#28114=CARTESIAN_POINT('Ctrl Pts',(-3.15709632883502,1.44912788777876,1.25368939609139));
#28115=CARTESIAN_POINT('Ctrl Pts',(-2.93528897896573,-1.85777219083972,
1.41198173480107));
#28116=CARTESIAN_POINT('Ctrl Pts',(-0.0415132245718345,-3.47353675349846,
1.57027407351074));
#28117=CARTESIAN_POINT('Ctrl Pts',(2.89004928033421,-1.9273884963075,1.72856641222042));
#28118=CARTESIAN_POINT('Ctrl Pts',(3.19083026616817,1.37324872519892,1.8868587509301));
#28119=CARTESIAN_POINT('Ctrl Pts',(0.587029982052427,3.42382799431733,2.04515108963977));
#28120=CARTESIAN_POINT('Ctrl Pts',(-2.55113744546929,2.35773296697854,2.20344342834945));
#28121=CARTESIAN_POINT('Ctrl Pts',(-3.36703034140273,-0.854583572490759,
2.36173576705913));
#28122=CARTESIAN_POINT('Ctrl Pts',(-1.11794935940593,-3.28898079903561,
2.52002810576881));
#28123=CARTESIAN_POINT('Ctrl Pts',(2.14878960983019,-2.72945221239069,2.67832044447848));
#28124=CARTESIAN_POINT('Ctrl Pts',(3.45950707796974,0.314669352524756,2.83661278318816));
#28125=CARTESIAN_POINT('Ctrl Pts',(1.6210701051072,3.072350505369,2.99490512189784));
#28126=CARTESIAN_POINT('Ctrl Pts',(-1.69301064028636,3.0333019941398,3.15319746060751));
#28127=CARTESIAN_POINT('Ctrl Pts',(-3.46596086572504,0.233069227837938,
3.3114897993172));
#28128=CARTESIAN_POINT('Ctrl Pts',(-2.08388184344624,-2.77932409737199,
3.46978213802687));
#28129=CARTESIAN_POINT('Ctrl Pts',(1.19513381840354,-3.26172671239436,3.62807447673655));
#28130=CARTESIAN_POINT('Ctrl Pts',(3.38623121053353,-0.775012370246788,
3.78636681544623));
#28131=CARTESIAN_POINT('Ctrl Pts',(2.49487645815869,2.41718792041892,3.9446591541559));
#28132=CARTESIAN_POINT('Ctrl Pts',(-0.667539190367716,3.40904640851925,
4.10295149286558));
#28133=CARTESIAN_POINT('Ctrl Pts',(-3.22230064149105,1.29768430718665,4.26124383157526));
#28134=CARTESIAN_POINT('Ctrl Pts',(-2.84383429323506,-1.99494674059711,
4.41953617028494));
#28135=CARTESIAN_POINT('Ctrl Pts',(0.123345751738387,-3.47159787576266,
4.57782850899461));
#28136=CARTESIAN_POINT('Ctrl Pts',(2.97824540200357,-1.78808845160989,4.73612084770429));
#28137=CARTESIAN_POINT('Ctrl Pts',(3.12207827781955,1.52309986951151,4.89441318641397));
#28138=CARTESIAN_POINT('Ctrl Pts',(0.42391476189898,3.44782572935734,5.05270552512364));
#28139=CARTESIAN_POINT('Ctrl Pts',(-2.66013408953218,2.2340305752299,5.21099786383333));
#28140=CARTESIAN_POINT('Ctrl Pts',(-3.32268968830985,-1.01338009678248,
5.36929020254299));
#28141=CARTESIAN_POINT('Ctrl Pts',(-0.960634350157316,-3.33832107962339,
5.52758254125269));
#28142=CARTESIAN_POINT('Ctrl Pts',(2.27587675559227,-2.62442202755419,5.68587487996235));
#28143=CARTESIAN_POINT('Ctrl Pts',(3.44068018719777,0.478461947057601,5.84416721867204));
#28144=CARTESIAN_POINT('Ctrl Pts',(1.47346711985291,3.14580683324172,6.0024595573817));
#28145=CARTESIAN_POINT('Ctrl Pts',(-1.8350282169722,2.94955546282373,6.1607518960914));
#28146=CARTESIAN_POINT('Ctrl Pts',(-3.47311586145163,0.0683534804580524,
6.31904423480106));
#28147=CARTESIAN_POINT('Ctrl Pts',(-1.94966113959674,-2.87506998629669,
6.47733657351074));
#28148=CARTESIAN_POINT('Ctrl Pts',(1.34855046878899,-3.20134621971548,6.63562891222042));
#28149=CARTESIAN_POINT('Ctrl Pts',(3.41919017623777,-0.61346925275575,6.7939212509301));
#28150=CARTESIAN_POINT('Ctrl Pts',(2.37737552513495,2.53284259239435,6.95221358963977));
#28151=CARTESIAN_POINT('Ctrl Pts',(-0.828540107113662,3.37353335188222,
7.11050592834946));
#28152=CARTESIAN_POINT('Ctrl Pts',(-3.28024402995153,1.14333069989614,7.26879826705912));
#28153=CARTESIAN_POINT('Ctrl Pts',(-2.74597487089154,-2.12763436562531,
7.42709060576881));
#28154=CARTESIAN_POINT('Ctrl Pts',(0.287927538982181,-3.46183531059079,
7.58538294447848));
#28155=CARTESIAN_POINT('Ctrl Pts',(3.05973241187765,-1.64476246098426,7.74367528318817));
#28156=CARTESIAN_POINT('Ctrl Pts',(3.04629370647385,1.66952108080595,7.90196762189784));
#28157=CARTESIAN_POINT('Ctrl Pts',(0.259844540863475,3.46405640830819,8.06025996060752));
#28158=CARTESIAN_POINT('Ctrl Pts',(-2.76313849156042,2.10529609837068,8.21855229931719));
#28159=CARTESIAN_POINT('Ctrl Pts',(-3.27086440225209,-1.16989403256776,
8.37684463802688));
#28160=CARTESIAN_POINT('Ctrl Pts',(-0.801155411612067,-3.38014141594732,
8.53513697673654));
#28161=CARTESIAN_POINT('Ctrl Pts',(2.39783727610882,-2.51348013373106,8.69342931544623));
#28162=CARTESIAN_POINT('Ctrl Pts',(3.41410285698758,0.641176783162679,8.8517216541559));
#28163=CARTESIAN_POINT('Ctrl Pts',(1.32254501475776,3.21217693617538,9.01001399286559));
#28164=CARTESIAN_POINT('Ctrl Pts',(-1.97291222568947,2.85916479676892,9.16830633157525));
#28165=CARTESIAN_POINT('Ctrl Pts',(-3.47244735026198,-0.0965162422401203,
9.32659867028495));
#28166=CARTESIAN_POINT('Ctrl Pts',(-1.81104864749881,-2.96433951863654,
9.4848910089946));
#28167=CARTESIAN_POINT('Ctrl Pts',(1.49892938718647,-3.13375440607372,9.6431833477043));
#28168=CARTESIAN_POINT('Ctrl Pts',(3.44444710704859,-0.45054423989462,9.80147568641397));
#28169=CARTESIAN_POINT('Ctrl Pts',(2.25451933878342,2.64279180723891,9.95976802512365));
#28170=CARTESIAN_POINT('Ctrl Pts',(-0.987674662346407,3.3304211065144,10.1180603638333));
#28171=CARTESIAN_POINT('Ctrl Pts',(-3.33079837220816,0.986401636785503,
10.276352702543));
#28172=CARTESIAN_POINT('Ctrl Pts',(-2.64192989190662,-2.25552930187303,
10.4346450412527));
#28173=CARTESIAN_POINT('Ctrl Pts',(0.45186074341242,-3.44427464844491,10.5929373799624));
#28174=CARTESIAN_POINT('Ctrl Pts',(3.13432709789262,-1.49773149421841,10.751229718672));
#28175=CARTESIAN_POINT('Ctrl Pts',(2.96364708316543,1.81218154493491,10.9095220573817));
#28176=CARTESIAN_POINT('Ctrl Pts',(0.0951889965099087,3.47248398704746,
11.0678143960914));
#28177=CARTESIAN_POINT('Ctrl Pts',(-2.85991867434608,1.97181925172773,11.2261067348011));
#28178=CARTESIAN_POINT('Ctrl Pts',(-3.21167119843867,-1.32377267628441,
11.3843990735108));
#28179=CARTESIAN_POINT('Ctrl Pts',(-0.639871798076946,-3.41434767816393,
11.5426914122204));
#28180=CARTESIAN_POINT('Ctrl Pts',(2.514396451394,-2.39687639868534,11.7009837509301));
#28181=CARTESIAN_POINT('Ctrl Pts',(3.37983495145364,0.802447310600554,11.8592760896398));
#28182=CARTESIAN_POINT('Ctrl Pts',(1.16864375745746,3.27131132017627,12.0175684283495));
#28183=CARTESIAN_POINT('Ctrl Pts',(-2.10635207126507,2.76233360353794,12.1758607670591));
#28184=CARTESIAN_POINT('Ctrl Pts',(-3.46395683750307,-0.261168553377433,
12.3341531057688));
#28185=CARTESIAN_POINT('Ctrl Pts',(-1.66835660460176,-3.04693160823137,
12.4924454444785));
#28186=CARTESIAN_POINT('Ctrl Pts',(1.64593183163456,-3.05910352733767,12.6507377831882));
#28187=CARTESIAN_POINT('Ctrl Pts',(3.4619451093692,-0.286604335403503,12.8090301218978));
#28188=CARTESIAN_POINT('Ctrl Pts',(2.1265846438105,2.74678789462661,12.9673224606075));
#28189=CARTESIAN_POINT('Ctrl Pts',(-1.14458439111546,3.27980678653062,13.1256147993172));
#28190=CARTESIAN_POINT('Ctrl Pts',(-3.37384979002366,0.827250614816437,
13.2839071380269));
#28191=CARTESIAN_POINT('Ctrl Pts',(-2.53193372700732,-2.37834345446631,
13.4421994767365));
#28192=CARTESIAN_POINT('Ctrl Pts',(0.614776090670012,-3.41895544628708,
13.6004918154462));
#28193=CARTESIAN_POINT('Ctrl Pts',(3.20186142877222,-1.34732675186611,13.7587841541559));
#28194=CARTESIAN_POINT('Ctrl Pts',(2.87432457688735,1.95075990631232,13.9170764928656));
#28195=CARTESIAN_POINT('Ctrl Pts',(-0.0696809696671145,3.47308948168699,
14.0753688315753));
#28196=CARTESIAN_POINT('Ctrl Pts',(-2.95025663177125,1.83390070397115,14.2336611702849));
#28197=CARTESIAN_POINT('Ctrl Pts',(-3.14524341492572,-1.47466940238759,
14.3919535089946));
#28198=CARTESIAN_POINT('Ctrl Pts',(-0.477146815446115,-3.44086281355539,
14.5502458477043));
#28199=CARTESIAN_POINT('Ctrl Pts',(2.62529172131977,-2.27487348290887,14.708538186414));
#28200=CARTESIAN_POINT('Ctrl Pts',(3.33795366224388,0.961910253000547,14.8668305251236));
#28201=CARTESIAN_POINT('Ctrl Pts',(1.01211002426958,3.32307677956238,15.0251228638333));
#28202=CARTESIAN_POINT('Ctrl Pts',(-2.23504716804512,2.65928000440727,15.183415202543));
#28203=CARTESIAN_POINT('Ctrl Pts',(-3.44766344946911,-0.425232559234952,
15.3417075412527));
#28204=CARTESIAN_POINT('Ctrl Pts',(-1.52190643639689,-3.12266020798474,
15.4999998799623));
#28205=CARTESIAN_POINT('Ctrl Pts',(1.78922666348011,-2.97756174317077,15.658292218672));
#28206=CARTESIAN_POINT('Ctrl Pts',(3.47164477187003,-0.122018825280182,
15.8165845573817));
#28207=CARTESIAN_POINT('Ctrl Pts',(1.99385961608439,2.84459658736723,15.9748768960914));
#28208=CARTESIAN_POINT('Ctrl Pts',(-1.29891582365465,3.22180441786908,16.1331692348011));
#28209=CARTESIAN_POINT('Ctrl Pts',(-3.40930133753709,0.666236111980054,
16.2914615735107));
#28210=CARTESIAN_POINT('Ctrl Pts',(-2.4162340926357,-2.49580012745533,16.4497539122204));
#28211=CARTESIAN_POINT('Ctrl Pts',(0.776306484896849,-3.3859348256877,16.6080462509301));
#28212=CARTESIAN_POINT('Ctrl Pts',(3.26218349561107,-1.19388686658981,16.7663385896398));
#28213=CARTESIAN_POINT('Ctrl Pts',(2.77852697784647,2.08494368458209,16.9246309283494));
#28214=CARTESIAN_POINT('Ctrl Pts',(-0.234393177244862,3.46587213947896,
17.0829232670591));
#28215=CARTESIAN_POINT('Ctrl Pts',(-3.03395038925589,1.69184996202172,17.2412156057688));
#28216=CARTESIAN_POINT('Ctrl Pts',(-3.0717277841222,-1.62224207378881,17.3995079444785));
#28217=CARTESIAN_POINT('Ctrl Pts',(-0.313352558263224,-3.45963134991648,
17.5578002831882));
#28218=CARTESIAN_POINT('Ctrl Pts',(2.73028386654254,-2.14773808290938,17.7160926218978));
#28219=CARTESIAN_POINT('Ctrl Pts',(3.28853312351893,1.11919088861887,17.8743849606075));
#28220=CARTESIAN_POINT('Ctrl Pts',(0.853335008049955,3.36738633833314,18.0326772993172));
#28221=CARTESIAN_POINT('Ctrl Pts',(-2.35878130152261,2.55017955638957,18.1909696380269));
#28222=CARTESIAN_POINT('Ctrl Pts',(-3.42346318292819,-0.58823064555564,
18.3492619767365));
#28223=CARTESIAN_POINT('Ctrl Pts',(-1.3722967672463,-3.19156107302743,18.5075543154462));
#28224=CARTESIAN_POINT('Ctrl Pts',(1.92900469321343,-2.88891850258502,18.6658466541559));
#28225=CARTESIAN_POINT('Ctrl Pts',(3.47253961472093,0.0420868345896532,
18.8241389928656));
#28226=CARTESIAN_POINT('Ctrl Pts',(1.85855788388951,2.93745562119467,18.9824313315753));
#28227=CARTESIAN_POINT('Ctrl Pts',(-1.45428025938601,3.15361087477854,19.1407236702849));
#28228=CARTESIAN_POINT('Ctrl Pts',(-2.76947321735942,1.39165108452637,19.2462518960914));
#28229=CARTESIAN_POINT('Ctrl Pts',(-2.91090525077877,0.426608275808834,
19.2990160089946));
#28230=CARTESIAN_POINT('Ctrl Pts',(1.59774743137964,-2.24059110187414,-0.219489327336925));
#28231=CARTESIAN_POINT('Ctrl Pts',(2.34056320305811,-1.71089517020912,-0.1667252144337));
#28232=CARTESIAN_POINT('Ctrl Pts',(3.24555696590951,0.135918132191012,-0.0611969886272476));
#28233=CARTESIAN_POINT('Ctrl Pts',(1.65137916205666,2.80087729111192,0.0970953500824295));
#28234=CARTESIAN_POINT('Ctrl Pts',(-1.44742355922437,2.90812226203881,0.255387688792107));
#28235=CARTESIAN_POINT('Ctrl Pts',(-3.22791977503548,0.372188659697663,
0.413680027501785));
#28236=CARTESIAN_POINT('Ctrl Pts',(-2.07045657173057,-2.50464714445445,
0.571972366211461));
#28237=CARTESIAN_POINT('Ctrl Pts',(0.971923218997645,-3.10042919965138,
0.73026470492114));
#28238=CARTESIAN_POINT('Ctrl Pts',(3.12946591806831,-0.874496900408864,
0.888557043630815));
#28239=CARTESIAN_POINT('Ctrl Pts',(2.43834241325956,2.14778225573103,1.0468493823405));
#28240=CARTESIAN_POINT('Ctrl Pts',(-0.472408462535135,3.2147991692499,1.20514172105017));
#28241=CARTESIAN_POINT('Ctrl Pts',(-2.95311556954223,1.35549938358592,1.36343405975985));
#28242=CARTESIAN_POINT('Ctrl Pts',(-2.7456392463286,-1.73774107914402,1.52172639846952));
#28243=CARTESIAN_POINT('Ctrl Pts',(-0.0388310450667128,-3.24911070164229,
1.68001873717921));
#28244=CARTESIAN_POINT('Ctrl Pts',(2.70332249559475,-1.80285945823596,1.83831107588888));
#28245=CARTESIAN_POINT('Ctrl Pts',(2.98466994900496,1.28452279209847,1.99660341459856));
#28246=CARTESIAN_POINT('Ctrl Pts',(0.549101832577521,3.20261363744452,2.15489575330824));
#28247=CARTESIAN_POINT('Ctrl Pts',(-2.38630783655485,2.20539926831328,2.31318809201791));
#28248=CARTESIAN_POINT('Ctrl Pts',(-3.1494856946562,-0.799368720665158,
2.47148043072759));
#28249=CARTESIAN_POINT('Ctrl Pts',(-1.04571838023061,-3.07647895214574,
2.62977276943727));
#28250=CARTESIAN_POINT('Ctrl Pts',(2.00995579213185,-2.55310164315028,2.78806510814695));
#28251=CARTESIAN_POINT('Ctrl Pts',(3.2359874868512,0.2943384893617,2.94635744685662));
#28252=CARTESIAN_POINT('Ctrl Pts',(1.51633237256273,2.87384519427829,3.1046497855663));
#28253=CARTESIAN_POINT('Ctrl Pts',(-1.58362481232089,2.83731961682751,3.26294212427598));
#28254=CARTESIAN_POINT('Ctrl Pts',(-3.24202429381481,0.218010568516082,
3.42123446298566));
#28255=CARTESIAN_POINT('Ctrl Pts',(-1.94924173227183,-2.59975129355074,
3.57952680169533));
#28256=CARTESIAN_POINT('Ctrl Pts',(1.11791593261785,-3.05098575865054,3.73781914040501));
#28257=CARTESIAN_POINT('Ctrl Pts',(3.16744599097691,-0.724938633091413,
3.89611147911469));
#28258=CARTESIAN_POINT('Ctrl Pts',(2.33368188527572,2.26101282279612,4.05440381782437));
#28259=CARTESIAN_POINT('Ctrl Pts',(-0.624409321422887,3.18878709348887,
4.21269615653404));
#28260=CARTESIAN_POINT('Ctrl Pts',(-3.01410701574777,1.21384060945571,4.37098849524372));
#28261=CARTESIAN_POINT('Ctrl Pts',(-2.66009347001759,-1.8660527479815,4.5292808339534));
#28262=CARTESIAN_POINT('Ctrl Pts',(0.115376352811499,-3.24729709526712,
4.68757317266307));
#28263=CARTESIAN_POINT('Ctrl Pts',(2.78582024445854,-1.6725596232017,4.84586551137275));
#28264=CARTESIAN_POINT('Ctrl Pts',(2.92036004329352,1.42469201764329,5.00415785008243));
#28265=CARTESIAN_POINT('Ctrl Pts',(0.396525526347995,3.22506087300498,5.16245018879211));
#28266=CARTESIAN_POINT('Ctrl Pts',(-2.48826218101693,2.08968931808907,5.32074252750178));
#28267=CARTESIAN_POINT('Ctrl Pts',(-3.10800990191072,-0.947905363019727,
5.47903486621146));
#28268=CARTESIAN_POINT('Ctrl Pts',(-0.898567531873009,-3.12263134524142,
5.63732720492114));
#28269=CARTESIAN_POINT('Ctrl Pts',(2.12883180659201,-2.45485748402225,5.79561954363082));
#28270=CARTESIAN_POINT('Ctrl Pts',(3.21837700605687,0.447548404647735,5.9539118823405));
#28271=CARTESIAN_POINT('Ctrl Pts',(1.37826605197434,2.94255549099653,6.11220422105017));
#28272=CARTESIAN_POINT('Ctrl Pts',(-1.71646659894271,2.75898396920541,6.27049655975985));
#28273=CARTESIAN_POINT('Ctrl Pts',(-3.24871700353266,0.063937145512284,
6.42878889846952));
#28274=CARTESIAN_POINT('Ctrl Pts',(-1.82369306064193,-2.68931101737694,
6.58708123717921));
#28275=CARTESIAN_POINT('Ctrl Pts',(1.26142029602366,-2.99450646424383,6.74537357588887));
#28276=CARTESIAN_POINT('Ctrl Pts',(3.1982754699156,-0.573832855590093,6.90366591459857));
#28277=CARTESIAN_POINT('Ctrl Pts',(2.22377271602456,2.36919501837296,7.06195825330823));
#28278=CARTESIAN_POINT('Ctrl Pts',(-0.775007929900716,3.15556854405185,
7.22025059201791));
#28279=CARTESIAN_POINT('Ctrl Pts',(-3.06830666783054,1.06945982615765,7.37854293072759));
#28280=CARTESIAN_POINT('Ctrl Pts',(-2.56855676867922,-1.99016739338446,
7.53683526943726));
#28281=CARTESIAN_POINT('Ctrl Pts',(0.269324470876077,-3.23816529179809,
7.69512760814696));
#28282=CARTESIAN_POINT('Ctrl Pts',(2.86204235886687,-1.53849395958199,7.85341994685661));
#28283=CARTESIAN_POINT('Ctrl Pts',(2.84947193147761,1.56165291897392,8.01171228556631));
#28284=CARTESIAN_POINT('Ctrl Pts',(0.243055922074948,3.24024288385343,8.17000462427597));
#28285=CARTESIAN_POINT('Ctrl Pts',(-2.5846114436551,1.96927240699339,8.32829696298566));
#28286=CARTESIAN_POINT('Ctrl Pts',(-3.059533060151,-1.0943068954647,8.48658930169534));
#28287=CARTESIAN_POINT('Ctrl Pts',(-0.749392566215293,-3.16174965949548,
8.64488164040499));
#28288=CARTESIAN_POINT('Ctrl Pts',(2.24291242830675,-2.35108357285861,8.8031739791147));
#28289=CARTESIAN_POINT('Ctrl Pts',(3.19351684359565,0.59975019573934,8.96146631782435));
#28290=CARTESIAN_POINT('Ctrl Pts',(1.23709506068279,3.00463740548719,9.11975865653406));
#28291=CARTESIAN_POINT('Ctrl Pts',(-1.84544188842464,2.67443346600101,9.27805099524372));
#28292=CARTESIAN_POINT('Ctrl Pts',(-3.24809168501307,-0.0902803044271455,
9.4363433339534));
#28293=CARTESIAN_POINT('Ctrl Pts',(-1.69403635526719,-2.77281282358755,
9.59463567266307));
#28294=CARTESIAN_POINT('Ctrl Pts',(1.40208319604178,-2.93128177407014,9.75292801137276));
#28295=CARTESIAN_POINT('Ctrl Pts',(3.22190054430279,-0.421434467313608,
9.91122035008243));
#28296=CARTESIAN_POINT('Ctrl Pts',(2.10885429766158,2.47204038778753,10.0695126887921));
#28297=CARTESIAN_POINT('Ctrl Pts',(-0.923860762935242,3.11524179131047,
10.2278050275018));
#28298=CARTESIAN_POINT('Ctrl Pts',(-3.1155946817763,0.922669987864471,10.3860973662115));
#28299=CARTESIAN_POINT('Ctrl Pts',(-2.47123416101382,-2.10979900679111,
10.5443897049211));
#28300=CARTESIAN_POINT('Ctrl Pts',(0.422665911219942,-3.2217392282913,10.7026820436308));
#28301=CARTESIAN_POINT('Ctrl Pts',(2.93181746413178,-1.40096269922882,10.8609743823405));
#28302=CARTESIAN_POINT('Ctrl Pts',(2.7721651265401,1.69509605592528,11.0192667210502));
#28303=CARTESIAN_POINT('Ctrl Pts',(0.0890388123653499,3.24812595468695,
11.1775590597599));
#28304=CARTESIAN_POINT('Ctrl Pts',(-2.67513863536514,1.84441953177557,11.3358513984695));
#28305=CARTESIAN_POINT('Ctrl Pts',(-3.00416434358826,-1.23824340270056,
11.4941437371792));
#28306=CARTESIAN_POINT('Ctrl Pts',(-0.598529526056383,-3.19374584681644,
11.6524360758889));
#28307=CARTESIAN_POINT('Ctrl Pts',(2.35194068701519,-2.24201363340657,11.8107284145986));
#28308=CARTESIAN_POINT('Ctrl Pts',(3.16146299574704,0.750600995296923,11.9690207533082));
#28309=CARTESIAN_POINT('Ctrl Pts',(1.0931374009324,3.05995110259973,12.1273130920179));
#28310=CARTESIAN_POINT('Ctrl Pts',(-1.97026015322306,2.58385855964291,12.2856054307276));
#28311=CARTESIAN_POINT('Ctrl Pts',(-3.24014974634217,-0.244294389819381,
12.4438977694372));
#28312=CARTESIAN_POINT('Ctrl Pts',(-1.56056367985961,-2.85006861824793,
12.602190108147));
#28313=CARTESIAN_POINT('Ctrl Pts',(1.53958777691108,-2.86145410670948,12.7604824468566));
#28314=CARTESIAN_POINT('Ctrl Pts',(3.23826799645081,-0.268086759801421,
12.9187747855663));
#28315=CARTESIAN_POINT('Ctrl Pts',(1.9891854943506,2.56931726275365,13.077067124276));
#28316=CARTESIAN_POINT('Ctrl Pts',(-1.07063251608334,3.06789767481307,13.2353594629857));
#28317=CARTESIAN_POINT('Ctrl Pts',(-3.15586453704825,0.773801752013446,
13.3936518016953));
#28318=CARTESIAN_POINT('Ctrl Pts',(-2.36834487499894,-2.22467810720716,
13.551944140405));
#28319=CARTESIAN_POINT('Ctrl Pts',(0.57505525838988,-3.19805590592392,13.7102364791147));
#28320=CARTESIAN_POINT('Ctrl Pts',(2.9949883855185,-1.26027564374785,13.8685288178244));
#28321=CARTESIAN_POINT('Ctrl Pts',(2.68861376905027,1.82472083577363,14.0268211565341));
#28322=CARTESIAN_POINT('Ctrl Pts',(-0.065178865321708,3.24869232817101,
14.1851134952437));
#28323=CARTESIAN_POINT('Ctrl Pts',(-2.75963983545724,1.71541193483002,14.3434058339534));
#28324=CARTESIAN_POINT('Ctrl Pts',(-2.94202847527452,-1.37939065474297,
14.5016981726631));
#28325=CARTESIAN_POINT('Ctrl Pts',(-0.446318244008518,-3.21854783288125,
14.6599905113728));
#28326=CARTESIAN_POINT('Ctrl Pts',(2.4556709866628,-2.12789335559991,14.8182828500824));
#28327=CARTESIAN_POINT('Ctrl Pts',(3.12228766678788,0.899760998324197,14.9765751887921));
#28328=CARTESIAN_POINT('Ctrl Pts',(0.946717350199806,3.10837198310357,15.1348675275018));
#28329=CARTESIAN_POINT('Ctrl Pts',(-2.09064022859603,2.48746327853901,15.2931598662115));
#28330=CARTESIAN_POINT('Ctrl Pts',(-3.22490907805967,-0.397758180478594,
15.4514522049212));
#28331=CARTESIAN_POINT('Ctrl Pts',(-1.42357569253155,-2.92090437480966,
15.6097445436308));
#28332=CARTESIAN_POINT('Ctrl Pts',(1.67362429492704,-2.78518075698867,15.7680368823405));
#28333=CARTESIAN_POINT('Ctrl Pts',(3.24734096140562,-0.114135159393468,
15.9263292210501));
#28334=CARTESIAN_POINT('Ctrl Pts',(1.86503586284711,2.66080651214107,16.0846215597599));
#28335=CARTESIAN_POINT('Ctrl Pts',(-1.21499255734613,3.01364285325432,16.2429138984695));
#28336=CARTESIAN_POINT('Ctrl Pts',(-3.18902555148107,0.623190435245776,
16.4012062371792));
#28337=CARTESIAN_POINT('Ctrl Pts',(-2.26012062205723,-2.33454587607517,
16.5594985758889));
#28338=CARTESIAN_POINT('Ctrl Pts',(0.726149134680179,-3.16716875562783,
16.7177909145985));
#28339=CARTESIAN_POINT('Ctrl Pts',(3.05141302899288,-1.11674954666312,16.8760832533082));
#28340=CARTESIAN_POINT('Ctrl Pts',(2.59900567611102,1.95023496759446,17.0343755920179));
#28341=CARTESIAN_POINT('Ctrl Pts',(-0.219248977230838,3.24194130019299,
17.1926679307276));
#28342=CARTESIAN_POINT('Ctrl Pts',(-2.83792611897795,1.58253912576034,17.3509602694372));
#28343=CARTESIAN_POINT('Ctrl Pts',(-2.87326270720222,-1.51742862006368,
17.509252608147));
#28344=CARTESIAN_POINT('Ctrl Pts',(-0.293106773496658,-3.23610372955733,
17.6675449468566));
#28345=CARTESIAN_POINT('Ctrl Pts',(2.55387956392575,-2.00897220462033,17.8258372855663));
#28346=CARTESIAN_POINT('Ctrl Pts',(3.07606020105273,1.04687969394011,17.984129624276));
#28347=CARTESIAN_POINT('Ctrl Pts',(0.798200826275583,3.14981869053862,18.1424219629856));
#28348=CARTESIAN_POINT('Ctrl Pts',(-2.20637986970829,2.38541183692082,18.3007143016953));
#28349=CARTESIAN_POINT('Ctrl Pts',(-3.20227239660768,-0.5502249209207,18.459006640405));
#28350=CARTESIAN_POINT('Ctrl Pts',(-1.28363234037996,-2.98535353825586,
18.6172989791147));
#28351=CARTESIAN_POINT('Ctrl Pts',(1.80437123226795,-2.70226477767009,18.7755913178244));
#28352=CARTESIAN_POINT('Ctrl Pts',(3.24817798824295,0.0393675940022248,
18.9338836565341));
#28353=CARTESIAN_POINT('Ctrl Pts',(1.73847600837534,2.74766590127781,19.0921759952437));
#28354=CARTESIAN_POINT('Ctrl Pts',(-1.36031885921439,2.94985531151743,19.2504683339534));
#28355=CARTESIAN_POINT('Ctrl Pts',(-2.59053688128428,1.30173617052782,19.3559965597598));
#28356=CARTESIAN_POINT('Ctrl Pts',(-2.72283095673202,0.399045011671049,
19.4087606726631));
#28357=CARTESIAN_POINT('Ctrl Pts',(1.48738611075532,-2.08582659521589,-0.109744663668464));
#28358=CARTESIAN_POINT('Ctrl Pts',(2.17889331642833,-1.5927183878681,-0.0569805507652379));
#28359=CARTESIAN_POINT('Ctrl Pts',(3.02137638149139,0.12652984949328,0.0485476750412134));
#28360=CARTESIAN_POINT('Ctrl Pts',(1.5373133331298,2.60741209712512,0.206840013750891));
#28361=CARTESIAN_POINT('Ctrl Pts',(-1.34744556998685,2.70724932863752,0.365132352460568));
#28362=CARTESIAN_POINT('Ctrl Pts',(-3.00495744554222,0.346480446247313,
0.523424691170246));
#28363=CARTESIAN_POINT('Ctrl Pts',(-1.92744377943072,-2.33164347620807,
0.681717029879923));
#28364=CARTESIAN_POINT('Ctrl Pts',(0.904789498180845,-2.88627303563221,
0.8400093685896));
#28365=CARTESIAN_POINT('Ctrl Pts',(2.91330409875712,-0.814092714543464,
0.998301707299278));
#28366=CARTESIAN_POINT('Ctrl Pts',(2.26991861637116,1.99942834102545,1.15659404600895));
#28367=CARTESIAN_POINT('Ctrl Pts',(-0.439777759599539,2.99274312028224,
1.31488638471863));
#28368=CARTESIAN_POINT('Ctrl Pts',(-2.74913481024945,1.26187087939309,1.47317872342831));
#28369=CARTESIAN_POINT('Ctrl Pts',(-2.55598951369148,-1.61770996744832,
1.63147106213799));
#28370=CARTESIAN_POINT('Ctrl Pts',(-0.0361488655615895,-3.02468464978613,
1.78976340084767));
#28371=CARTESIAN_POINT('Ctrl Pts',(2.51659571085528,-1.67833042016441,1.94805573955734));
#28372=CARTESIAN_POINT('Ctrl Pts',(2.77850963184176,1.19579685899802,2.10634807826702));
#28373=CARTESIAN_POINT('Ctrl Pts',(0.511173683102615,2.9813992805717,2.26464041697669));
#28374=CARTESIAN_POINT('Ctrl Pts',(-2.22147822764042,2.05306556964801,2.42293275568638));
#28375=CARTESIAN_POINT('Ctrl Pts',(-2.93194104790966,-0.744153868839558,
2.58122509439605));
#28376=CARTESIAN_POINT('Ctrl Pts',(-0.973487401055298,-2.86397710525587,
2.73951743310573));
#28377=CARTESIAN_POINT('Ctrl Pts',(1.87112197443351,-2.37675107390986,2.8978097718154));
#28378=CARTESIAN_POINT('Ctrl Pts',(3.01246789573266,0.274007626198644,3.05610211052509));
#28379=CARTESIAN_POINT('Ctrl Pts',(1.41159464001826,2.67533988318758,3.21439444923477));
#28380=CARTESIAN_POINT('Ctrl Pts',(-1.47423898435543,2.64133723951521,3.37268678794443));
#28381=CARTESIAN_POINT('Ctrl Pts',(-3.01808772190458,0.202951909194227,
3.53097912665412));
#28382=CARTESIAN_POINT('Ctrl Pts',(-1.81460162109742,-2.4201784897295,3.68927146536379));
#28383=CARTESIAN_POINT('Ctrl Pts',(1.04069804683216,-2.84024480490672,3.84756380407347));
#28384=CARTESIAN_POINT('Ctrl Pts',(2.94866077142029,-0.674864895936037,
4.00585614278315));
#28385=CARTESIAN_POINT('Ctrl Pts',(2.17248731239275,2.10483772517333,4.16414848149283));
#28386=CARTESIAN_POINT('Ctrl Pts',(-0.581279452478057,2.96852777845849,
4.3224408202025));
#28387=CARTESIAN_POINT('Ctrl Pts',(-2.80591339000449,1.12999691172477,4.48073315891218));
#28388=CARTESIAN_POINT('Ctrl Pts',(-2.47635264680012,-1.73715875536589,
4.63902549762186));
#28389=CARTESIAN_POINT('Ctrl Pts',(0.107406953884614,-3.02299631477157,
4.79731783633154));
#28390=CARTESIAN_POINT('Ctrl Pts',(2.5933950869135,-1.55703079479352,4.95561017504121));
#28391=CARTESIAN_POINT('Ctrl Pts',(2.71864180876751,1.32628416577508,5.1139025137509));
#28392=CARTESIAN_POINT('Ctrl Pts',(0.369136290797007,3.0022960166526,5.27219485246056));
#28393=CARTESIAN_POINT('Ctrl Pts',(-2.31639027250168,1.94534806094824,5.43048719117025));
#28394=CARTESIAN_POINT('Ctrl Pts',(-2.89333011551159,-0.88243062925697,
5.58877952987992));
#28395=CARTESIAN_POINT('Ctrl Pts',(-0.836500713588696,-2.90694161085946,
5.7470718685896));
#28396=CARTESIAN_POINT('Ctrl Pts',(1.98178685759173,-2.28529294049032,5.90536420729928));
#28397=CARTESIAN_POINT('Ctrl Pts',(2.99607382491597,0.416634862237868,6.06365654600896));
#28398=CARTESIAN_POINT('Ctrl Pts',(1.28306498409578,2.73930414875135,6.22194888471863));
#28399=CARTESIAN_POINT('Ctrl Pts',(-1.59790498091322,2.56841247558709,6.38024122342832));
#28400=CARTESIAN_POINT('Ctrl Pts',(-3.0243181456137,0.0595208105665224,
6.53853356213798));
#28401=CARTESIAN_POINT('Ctrl Pts',(-1.69772498168712,-2.50355204845721,
6.69682590084767));
#28402=CARTESIAN_POINT('Ctrl Pts',(1.17429012325833,-2.78766670877218,6.85511823955734));
#28403=CARTESIAN_POINT('Ctrl Pts',(2.97736076359342,-0.534196458424437,
7.01341057826702));
#28404=CARTESIAN_POINT('Ctrl Pts',(2.07016990691417,2.20554744435157,7.1717029169767));
#28405=CARTESIAN_POINT('Ctrl Pts',(-0.721475752687772,2.93760373622148,
7.32999525568637));
#28406=CARTESIAN_POINT('Ctrl Pts',(-2.85636930570956,0.995588952419164,
7.48828759439606));
#28407=CARTESIAN_POINT('Ctrl Pts',(-2.39113866646689,-1.85270042114361,
7.64657993310571));
#28408=CARTESIAN_POINT('Ctrl Pts',(0.250721402769973,-3.01449527300539,
7.80487227181542));
#28409=CARTESIAN_POINT('Ctrl Pts',(2.66435230585608,-1.43222545817973,7.96316461052508));
#28410=CARTESIAN_POINT('Ctrl Pts',(2.65265015648138,1.45378475714189,8.12145694923476));
#28411=CARTESIAN_POINT('Ctrl Pts',(0.226267303286426,3.01642935939867,8.27974928794444));
#28412=CARTESIAN_POINT('Ctrl Pts',(-2.4060843957498,1.83324871561609,8.43804162665412));
#28413=CARTESIAN_POINT('Ctrl Pts',(-2.8482017180499,-1.01871975836163,8.59633396536379));
#28414=CARTESIAN_POINT('Ctrl Pts',(-0.697629720818526,-2.94335790304364,
8.75462630407348));
#28415=CARTESIAN_POINT('Ctrl Pts',(2.0879875805047,-2.18868701198616,8.91291864278314));
#28416=CARTESIAN_POINT('Ctrl Pts',(2.97293083020372,0.558323608315999,9.07121098149283));
#28417=CARTESIAN_POINT('Ctrl Pts',(1.15164510660782,2.797097874799,9.2295033202025));
#28418=CARTESIAN_POINT('Ctrl Pts',(-1.71797155115982,2.4897021352331,9.38779565891218));
#28419=CARTESIAN_POINT('Ctrl Pts',(-3.02373601976415,-0.0840443666141708,
9.54608799762186));
#28420=CARTESIAN_POINT('Ctrl Pts',(-1.57702406303557,-2.58128612853855,
9.70438033633154));
#28421=CARTESIAN_POINT('Ctrl Pts',(1.3052370048971,-2.72880914206656,9.86267267504121));
#28422=CARTESIAN_POINT('Ctrl Pts',(2.99935398155699,-0.392324694732591,
10.0209650137509));
#28423=CARTESIAN_POINT('Ctrl Pts',(1.96318925653975,2.30128896833614,10.1792573524606));
#28424=CARTESIAN_POINT('Ctrl Pts',(-0.860046863524081,2.90006247610654,
10.3375496911703));
#28425=CARTESIAN_POINT('Ctrl Pts',(-2.90039099134443,0.858938338943435,
10.4958420298799));
#28426=CARTESIAN_POINT('Ctrl Pts',(-2.30053843012103,-1.9640687117092,10.6541343685896));
#28427=CARTESIAN_POINT('Ctrl Pts',(0.393471079027465,-2.9992038081377,10.8124267072993));
#28428=CARTESIAN_POINT('Ctrl Pts',(2.72930783037093,-1.30419390423922,10.970719046009));
#28429=CARTESIAN_POINT('Ctrl Pts',(2.58068316991478,1.57801056691565,11.1290113847186));
#28430=CARTESIAN_POINT('Ctrl Pts',(0.0828886282207864,3.02376792232645,
11.2873037234283));
#28431=CARTESIAN_POINT('Ctrl Pts',(-2.4903585963842,1.7170198118234,11.445596062138));
#28432=CARTESIAN_POINT('Ctrl Pts',(-2.79665748873786,-1.15271412911671,
11.6038884008477));
#28433=CARTESIAN_POINT('Ctrl Pts',(-0.557187254035818,-2.97314401546895,
11.7621807395573));
#28434=CARTESIAN_POINT('Ctrl Pts',(2.18948492263639,-2.08715086812781,11.920473078267));
#28435=CARTESIAN_POINT('Ctrl Pts',(2.94309104004043,0.698754679993293,12.0787654169767));
#28436=CARTESIAN_POINT('Ctrl Pts',(1.01763104440733,2.8485908850232,12.2370577556864));
#28437=CARTESIAN_POINT('Ctrl Pts',(-1.83416823518104,2.40538351574787,12.3953500943961));
#28438=CARTESIAN_POINT('Ctrl Pts',(-3.01634265518126,-0.227420226261331,
12.5536424331057));
#28439=CARTESIAN_POINT('Ctrl Pts',(-1.45277075511745,-2.65320562826448,
12.7119347718154));
#28440=CARTESIAN_POINT('Ctrl Pts',(1.43324372218759,-2.6638046860813,12.8702271105251));
#28441=CARTESIAN_POINT('Ctrl Pts',(3.01459088353241,-0.249569184199341,
13.0285194492348));
#28442=CARTESIAN_POINT('Ctrl Pts',(1.8517863448907,2.39184663088069,13.1868117879444));
#28443=CARTESIAN_POINT('Ctrl Pts',(-0.996680641051226,2.85598856309551,
13.3451041266541));
#28444=CARTESIAN_POINT('Ctrl Pts',(-2.93787928407284,0.720352889210458,
13.5033964653638));
#28445=CARTESIAN_POINT('Ctrl Pts',(-2.20475602299055,-2.071012759948,13.6616888040735));
#28446=CARTESIAN_POINT('Ctrl Pts',(0.535334426109747,-2.97715636556076,
13.8199811427831));
#28447=CARTESIAN_POINT('Ctrl Pts',(2.78811534226478,-1.17322453562959,13.9782734814928));
#28448=CARTESIAN_POINT('Ctrl Pts',(2.50290296121319,1.69868176523493,14.1365658202025));
#28449=CARTESIAN_POINT('Ctrl Pts',(-0.0606767609763033,3.02429517465504,
14.2948581589122));
#28450=CARTESIAN_POINT('Ctrl Pts',(-2.56902303914322,1.59692316568888,14.4531504976219));
#28451=CARTESIAN_POINT('Ctrl Pts',(-2.73881353562333,-1.28411190709835,
14.6114428363315));
#28452=CARTESIAN_POINT('Ctrl Pts',(-0.415489672570913,-2.99623285220711,
14.7697351750412));
#28453=CARTESIAN_POINT('Ctrl Pts',(2.28605025200581,-1.98091322829095,14.9280275137509));
#28454=CARTESIAN_POINT('Ctrl Pts',(2.90662167133189,0.837611743647851,15.0863198524606));
#28455=CARTESIAN_POINT('Ctrl Pts',(0.881324676130029,2.89366718664477,15.2446121911703));
#28456=CARTESIAN_POINT('Ctrl Pts',(-1.94623328914695,2.31564655267074,15.4029045298799));
#28457=CARTESIAN_POINT('Ctrl Pts',(-3.00215470665022,-0.370283801722237,
15.5611968685896));
#28458=CARTESIAN_POINT('Ctrl Pts',(-1.32524494866622,-2.71914854163458,
15.7194892072993));
#28459=CARTESIAN_POINT('Ctrl Pts',(1.55802192637397,-2.59279977080658,15.877781546009));
#28460=CARTESIAN_POINT('Ctrl Pts',(3.0230371509412,-0.106251493506751,16.0360738847186));
#28461=CARTESIAN_POINT('Ctrl Pts',(1.73621210960984,2.47701643691491,16.1943662234283));
#28462=CARTESIAN_POINT('Ctrl Pts',(-1.13106929103762,2.80548128863956,16.352658562138));
#28463=CARTESIAN_POINT('Ctrl Pts',(-2.96874976542504,0.580144758511495,
16.5109509008477));
#28464=CARTESIAN_POINT('Ctrl Pts',(-2.10400715147876,-2.173291624695,16.6692432395573));
#28465=CARTESIAN_POINT('Ctrl Pts',(0.675991784463513,-2.94840268556796,
16.827535578267));
#28466=CARTESIAN_POINT('Ctrl Pts',(2.84064256237469,-1.03961222673644,16.9858279169767));
#28467=CARTESIAN_POINT('Ctrl Pts',(2.41948437437558,1.81552625060683,17.1441202556864));
#28468=CARTESIAN_POINT('Ctrl Pts',(-0.204104777216815,3.01801046090703,
17.3024125943961));
#28469=CARTESIAN_POINT('Ctrl Pts',(-2.64190184870001,1.47322828949895,17.4607049331057));
#28470=CARTESIAN_POINT('Ctrl Pts',(-2.67479763028224,-1.41261516633856,
17.6189972718154));
#28471=CARTESIAN_POINT('Ctrl Pts',(-0.272860988730089,-3.01257610919817,
17.7772896105251));
#28472=CARTESIAN_POINT('Ctrl Pts',(2.37747526130895,-1.87020632633128,17.9355819492348));
#28473=CARTESIAN_POINT('Ctrl Pts',(2.86358727858653,0.974568499261341,18.0938742879444));
#28474=CARTESIAN_POINT('Ctrl Pts',(0.74306664450121,2.93225104274409,18.2521666266541));
#28475=CARTESIAN_POINT('Ctrl Pts',(-2.05397843789397,2.22064411745206,18.4104589653638));
#28476=CARTESIAN_POINT('Ctrl Pts',(-2.98108161028717,-0.512219196285761,
18.5687513040735));
#28477=CARTESIAN_POINT('Ctrl Pts',(-1.19496791351362,-2.77914600348429,
18.7270436427832));
#28478=CARTESIAN_POINT('Ctrl Pts',(1.67973777132246,-2.51561105275516,18.8853359814928));
#28479=CARTESIAN_POINT('Ctrl Pts',(3.02381636176497,0.0366483534147998,
19.0436283202025));
#28480=CARTESIAN_POINT('Ctrl Pts',(1.61839413286117,2.55787618136095,19.2019206589122));
#28481=CARTESIAN_POINT('Ctrl Pts',(-1.26635745904276,2.74609974825633,19.3602129976219));
#28482=CARTESIAN_POINT('Ctrl Pts',(-2.41160054520915,1.21182125652926,19.4657412234283));
#28483=CARTESIAN_POINT('Ctrl Pts',(-2.53475666268528,0.371481747533264,
19.5185053363315));
#28484=CARTESIAN_POINT('Ctrl Pts',(1.37702479013101,-1.93106208855765,-2.4980018054066E-15));
#28485=CARTESIAN_POINT('Ctrl Pts',(2.01722342979855,-1.47454160552709,0.0527641129032233));
#28486=CARTESIAN_POINT('Ctrl Pts',(2.79719579707326,0.117141566795549,0.158292338709675));
#28487=CARTESIAN_POINT('Ctrl Pts',(1.42324750420295,2.41394690313832,0.316584677419352));
#28488=CARTESIAN_POINT('Ctrl Pts',(-1.24746758074934,2.50637639523624,0.474877016129029));
#28489=CARTESIAN_POINT('Ctrl Pts',(-2.78199511604896,0.320772232796965,
0.633169354838707));
#28490=CARTESIAN_POINT('Ctrl Pts',(-1.78443098713088,-2.15863980796169,
0.791461693548384));
#28491=CARTESIAN_POINT('Ctrl Pts',(0.837655777364047,-2.67211687161305,
0.949754032258061));
#28492=CARTESIAN_POINT('Ctrl Pts',(2.69714227944592,-0.753688528678065,
1.10804637096774));
#28493=CARTESIAN_POINT('Ctrl Pts',(2.10149481948277,1.85107442631988,1.26633870967742));
#28494=CARTESIAN_POINT('Ctrl Pts',(-0.407147056663944,2.77068707131458,
1.42463104838709));
#28495=CARTESIAN_POINT('Ctrl Pts',(-2.54515405095666,1.16824237520026,1.58292338709677));
#28496=CARTESIAN_POINT('Ctrl Pts',(-2.36633978105435,-1.49767885575262,
1.74121572580645));
#28497=CARTESIAN_POINT('Ctrl Pts',(-0.0334666860564693,-2.80025859792997,
1.89950806451613));
#28498=CARTESIAN_POINT('Ctrl Pts',(2.32986892611582,-1.55380138209287,2.0578004032258));
#28499=CARTESIAN_POINT('Ctrl Pts',(2.57234931467855,1.10707092589757,2.21609274193548));
#28500=CARTESIAN_POINT('Ctrl Pts',(0.473245533627712,2.76018492369889,2.37438508064516));
#28501=CARTESIAN_POINT('Ctrl Pts',(-2.05664861872599,1.90073187098275,2.53267741935483));
#28502=CARTESIAN_POINT('Ctrl Pts',(-2.71439640116312,-0.688939017013961,
2.69096975806451));
#28503=CARTESIAN_POINT('Ctrl Pts',(-0.901256421879981,-2.65147525836599,
2.84926209677419));
#28504=CARTESIAN_POINT('Ctrl Pts',(1.73228815673516,-2.20040050466946,3.00755443548387));
#28505=CARTESIAN_POINT('Ctrl Pts',(2.78894830461411,0.253676763035589,3.16584677419355));
#28506=CARTESIAN_POINT('Ctrl Pts',(1.30685690747379,2.47683457209687,3.32413911290322));
#28507=CARTESIAN_POINT('Ctrl Pts',(-1.36485315638996,2.44535486220292,3.4824314516129));
#28508=CARTESIAN_POINT('Ctrl Pts',(-2.79415114999435,0.187893249872369,
3.64072379032258));
#28509=CARTESIAN_POINT('Ctrl Pts',(-1.67996150992302,-2.24060568590825,
3.79901612903226));
#28510=CARTESIAN_POINT('Ctrl Pts',(0.963480161046465,-2.62950385116291,
3.95730846774193));
#28511=CARTESIAN_POINT('Ctrl Pts',(2.72987555186367,-0.62479115878066,4.11560080645161));
#28512=CARTESIAN_POINT('Ctrl Pts',(2.01129273950979,1.94866262755053,4.27389314516129));
#28513=CARTESIAN_POINT('Ctrl Pts',(-0.538149583533225,2.74826846342811,
4.43218548387097));
#28514=CARTESIAN_POINT('Ctrl Pts',(-2.5977197642612,1.04615321399383,4.59047782258064));
#28515=CARTESIAN_POINT('Ctrl Pts',(-2.29261182358265,-1.60826476275027,
4.74877016129032));
#28516=CARTESIAN_POINT('Ctrl Pts',(0.099437554957728,-2.79869553427603,
4.9070625));
#28517=CARTESIAN_POINT('Ctrl Pts',(2.40096992936847,-1.44150196638533,5.06535483870968));
#28518=CARTESIAN_POINT('Ctrl Pts',(2.51692357424149,1.22787631390688,5.22364717741935));
#28519=CARTESIAN_POINT('Ctrl Pts',(0.341747055246021,2.77953116030023,5.38193951612902));
#28520=CARTESIAN_POINT('Ctrl Pts',(-2.14451836398642,1.80100680380742,5.54023185483871));
#28521=CARTESIAN_POINT('Ctrl Pts',(-2.67865032911246,-0.816955895494213,
5.69852419354838));
#28522=CARTESIAN_POINT('Ctrl Pts',(-0.774433895304387,-2.6912518764775,
5.85681653225807));
#28523=CARTESIAN_POINT('Ctrl Pts',(1.83474190859146,-2.11572839695838,6.01510887096773));
#28524=CARTESIAN_POINT('Ctrl Pts',(2.77377064377508,0.385721319828002,6.17340120967742));
#28525=CARTESIAN_POINT('Ctrl Pts',(1.18786391621721,2.53605280650616,6.3316935483871));
#28526=CARTESIAN_POINT('Ctrl Pts',(-1.47934336288373,2.37784098196877,6.48998588709676));
#28527=CARTESIAN_POINT('Ctrl Pts',(-2.79991928769473,0.0551044756207588,
6.64827822580646));
#28528=CARTESIAN_POINT('Ctrl Pts',(-1.57175690273231,-2.31779307953747,
6.80657056451611));
#28529=CARTESIAN_POINT('Ctrl Pts',(1.087159950493,-2.58082695330052,6.96486290322581));
#28530=CARTESIAN_POINT('Ctrl Pts',(2.75644605727123,-0.494560061258782,
7.12315524193547));
#28531=CARTESIAN_POINT('Ctrl Pts',(1.91656709780378,2.04189987033018,7.28144758064516));
#28532=CARTESIAN_POINT('Ctrl Pts',(-0.667943575474826,2.7196389283911,7.43973991935484));
#28533=CARTESIAN_POINT('Ctrl Pts',(-2.64443194358857,0.921718078680678,
7.59803225806451));
#28534=CARTESIAN_POINT('Ctrl Pts',(-2.21372056425457,-1.71523344890277,
7.75632459677419));
#28535=CARTESIAN_POINT('Ctrl Pts',(0.23211833466387,-2.79082525421268,7.91461693548387));
#28536=CARTESIAN_POINT('Ctrl Pts',(2.4666622528453,-1.32595695677747,8.07290927419355));
#28537=CARTESIAN_POINT('Ctrl Pts',(2.45582838148514,1.34591659530986,8.23120161290321));
#28538=CARTESIAN_POINT('Ctrl Pts',(0.209478684497901,2.79261583494391,8.38949395161291));
#28539=CARTESIAN_POINT('Ctrl Pts',(-2.22755734784449,1.6972250242388,8.54778629032258));
#28540=CARTESIAN_POINT('Ctrl Pts',(-2.6368703759488,-0.943132621258565,
8.70607862903226));
#28541=CARTESIAN_POINT('Ctrl Pts',(-0.645866875421753,-2.72496614659181,
8.86437096774193));
#28542=CARTESIAN_POINT('Ctrl Pts',(1.93306273270264,-2.02629045111372,9.02266330645161));
#28543=CARTESIAN_POINT('Ctrl Pts',(2.75234481681179,0.516897020892659,9.18095564516129));
#28544=CARTESIAN_POINT('Ctrl Pts',(1.06619515253284,2.58955834411081,9.33924798387097));
#28545=CARTESIAN_POINT('Ctrl Pts',(-1.590501213895,2.3049708044652,9.49754032258064));
#28546=CARTESIAN_POINT('Ctrl Pts',(-2.79938035451524,-0.077808428801199,
9.65583266129033));
#28547=CARTESIAN_POINT('Ctrl Pts',(-1.46001177080394,-2.38975943348956,
9.81412499999998));
#28548=CARTESIAN_POINT('Ctrl Pts',(1.20839081375242,-2.52633651006299,9.97241733870969));
#28549=CARTESIAN_POINT('Ctrl Pts',(2.77680741881119,-0.363214922151578,
10.1307096774193));
#28550=CARTESIAN_POINT('Ctrl Pts',(1.81752421541791,2.13053754888476,10.2890020161291));
#28551=CARTESIAN_POINT('Ctrl Pts',(-0.796232964112916,2.68488316090261,
10.4472943548387));
#28552=CARTESIAN_POINT('Ctrl Pts',(-2.68518730091256,0.795206690022401,
10.6055866935484));
#28553=CARTESIAN_POINT('Ctrl Pts',(-2.12984269922823,-1.81833841662728,
10.7638790322581));
#28554=CARTESIAN_POINT('Ctrl Pts',(0.364276246834986,-2.77666838798409,
10.9221713709677));
#28555=CARTESIAN_POINT('Ctrl Pts',(2.52679819661009,-1.20742510924963,11.0804637096774));
#28556=CARTESIAN_POINT('Ctrl Pts',(2.38920121328945,1.46092507790601,11.2387560483871));
#28557=CARTESIAN_POINT('Ctrl Pts',(0.0767384440762257,2.79940988996594,
11.3970483870968));
#28558=CARTESIAN_POINT('Ctrl Pts',(-2.30557855740325,1.58962009187123,11.5553407258065));
#28559=CARTESIAN_POINT('Ctrl Pts',(-2.58915063388745,-1.06718485553286,
11.7136330645161));
#28560=CARTESIAN_POINT('Ctrl Pts',(-0.515844982015253,-2.75254218412146,
11.8719254032258));
#28561=CARTESIAN_POINT('Ctrl Pts',(2.02702915825758,-1.93228810284904,12.0302177419355));
#28562=CARTESIAN_POINT('Ctrl Pts',(2.72471908433383,0.646908364689661,12.1885100806452));
#28563=CARTESIAN_POINT('Ctrl Pts',(0.942124687882267,2.63723066744667,12.3468024193548));
#28564=CARTESIAN_POINT('Ctrl Pts',(-1.69807631713903,2.22690847185283,12.5050947580645));
#28565=CARTESIAN_POINT('Ctrl Pts',(-2.79253556402036,-0.210546062703279,
12.6633870967742));
#28566=CARTESIAN_POINT('Ctrl Pts',(-1.3449778303753,-2.45634263828104,12.8216794354839));
#28567=CARTESIAN_POINT('Ctrl Pts',(1.3268996674641,-2.46615526545311,12.9799717741935));
#28568=CARTESIAN_POINT('Ctrl Pts',(2.79091377061401,-0.231051608597259,
13.1382641129033));
#28569=CARTESIAN_POINT('Ctrl Pts',(1.71438719543081,2.21437599900773,13.2965564516129));
#28570=CARTESIAN_POINT('Ctrl Pts',(-0.922728766019108,2.64407945137796,
13.4548487903226));
#28571=CARTESIAN_POINT('Ctrl Pts',(-2.71989403109743,0.666904026407466,
13.6131411290322));
#28572=CARTESIAN_POINT('Ctrl Pts',(-2.04116717098217,-1.91734741268884,
13.7714334677419));
#28573=CARTESIAN_POINT('Ctrl Pts',(0.495613593829615,-2.7562568251976,13.9297258064516));
#28574=CARTESIAN_POINT('Ctrl Pts',(2.58124229901106,-1.08617342751133,14.0880181451613));
#28575=CARTESIAN_POINT('Ctrl Pts',(2.31719215337611,1.57264269469624,14.246310483871));
#28576=CARTESIAN_POINT('Ctrl Pts',(-0.0561746566308962,2.79989802113906,
14.4046028225806));
#28577=CARTESIAN_POINT('Ctrl Pts',(-2.37840624282921,1.47843439654775,14.5628951612903));
#28578=CARTESIAN_POINT('Ctrl Pts',(-2.53559859597213,-1.18883315945374,
14.7211875));
#28579=CARTESIAN_POINT('Ctrl Pts',(-0.384661101133316,-2.77391787153297,
14.8794798387097));
#28580=CARTESIAN_POINT('Ctrl Pts',(2.11642951734883,-1.833933100982,15.0377721774193));
#28581=CARTESIAN_POINT('Ctrl Pts',(2.69095567587589,0.775462488971503,15.196064516129));
#28582=CARTESIAN_POINT('Ctrl Pts',(0.815932002060255,2.67896239018596,15.3543568548387));
#28583=CARTESIAN_POINT('Ctrl Pts',(-1.80182634969786,2.14382982680247,15.5126491935484));
#28584=CARTESIAN_POINT('Ctrl Pts',(-2.77940033524077,-0.342809422965879,
15.6709415322581));
#28585=CARTESIAN_POINT('Ctrl Pts',(-1.22691420480089,-2.5173927084595,15.8292338709677));
#28586=CARTESIAN_POINT('Ctrl Pts',(1.44241955782089,-2.40041878462448,15.9875262096774));
#28587=CARTESIAN_POINT('Ctrl Pts',(2.7987333404768,-0.0983678276200387,
16.1458185483871));
#28588=CARTESIAN_POINT('Ctrl Pts',(1.60738835637255,2.29322636168875,16.3041108870968));
#28589=CARTESIAN_POINT('Ctrl Pts',(-1.0471460247291,2.59731972402479,16.4624032258064));
#28590=CARTESIAN_POINT('Ctrl Pts',(-2.74847397936901,0.537099081777219,
16.6206955645161));
#28591=CARTESIAN_POINT('Ctrl Pts',(-1.94789368090028,-2.01203737331484,
16.7789879032258));
#28592=CARTESIAN_POINT('Ctrl Pts',(0.625834434246847,-2.72963661550809,
16.9372802419355));
#28593=CARTESIAN_POINT('Ctrl Pts',(2.62987209575649,-0.962474906809746,
17.0955725806452));
#28594=CARTESIAN_POINT('Ctrl Pts',(2.23996307264014,1.6808175336192,17.2538649193548));
#28595=CARTESIAN_POINT('Ctrl Pts',(-0.188960577202794,2.79407962162107,
17.4121572580645));
#28596=CARTESIAN_POINT('Ctrl Pts',(-2.44587757842207,1.36391745323756,17.5704495967742));
#28597=CARTESIAN_POINT('Ctrl Pts',(-2.47633255336226,-1.30780171261343,
17.7287419354839));
#28598=CARTESIAN_POINT('Ctrl Pts',(-0.252615203963521,-2.78904848883903,
17.8870342741935));
#28599=CARTESIAN_POINT('Ctrl Pts',(2.20107095869216,-1.73144044804223,18.0453266129032));
#28600=CARTESIAN_POINT('Ctrl Pts',(2.65111435612032,0.902257304582571,18.2036189516129));
#28601=CARTESIAN_POINT('Ctrl Pts',(0.687932462726838,2.71468339494958,18.3619112903226));
#28602=CARTESIAN_POINT('Ctrl Pts',(-1.90157700607965,2.0558763979833,18.5202036290323));
#28603=CARTESIAN_POINT('Ctrl Pts',(-2.75989082396666,-0.474213471650817,
18.6784959677419));
#28604=CARTESIAN_POINT('Ctrl Pts',(-1.10630348664728,-2.57293846871273,
18.8367883064516));
#28605=CARTESIAN_POINT('Ctrl Pts',(1.55510431037697,-2.32895732784023,18.9950806451613));
#28606=CARTESIAN_POINT('Ctrl Pts',(2.799454735287,0.0339291128273711,19.153372983871));
#28607=CARTESIAN_POINT('Ctrl Pts',(1.49831225734699,2.36808646144409,19.3116653225806));
#28608=CARTESIAN_POINT('Ctrl Pts',(-1.17239605887113,2.54234418499522,19.4699576612903));
#28609=CARTESIAN_POINT('Ctrl Pts',(-2.23266420913401,1.1219063425307,19.5754858870968));
#28610=CARTESIAN_POINT('Ctrl Pts',(-2.34668236863853,0.34391848339548,19.62825));
#28611=CARTESIAN_POINT('',(1.37702479013102,-1.93106208855765,0.));
#28612=CARTESIAN_POINT('Ctrl Pts',(1.37702479013101,-1.93106208855765,-2.4980018054066E-15));
#28613=CARTESIAN_POINT('Ctrl Pts',(2.01722342979855,-1.47454160552709,0.0527641129032233));
#28614=CARTESIAN_POINT('Ctrl Pts',(2.79719579707326,0.117141566795549,0.158292338709675));
#28615=CARTESIAN_POINT('Ctrl Pts',(1.42324750420295,2.41394690313832,0.316584677419352));
#28616=CARTESIAN_POINT('Ctrl Pts',(-1.24746758074934,2.50637639523624,0.474877016129029));
#28617=CARTESIAN_POINT('Ctrl Pts',(-2.32942948970535,0.965354551432513,
0.586485493020905));
#28618=CARTESIAN_POINT('Ctrl Pts',(-2.3750014795357,0.091963591913039,0.645329857009555));
#28619=CARTESIAN_POINT('Ctrl Pts',(-2.37433784198147,0.00164420209662409,
0.651410108094979));
#28620=CARTESIAN_POINT('Ctrl Pts',(1.29201086331817,2.64828936846223,6.41847686111419E-17));
#28621=CARTESIAN_POINT('Ctrl Pts',(1.35862032458796,2.60817485458433,2.61969259968471E-17));
#28622=CARTESIAN_POINT('Ctrl Pts',(1.42341581930837,2.56531698465799,3.28157858661721E-16));
#28623=CARTESIAN_POINT('Ctrl Pts',(1.48620178418383,2.51970672695701,2.04697370165263E-16));
#28624=CARTESIAN_POINT('Ctrl Pts',(1.56531098107701,2.46223861503148,5.43435251614495E-17));
#28625=CARTESIAN_POINT('Ctrl Pts',(1.64123143087454,2.40040132841406,-5.27955452558019E-16));
#28626=CARTESIAN_POINT('Ctrl Pts',(1.71378595850393,2.33457408786609,-7.3899220076612E-16));
#28627=CARTESIAN_POINT('Ctrl Pts',(1.75212006782637,2.29979433368659,-8.50493247512412E-16));
#28628=CARTESIAN_POINT('Ctrl Pts',(1.78951386694703,2.26390023027539,-3.7350885354349E-16));
#28629=CARTESIAN_POINT('Ctrl Pts',(1.82593618288559,2.22694486783177,-3.67761376907083E-16));
#28630=CARTESIAN_POINT('Ctrl Pts',(1.84259085550132,2.21004645137928,-3.65133253481123E-16));
#28631=CARTESIAN_POINT('Ctrl Pts',(1.85904234863816,2.19292611311178,-2.46595166079732E-16));
#28632=CARTESIAN_POINT('Ctrl Pts',(1.87528742149878,2.17558883786553,-2.63677968348475E-16));
#28633=CARTESIAN_POINT('Ctrl Pts',(1.88718261793227,2.16289389359258,-2.76186578827762E-16));
#28634=CARTESIAN_POINT('Ctrl Pts',(1.89896688194925,2.15008278084551,-1.10225564131519E-15));
#28635=CARTESIAN_POINT('Ctrl Pts',(1.91062984003561,2.13716785713421,-1.06165076729781E-15));
#28636=CARTESIAN_POINT('Ctrl Pts',(1.97578401617971,2.0650196758458,-8.34814908466034E-16));
#28637=CARTESIAN_POINT('Ctrl Pts',(2.03723207640777,1.98955383080639,-9.74476180451947E-16));
#28638=CARTESIAN_POINT('Ctrl Pts',(2.09480296364938,1.91114695058468,-8.46545056276682E-16));
#28639=CARTESIAN_POINT('Ctrl Pts',(2.142269300225,1.84650164903097,-7.41067755343023E-16));
#28640=CARTESIAN_POINT('Ctrl Pts',(2.1870993303121,1.77985624721179,2.24451139630718E-16));
#28641=CARTESIAN_POINT('Ctrl Pts',(2.229172411834,1.71141200033172,1.52655665885959E-16));
#28642=CARTESIAN_POINT('Ctrl Pts',(2.24800974392323,1.68076753690192,1.20510761531148E-16));
#28643=CARTESIAN_POINT('Ctrl Pts',(2.26629410220438,1.6497623951442,5.54871798735934E-17));
#28644=CARTESIAN_POINT('Ctrl Pts',(2.28401308817003,1.61841438574687,8.32667268468867E-17));
#28645=CARTESIAN_POINT('Ctrl Pts',(2.29435495135519,1.60011780687136,9.94805369769141E-17));
#28646=CARTESIAN_POINT('Ctrl Pts',(2.3045041967679,1.58170442532538,5.28474538527533E-16));
#28647=CARTESIAN_POINT('Ctrl Pts',(2.31445819927483,1.56317777718625,5.55111512312578E-16));
#28648=CARTESIAN_POINT('Ctrl Pts',(2.32185832866684,1.54940446405576,5.74914305458692E-16));
#28649=CARTESIAN_POINT('Ctrl Pts',(2.32915061183048,1.5355682586848,6.28531276475973E-16));
#28650=CARTESIAN_POINT('Ctrl Pts',(2.33632722813254,1.52168406757476,6.10622663543836E-16));
#28651=CARTESIAN_POINT('Ctrl Pts',(2.37998634723912,1.43721925465201,5.01675182986223E-16));
#28652=CARTESIAN_POINT('Ctrl Pts',(2.4194343086838,1.35085952195958,-2.85148112393472E-16));
#28653=CARTESIAN_POINT('Ctrl Pts',(2.45450882946931,1.26295234700174,-2.91433543964104E-16));
#28654=CARTESIAN_POINT('Ctrl Pts',(2.49097294870383,1.17156242527378,-2.97967994645086E-16));
#28655=CARTESIAN_POINT('Ctrl Pts',(2.522710946502,1.07849900531789,-2.19554586473301E-16));
#28656=CARTESIAN_POINT('Ctrl Pts',(2.5494811878723,0.984141912890972,-2.91433543964104E-16));
#28657=CARTESIAN_POINT('Ctrl Pts',(2.57415365468709,0.897178848216262,-3.57679909427988E-16));
#28658=CARTESIAN_POINT('Ctrl Pts',(2.59460600088325,0.809116138918699,-3.16658239360586E-16));
#28659=CARTESIAN_POINT('Ctrl Pts',(2.61059963694684,0.720255260258035,-3.60822483003176E-16));
#28660=CARTESIAN_POINT('Ctrl Pts',(2.62008388056236,0.667560662371934,-3.87011927613296E-16));
#28661=CARTESIAN_POINT('Ctrl Pts',(2.6279992974166,0.614585522567766,-5.86434132422756E-17));
#28662=CARTESIAN_POINT('Ctrl Pts',(2.63428771987185,0.561395014680878,-1.11022302462516E-16));
#28663=CARTESIAN_POINT('Ctrl Pts',(2.63631849388102,0.544217749362041,-1.27937464828616E-16));
#28664=CARTESIAN_POINT('Ctrl Pts',(2.63817971938346,0.527015146377361,-5.57610343116661E-16));
#28665=CARTESIAN_POINT('Ctrl Pts',(2.63986723376609,0.50981362072198,-5.55111512312578E-16));
#28666=CARTESIAN_POINT('Ctrl Pts',(2.64857594877992,0.421042119704249,-5.42215856095108E-16));
#28667=CARTESIAN_POINT('Ctrl Pts',(2.65267958281541,0.332167648005602,-3.9556124136452E-16));
#28668=CARTESIAN_POINT('Ctrl Pts',(2.65199707698894,0.243482089150498,-3.33066907387547E-16));
#28669=CARTESIAN_POINT('Ctrl Pts',(2.6516640117541,0.200203225671092,-3.02569453423877E-16));
#28670=CARTESIAN_POINT('Ctrl Pts',(2.65019037381467,0.156969394455165,3.29031573743661E-16));
#28671=CARTESIAN_POINT('Ctrl Pts',(2.64755062273554,0.113815198443072,3.05311331771918E-16));
#28672=CARTESIAN_POINT('Ctrl Pts',(2.64202705093324,0.0235167979128891,
2.25896251348351E-16));
#28673=CARTESIAN_POINT('Ctrl Pts',(2.63140068084878,-0.0664344653587478,
-3.57990035170166E-16));
#28674=CARTESIAN_POINT('Ctrl Pts',(2.61586718053927,-0.155705179881193,
-4.44089209850063E-16));
#28675=CARTESIAN_POINT('Ctrl Pts',(2.59996532115929,-0.247092846588728,
-5.32230127300229E-16));
#28676=CARTESIAN_POINT('Ctrl Pts',(2.57892033292169,-0.337768326694507,
-1.15896493065795E-16));
#28677=CARTESIAN_POINT('Ctrl Pts',(2.55289626581674,-0.427342175555427,
-2.77555756156289E-17));
#28678=CARTESIAN_POINT('Ctrl Pts',(2.54882874919627,-0.441342413009925,
-1.39793028591053E-17));
#28679=CARTESIAN_POINT('Ctrl Pts',(2.54463896540328,-0.455317440734485,
-3.65684696917243E-16));
#28680=CARTESIAN_POINT('Ctrl Pts',(2.54032919703339,-0.469260060669249,
-3.60822483003176E-16));
#28681=CARTESIAN_POINT('Ctrl Pts',(2.51414391528516,-0.553972602032386,
-3.31280653760249E-16));
#28682=CARTESIAN_POINT('Ctrl Pts',(2.48362384320016,-0.637202118714745,
1.1028949584026E-16));
#28683=CARTESIAN_POINT('Ctrl Pts',(2.44898771893138,-0.718649795920404,
0.));
#28684=CARTESIAN_POINT('Ctrl Pts',(2.41432501221678,-0.800159982385209,
-1.10374140546078E-16));
#28685=CARTESIAN_POINT('Ctrl Pts',(2.37553928084343,-0.879886390297083,
5.56731917103673E-17));
#28686=CARTESIAN_POINT('Ctrl Pts',(2.33280620908713,-0.957500984689981,
8.32667268468867E-17));
#28687=CARTESIAN_POINT('Ctrl Pts',(2.29068411086063,-1.0340058890758,1.10465745070182E-16));
#28688=CARTESIAN_POINT('Ctrl Pts',(2.24472605801825,-1.10845957586292,-1.45162796518328E-16));
#28689=CARTESIAN_POINT('Ctrl Pts',(2.19506803735907,-1.18050963761054,-1.66533453693773E-16));
#28690=CARTESIAN_POINT('Ctrl Pts',(2.16851747476405,-1.21903251164,-1.77959663669557E-16));
#28691=CARTESIAN_POINT('Ctrl Pts',(2.14090871133255,-1.25686754949034,-6.12242562191498E-17));
#28692=CARTESIAN_POINT('Ctrl Pts',(2.11225966440144,-1.29395535226115,-5.55111512312578E-17));
#28693=CARTESIAN_POINT('Ctrl Pts',(2.10389009111628,-1.30479023567008,-5.38421166208939E-17));
#28694=CARTESIAN_POINT('Ctrl Pts',(2.0954317221698,-1.31556131757123,-5.76575592671161E-18));
#28695=CARTESIAN_POINT('Ctrl Pts',(2.08688497852084,-1.32626704704954,0.));
#28696=CARTESIAN_POINT('Ctrl Pts',(2.07860608678634,-1.33663726276327,5.58505918105939E-18));
#28697=CARTESIAN_POINT('Ctrl Pts',(2.07025013926869,-1.34693879666623,-1.85493259861054E-16));
#28698=CARTESIAN_POINT('Ctrl Pts',(2.06181881264409,-1.35716935688295,-1.66533453693773E-16));
#28699=CARTESIAN_POINT('Ctrl Pts',(2.00758715298996,-1.42297397867583,-4.45809068463581E-17));
#28700=CARTESIAN_POINT('Ctrl Pts',(1.95022582590432,-1.48586254952678,-2.55249516657381E-17));
#28701=CARTESIAN_POINT('Ctrl Pts',(1.8898935724857,-1.54553906223415,0.));
#28702=CARTESIAN_POINT('Ctrl Pts',(1.83050776280639,-1.6042794179337,2.51245368074963E-17));
#28703=CARTESIAN_POINT('Ctrl Pts',(1.76824286709423,-1.65990821687079,-2.08086528920867E-16));
#28704=CARTESIAN_POINT('Ctrl Pts',(1.70322439968709,-1.71210071694254,-2.22044604925031E-16));
#28705=CARTESIAN_POINT('Ctrl Pts',(1.64023093603462,-1.76266767871992,-2.35567955881933E-16));
#28706=CARTESIAN_POINT('Ctrl Pts',(1.57465218130676,-1.81000934229147,8.12709303573321E-17));
#28707=CARTESIAN_POINT('Ctrl Pts',(1.50658663996491,-1.85378460546696,1.11022302462516E-16));
#28708=CARTESIAN_POINT('Ctrl Pts',(1.46434993749398,-1.88094846444582,1.2948391794277E-16));
#28709=CARTESIAN_POINT('Ctrl Pts',(1.42115540397303,-1.9067381345186,4.99167222978473E-17));
#28710=CARTESIAN_POINT('Ctrl Pts',(1.37702479013104,-1.93106208855763,5.55111512312578E-17));
#28711=CARTESIAN_POINT('Ctrl Pts',(0.260898964428461,2.9250678849183,19.058));
#28712=CARTESIAN_POINT('Ctrl Pts',(0.726863739861969,2.88429659618081,19.0328104438584));
#28713=CARTESIAN_POINT('Ctrl Pts',(1.18340500184494,2.7384933202854,19.0076208877168));
#28714=CARTESIAN_POINT('Ctrl Pts',(1.57541514848214,2.49092003235782,18.9824313315753));
#28715=CARTESIAN_POINT('Ctrl Pts',(2.39655179416664,1.97233269232634,18.929667218672));
#28716=CARTESIAN_POINT('Ctrl Pts',(2.93454570444379,1.00720976345797,18.8769031057688));
#28717=CARTESIAN_POINT('Ctrl Pts',(2.94628683933111,0.0361474094946818,
18.8241389928656));
#28718=CARTESIAN_POINT('Ctrl Pts',(2.95802797421842,-0.934914944468595,
18.7713748799624));
#28719=CARTESIAN_POINT('Ctrl Pts',(2.44351633371593,-1.9119167235268,18.7186107670591));
#28720=CARTESIAN_POINT('Ctrl Pts',(1.63604360338806,-2.45085804146298,18.6658466541559));
#28721=CARTESIAN_POINT('Ctrl Pts',(0.828570873060194,-2.98979935939915,
18.6130825412527));
#28722=CARTESIAN_POINT('Ctrl Pts',(-0.271862947093059,-3.09068021621329,
18.5603184283495));
#28723=CARTESIAN_POINT('Ctrl Pts',(-1.16394092644999,-2.70723224004173,
18.5075543154462));
#28724=CARTESIAN_POINT('Ctrl Pts',(-2.05601890580693,-2.32378426387017,
18.454790202543));
#28725=CARTESIAN_POINT('Ctrl Pts',(-2.73974104436754,-1.45600745471292,
18.4020260896398));
#28726=CARTESIAN_POINT('Ctrl Pts',(-2.9041551334136,-0.499050683143429,
18.3492619767365));
#28727=CARTESIAN_POINT('Ctrl Pts',(-2.93228850345654,-0.335303043717479,
18.3402333568542));
#28728=CARTESIAN_POINT('Ctrl Pts',(-2.94521673044455,-0.168944248759899,
18.3312047369719));
#28729=CARTESIAN_POINT('Ctrl Pts',(-2.94374845943093,-0.00235935217182681,
18.3221761170896));
#28730=CARTESIAN_POINT('Origin',(0.,0.,-1.84858989190501));
#28731=CARTESIAN_POINT('',(-1.37702479013099,-1.93106208855767,0.));
#28732=CARTESIAN_POINT('Ctrl Pts',(-1.37997554054992,-1.93359434039962,
-2.49583340106163E-15));
#28733=CARTESIAN_POINT('Ctrl Pts',(-0.789677438324666,-2.34979595234001,
0.0486480664188813));
#28734=CARTESIAN_POINT('Ctrl Pts',(0.870549345642383,-2.62706253801033,
0.150093709533546));
#28735=CARTESIAN_POINT('Ctrl Pts',(2.69329736340148,-0.769327930944301,
0.304336929343994));
#28736=CARTESIAN_POINT('Ctrl Pts',(2.11117816219839,1.84124601305982,0.462729659431337));
#28737=CARTESIAN_POINT('Ctrl Pts',(-0.39528737250602,2.77289693006155,0.621122389518683));
#28738=CARTESIAN_POINT('Ctrl Pts',(-2.13794957738225,1.47774671669238,0.749742467009907));
#28739=CARTESIAN_POINT('Ctrl Pts',(-2.36920067152979,0.345159485015423,
0.825564967805353));
#28740=CARTESIAN_POINT('Ctrl Pts',(-2.36815429608612,0.000817443606317657,
0.848589891905016));
#28741=CARTESIAN_POINT('Origin',(0.,0.,0.));
#28742=CARTESIAN_POINT('Ctrl Pts',(-1.03908919352509,2.13201587949044,-0.329233991005384));
#28743=CARTESIAN_POINT('Ctrl Pts',(-1.74635765611394,1.78731159118428,-0.276436414309603));
#28744=CARTESIAN_POINT('Ctrl Pts',(-2.77891474382729,0.344899083844066,
-0.17084126091804));
#28745=CARTESIAN_POINT('Ctrl Pts',(-1.80015933390001,-2.14838790817324,
-0.0124485308306951));
#28746=CARTESIAN_POINT('Ctrl Pts',(0.821513079145993,-2.67704002715534,
0.145944199256649));
#28747=CARTESIAN_POINT('Ctrl Pts',(2.69329736340148,-0.769327930944301,
0.304336929343994));
#28748=CARTESIAN_POINT('Ctrl Pts',(2.11117816219839,1.84124601305982,0.462729659431337));
#28749=CARTESIAN_POINT('Ctrl Pts',(-0.39528737250602,2.77289693006155,0.621122389518683));
#28750=CARTESIAN_POINT('Ctrl Pts',(-2.54133664906011,1.1779485971876,0.779515119606025));
#28751=CARTESIAN_POINT('Ctrl Pts',(-2.37143388856986,-1.49076941799294,
0.937907849693373));
#28752=CARTESIAN_POINT('Ctrl Pts',(-0.0402824848387021,-2.80074754850057,
1.09630057978071));
#28753=CARTESIAN_POINT('Ctrl Pts',(2.32755559974952,-1.55833818967747,1.25469330986806));
#28754=CARTESIAN_POINT('Ctrl Pts',(2.57419348860935,1.10429523958194,1.4130860399554));
#28755=CARTESIAN_POINT('Ctrl Pts',(0.474838546093255,2.76051273114501,1.57147877004275));
#28756=CARTESIAN_POINT('Ctrl Pts',(-2.05725600774418,1.90095227802787,1.72987150013009));
#28757=CARTESIAN_POINT('Ctrl Pts',(-2.71447628777791,-0.691042339108541,
1.88826423021744));
#28758=CARTESIAN_POINT('Ctrl Pts',(-0.897863084978552,-2.65325422541087,
2.04665696030478));
#28759=CARTESIAN_POINT('Ctrl Pts',(1.7370153276097,-2.19742960924133,2.20504969039212));
#28760=CARTESIAN_POINT('Ctrl Pts',(2.78886857766781,0.261018802222555,2.36344242047947));
#28761=CARTESIAN_POINT('Ctrl Pts',(1.29909191311228,2.48158786740548,2.52183515056681));
#28762=CARTESIAN_POINT('Ctrl Pts',(-1.37460948338166,2.44056701717432,2.68022788065416));
#28763=CARTESIAN_POINT('Ctrl Pts',(-2.79556332719592,0.175340213572512,
2.8386206107415));
#28764=CARTESIAN_POINT('Ctrl Pts',(-1.6687861293442,-2.24968248607005,2.99701334082885));
#28765=CARTESIAN_POINT('Ctrl Pts',(0.978835944215164,-2.62446160086853,
3.15540607091619));
#28766=CARTESIAN_POINT('Ctrl Pts',(2.73439785209926,-0.607442893388946,
3.31379880100354));
#28767=CARTESIAN_POINT('Ctrl Pts',(1.99797176831316,1.9631676666159,3.47219153109088));
#28768=CARTESIAN_POINT('Ctrl Pts',(-0.559301870866465,2.7446493220368,3.63058426117822));
#28769=CARTESIAN_POINT('Ctrl Pts',(-2.60685687452164,1.02480032995442,3.78897699126557));
#28770=CARTESIAN_POINT('Ctrl Pts',(-2.27865810264075,-1.62899838275098,
3.94736972135291));
#28771=CARTESIAN_POINT('Ctrl Pts',(0.126191152782097,-2.79821269277661,
4.10576245144026));
#28772=CARTESIAN_POINT('Ctrl Pts',(2.41603635476259,-1.41728148685534,4.26415518152759));
#28773=CARTESIAN_POINT('Ctrl Pts',(2.50403167886292,1.25528635446798,4.42254791161495));
#28774=CARTESIAN_POINT('Ctrl Pts',(0.309982763347203,2.78385149874581,4.58094064170228));
#28775=CARTESIAN_POINT('Ctrl Pts',(-2.16656832077059,1.77535917267124,4.73933337178964));
#28776=CARTESIAN_POINT('Ctrl Pts',(-2.66862171862793,-0.851103168495116,
4.89772610187697));
#28777=CARTESIAN_POINT('Ctrl Pts',(-0.738632074782922,-2.7019143470289,
5.05611883196433));
#28778=CARTESIAN_POINT('Ctrl Pts',(1.86450842642192,-2.09034131384488,5.21451156205166));
#28779=CARTESIAN_POINT('Ctrl Pts',(2.76843291921558,0.426260075974678,5.37290429213902));
#28780=CARTESIAN_POINT('Ctrl Pts',(1.14935163317956,2.55439020196149,5.53129702222635));
#28781=CARTESIAN_POINT('Ctrl Pts',(-1.51718895457673,2.35458194945041,5.68968975231371));
#28782=CARTESIAN_POINT('Ctrl Pts',(-2.80104243678463,0.00893016793130419,
5.84808248240103));
#28783=CARTESIAN_POINT('Ctrl Pts',(-1.53217152184201,-2.34486010419053,
6.0064752124884));
#28784=CARTESIAN_POINT('Ctrl Pts',(1.13304083122442,-2.56166683144901,6.16486794257572));
#28785=CARTESIAN_POINT('Ctrl Pts',(2.76565869916243,-0.443903638546721,
6.32326067266308));
#28786=CARTESIAN_POINT('Ctrl Pts',(1.87779906814186,2.07841024349223,6.48165340275042));
#28787=CARTESIAN_POINT('Ctrl Pts',(-0.721388970917745,2.70656912588725,
6.64004613283776));
#28788=CARTESIAN_POINT('Ctrl Pts',(-2.66314062068401,0.868101673210355,
6.79843886292512));
#28789=CARTESIAN_POINT('Ctrl Pts',(-2.17784441634251,-1.76150849523174,
6.95683159301245));
#28790=CARTESIAN_POINT('Ctrl Pts',(0.292225921295444,-2.78577143561543,
7.11522432309981));
#28791=CARTESIAN_POINT('Ctrl Pts',(2.49597675267592,-1.27122717508287,7.27361705318714));
#28792=CARTESIAN_POINT('Ctrl Pts',(2.42502418520658,1.40184741742138,7.43200978327449));
#28793=CARTESIAN_POINT('Ctrl Pts',(0.144030698698804,2.79735118252968,7.59040251336184));
#28794=CARTESIAN_POINT('Ctrl Pts',(-2.26822487569406,1.64349456763645,7.74879524344916));
#28795=CARTESIAN_POINT('Ctrl Pts',(-2.61333826674507,-1.00815751950462,
7.90718797353653));
#28796=CARTESIAN_POINT('Ctrl Pts',(-0.576791078891976,-2.74102727674834,
8.06558070362385));
#28797=CARTESIAN_POINT('Ctrl Pts',(1.9854134998704,-1.97586733236324,8.22397343371122));
#28798=CARTESIAN_POINT('Ctrl Pts',(2.73821547444757,0.589995335628766,8.38236616379854));
#28799=CARTESIAN_POINT('Ctrl Pts',(0.995550277773485,2.61816693986326,8.54075889388591));
#28800=CARTESIAN_POINT('Ctrl Pts',(-1.65440766437566,2.26027736364875,8.69915162397323));
#28801=CARTESIAN_POINT('Ctrl Pts',(-2.79662450548933,-0.15751144677259,
8.85754435406059));
#28802=CARTESIAN_POINT('Ctrl Pts',(-1.39014322226223,-2.43175251663614,
9.01593708414793));
#28803=CARTESIAN_POINT('Ctrl Pts',(1.2832422936176,-2.48982081613093,9.17432981423527));
#28804=CARTESIAN_POINT('Ctrl Pts',(2.78714752338885,-0.278795917178183,
9.33272254432263));
#28805=CARTESIAN_POINT('Ctrl Pts',(1.75099145741626,2.18630908076216,9.49111527440996));
#28806=CARTESIAN_POINT('Ctrl Pts',(-0.880927155331511,2.6589256904937,9.64950800449731));
#28807=CARTESIAN_POINT('Ctrl Pts',(-2.71001457495083,0.708335714278131,
9.80790073458465));
#28808=CARTESIAN_POINT('Ctrl Pts',(-2.06933565641643,-1.88779459201775,
9.966293464672));
#28809=CARTESIAN_POINT('Ctrl Pts',(0.457228155062243,-2.76348708967243,
10.1246861947593));
#28810=CARTESIAN_POINT('Ctrl Pts',(2.56709800604834,-1.12068118031423,10.2830789248467));
#28811=CARTESIAN_POINT('Ctrl Pts',(2.33744824681434,1.54345527114731,10.441471654934));
#28812=CARTESIAN_POINT('Ctrl Pts',(-0.0224302759543461,2.80096686222604,
10.5998643850214));
#28813=CARTESIAN_POINT('Ctrl Pts',(-2.36186701179702,1.5058229308763,10.7582571151087));
#28814=CARTESIAN_POINT('Ctrl Pts',(-2.54882099169811,-1.16164970315792,
10.9166498451961));
#28815=CARTESIAN_POINT('Ctrl Pts',(-0.412912081686591,-2.77045521410563,
11.0750425752834));
#28816=CARTESIAN_POINT('Ctrl Pts',(2.09930342438264,-1.85441193183801,11.2334353053708));
#28817=CARTESIAN_POINT('Ctrl Pts',(2.69832297238025,0.751645938785551,11.3918280354581));
#28818=CARTESIAN_POINT('Ctrl Pts',(0.838231300737091,2.67269279323914,11.5502207655454));
#28819=CARTESIAN_POINT('Ctrl Pts',(-1.78578078273074,2.15798644031825,11.7086134956328));
#28820=CARTESIAN_POINT('Ctrl Pts',(-2.78232513769374,-0.323396519346309,
11.8670062257201));
#28821=CARTESIAN_POINT('Ctrl Pts',(-1.24320306842743,-2.51005271084502,
12.0253989558075));
#28822=CARTESIAN_POINT('Ctrl Pts',(1.42890961951376,-2.40917740729671,12.1837916858948));
#28823=CARTESIAN_POINT('Ctrl Pts',(2.79878839655315,-0.112703113920128,
12.3421844159822));
#28824=CARTESIAN_POINT('Ctrl Pts',(1.61799699147824,2.28648293589416,12.5005771460695));
#28825=CARTESIAN_POINT('Ctrl Pts',(-1.03735272104025,2.60188735588576,12.6589698761568));
#28826=CARTESIAN_POINT('Ctrl Pts',(-2.7473131153984,0.546066961578709,12.8173626062442));
#28827=CARTESIAN_POINT('Ctrl Pts',(-1.95351522170293,-2.00741046105244,
12.9757553363315));
#28828=CARTESIAN_POINT('Ctrl Pts',(0.620614844457064,-2.73143839311951,
13.1341480664189));
#28829=CARTESIAN_POINT('Ctrl Pts',(2.62914881900703,-0.966175433387754,
13.2925407965062));
#28830=CARTESIAN_POINT('Ctrl Pts',(2.24161329961403,1.67960956640559,13.4509335265936));
#28831=CARTESIAN_POINT('Ctrl Pts',(-0.18881199672574,2.79468576238185,13.6093262566809));
#28832=CARTESIAN_POINT('Ctrl Pts',(-2.44716385919473,1.36283070365345,13.7677189867683));
#28833=CARTESIAN_POINT('Ctrl Pts',(-2.47529785521649,-1.31103737876807,
13.9261117168556));
#28834=CARTESIAN_POINT('Ctrl Pts',(-0.247574124043378,-2.79009418007158,
14.084504446943));
#28835=CARTESIAN_POINT('Ctrl Pts',(2.20577578767506,-1.72640425598558,14.2428971770303));
#28836=CARTESIAN_POINT('Ctrl Pts',(2.64889636694473,0.910640718254001,14.4012899071176));
#28837=CARTESIAN_POINT('Ctrl Pts',(0.677950564144521,2.71777510348644,14.559682637205));
#28838=CARTESIAN_POINT('Ctrl Pts',(-1.91084412322983,2.04807060848979,14.7180753672923));
#28839=CARTESIAN_POINT('Ctrl Pts',(-2.75819485796213,-0.488138920773397,
14.8764680973797));
#28840=CARTESIAN_POINT('Ctrl Pts',(-1.09187025049414,-2.57948402526614,
15.034860827467));
#28841=CARTESIAN_POINT('Ctrl Pts',(1.56952811621541,-2.32002154590554,15.1932535575544));
#28842=CARTESIAN_POINT('Ctrl Pts',(2.80054018729513,0.0537879083119886,
15.3516462876417));
#28843=CARTESIAN_POINT('Ctrl Pts',(1.47928558581743,2.37857786000547,15.510039017729));
#28844=CARTESIAN_POINT('Ctrl Pts',(-1.19011296325406,2.53565565848489,15.6684317478164));
#28845=CARTESIAN_POINT('Ctrl Pts',(-2.77490445240338,0.381868765748693,
15.8268244779037));
#28846=CARTESIAN_POINT('Ctrl Pts',(-1.83079234764519,-2.11993345699756,
15.9852172079911));
#28847=CARTESIAN_POINT('Ctrl Pts',(0.781808691918871,-2.68973858755105,
16.1436099380784));
#28848=CARTESIAN_POINT('Ctrl Pts',(2.68190993738254,-0.808255851442284,
16.3020026681657));
#28849=CARTESIAN_POINT('Ctrl Pts',(2.137857975385,1.80982921402577,16.4603953982531));
#28850=CARTESIAN_POINT('Ctrl Pts',(-0.354526606378597,2.77853009386107,
16.6187881283404));
#28851=CARTESIAN_POINT('Ctrl Pts',(-2.52381398393833,1.21502309313244,16.7771808584278));
#28852=CARTESIAN_POINT('Ctrl Pts',(-2.39302873693005,-1.45579264417825,
16.9355735885151));
#28853=CARTESIAN_POINT('Ctrl Pts',(-0.0813612164248821,-2.79987490584551,
17.0939663186025));
#28854=CARTESIAN_POINT('Ctrl Pts',(2.3044540321531,-1.59229636617095,17.2523590486898));
#28855=CARTESIAN_POINT('Ctrl Pts',(2.59011097558326,1.0664174443023,17.4107517787772));
#28856=CARTESIAN_POINT('Ctrl Pts',(0.515273103550636,2.75325543193802,17.5691445088645));
#28857=CARTESIAN_POINT('Ctrl Pts',(-2.02915332780205,1.93091661030183,17.7275372389519));
#28858=CARTESIAN_POINT('Ctrl Pts',(-2.72432363673881,-0.651153449862876,
17.8859299690392));
#28859=CARTESIAN_POINT('Ctrl Pts',(-0.936670484863442,-2.63980707365487,
18.0443226991266));
#28860=CARTESIAN_POINT('Ctrl Pts',(1.70458375322942,-2.22265690947637,18.2027154292139));
#28861=CARTESIAN_POINT('Ctrl Pts',(2.7924295091237,0.220067221674903,18.3611081593012));
#28862=CARTESIAN_POINT('Ctrl Pts',(1.33528471034559,2.46230981068379,18.5195008893886));
#28863=CARTESIAN_POINT('Ctrl Pts',(-1.33854848928615,2.46038562697746,18.6778936194759));
#28864=CARTESIAN_POINT('Ctrl Pts',(-2.79291960316285,0.216472177012814,
18.8362863495633));
#28865=CARTESIAN_POINT('Ctrl Pts',(-1.7011639917225,-2.22525441833135,18.9946790796506));
#28866=CARTESIAN_POINT('Ctrl Pts',(0.939403752255799,-2.63798173542721,
19.153071809738));
#28867=CARTESIAN_POINT('Ctrl Pts',(2.72681418428107,-0.648558891555657,
19.3114645398253));
#28868=CARTESIAN_POINT('Ctrl Pts',(2.02326260265721,1.93590572399224,19.4698572699127));
#28869=CARTESIAN_POINT('Ctrl Pts',(0.333728659905137,2.4764638032096,19.5754524233042));
#28870=CARTESIAN_POINT('Ctrl Pts',(-0.439445221994122,2.33068358199189,
19.62825));
#28871=CARTESIAN_POINT('Ctrl Pts',(-1.12236674703447,2.30288577939268,-0.219489327336923));
#28872=CARTESIAN_POINT('Ctrl Pts',(-1.88631907045622,1.93055524880318,-0.166691750641141));
#28873=CARTESIAN_POINT('Ctrl Pts',(-3.00163019762969,0.372540937968967,
-0.0610965972495787));
#28874=CARTESIAN_POINT('Ctrl Pts',(-1.94443267076893,-2.32056994037671,
0.0972961328377661));
#28875=CARTESIAN_POINT('Ctrl Pts',(0.887353047296498,-2.8915907562914,0.25568886292511));
#28876=CARTESIAN_POINT('Ctrl Pts',(2.90915103284102,-0.830985532942982,
0.414081593012455));
#28877=CARTESIAN_POINT('Ctrl Pts',(2.28037802825984,1.98881223194844,0.572474323099799));
#28878=CARTESIAN_POINT('Ctrl Pts',(-0.426967583907085,2.995130087627,0.730867053187144));
#28879=CARTESIAN_POINT('Ctrl Pts',(-2.745011463596,1.27235500420722,0.889259783274488));
#28880=CARTESIAN_POINT('Ctrl Pts',(-2.56149188722866,-1.61024677446114,
1.04765251336183));
#28881=CARTESIAN_POINT('Ctrl Pts',(-0.0435109148979961,-3.02521278718262,
1.20604524344918));
#28882=CARTESIAN_POINT('Ctrl Pts',(2.51409698350372,-1.68323082910176,1.36443797353652));
#28883=CARTESIAN_POINT('Ctrl Pts',(2.78050160664871,1.19279871597019,1.52283070362387));
#28884=CARTESIAN_POINT('Ctrl Pts',(0.512894367169087,2.98175336006676,1.68122343371121));
#28885=CARTESIAN_POINT('Ctrl Pts',(-2.2221342957054,2.05330364116276,1.83961616379856));
#28886=CARTESIAN_POINT('Ctrl Pts',(-2.93202733701797,-0.74642576117755,
1.9980088938859));
#28887=CARTESIAN_POINT('Ctrl Pts',(-0.969822105984018,-2.86589864718671,
2.15640162397324));
#28888=CARTESIAN_POINT('Ctrl Pts',(1.87622800328088,-2.37354207678217,2.31479435406059));
#28889=CARTESIAN_POINT('Ctrl Pts',(3.01238177908942,0.281938091350456,2.47318708414793));
#28890=CARTESIAN_POINT('Ctrl Pts',(1.40320732205116,2.68047413020551,2.63157981423527));
#28891=CARTESIAN_POINT('Ctrl Pts',(-1.48477722982743,2.63616567379829,2.78997254432262));
#28892=CARTESIAN_POINT('Ctrl Pts',(-3.01961307770834,0.189392812819178,
2.94836527440996));
#28893=CARTESIAN_POINT('Ctrl Pts',(-1.80253059232985,-2.42998274785725,
3.10675800449731));
#28894=CARTESIAN_POINT('Ctrl Pts',(1.05728451554978,-2.83479844467519,3.26515073458465));
#28895=CARTESIAN_POINT('Ctrl Pts',(2.95354551032062,-0.656126257986841,
3.423543464672));
#28896=CARTESIAN_POINT('Ctrl Pts',(2.15809873516333,2.12050526710607,3.58193619475934));
#28897=CARTESIAN_POINT('Ctrl Pts',(-0.604126984792399,2.96461858185079,
3.74032892484669));
#28898=CARTESIAN_POINT('Ctrl Pts',(-2.81578279176923,1.1069327059295,3.89872165493403));
#28899=CARTESIAN_POINT('Ctrl Pts',(-2.46128060824926,-1.75955406635503,
4.05711438502138));
#28900=CARTESIAN_POINT('Ctrl Pts',(0.136304712372256,-3.0224747760563,4.21550711510872));
#28901=CARTESIAN_POINT('Ctrl Pts',(2.60966900734729,-1.53086917075673,4.37389984519606));
#28902=CARTESIAN_POINT('Ctrl Pts',(2.70471669553439,1.35589097744473,4.5322925752834));
#28903=CARTESIAN_POINT('Ctrl Pts',(0.334826257363418,3.00696260758384,4.69068530537076));
#28904=CARTESIAN_POINT('Ctrl Pts',(-2.3402074177692,1.91764490658303,4.8490780354581));
#28905=CARTESIAN_POINT('Ctrl Pts',(-2.88249776445171,-0.919314627239958,
5.00747076554544));
#28906=CARTESIAN_POINT('Ctrl Pts',(-0.797829564772043,-2.91845862254883,
5.16586349563279));
#28907=CARTESIAN_POINT('Ctrl Pts',(2.01393900583474,-2.25787121570639,5.32425622572012));
#28908=CARTESIAN_POINT('Ctrl Pts',(2.9903083097054,0.460422587246163,5.48264895580748));
#28909=CARTESIAN_POINT('Ctrl Pts',(1.24146614339645,2.75911119035523,5.64104168589481));
#28910=CARTESIAN_POINT('Ctrl Pts',(-1.63878369845042,2.54328935350145,5.79943441598217));
#28911=CARTESIAN_POINT('Ctrl Pts',(-3.02553130921729,0.00964587409243157,
5.9578271460695));
#28912=CARTESIAN_POINT('Ctrl Pts',(-1.65496703996583,-2.53278835329135,
6.11621987615686));
#28913=CARTESIAN_POINT('Ctrl Pts',(1.22384811614141,-2.76697100356297,6.27461260624418));
#28914=CARTESIAN_POINT('Ctrl Pts',(2.9873117504533,-0.47948018889722,6.43300533633155));
#28915=CARTESIAN_POINT('Ctrl Pts',(2.02829482283888,2.24498393258978,6.59139806641888));
#28916=CARTESIAN_POINT('Ctrl Pts',(-0.7792045164946,2.92348645753929,6.74979079650623));
#28917=CARTESIAN_POINT('Ctrl Pts',(-2.87657738523129,0.937675473027413,
6.90818352659357));
#28918=CARTESIAN_POINT('Ctrl Pts',(-2.3523872333088,-1.90268416993127,7.06657625668092));
#28919=CARTESIAN_POINT('Ctrl Pts',(0.315646297475985,-3.00903641733213,
7.22496898676826));
#28920=CARTESIAN_POINT('Ctrl Pts',(2.69601620922536,-1.37310937129398,7.38336171685561));
#28921=CARTESIAN_POINT('Ctrl Pts',(2.61937716530061,1.51419814153992,7.54175444694295));
#28922=CARTESIAN_POINT('Ctrl Pts',(0.155574004406001,3.02154422027783,7.7001471770303));
#28923=CARTESIAN_POINT('Ctrl Pts',(-2.45001121283815,1.77521204449176,7.85853990711763));
#28924=CARTESIAN_POINT('Ctrl Pts',(-2.82278363361361,-1.08895606143883,
8.01693263720499));
#28925=CARTESIAN_POINT('Ctrl Pts',(-0.623017861188913,-2.9607062486138,
8.17532536729232));
#28926=CARTESIAN_POINT('Ctrl Pts',(2.14453398731652,-2.13422274451042,8.33371809737967));
#28927=CARTESIAN_POINT('Ctrl Pts',(2.95766909509389,0.637280369906155,8.49211082746702));
#28928=CARTESIAN_POINT('Ctrl Pts',(1.07533841535129,2.82799929957753,8.65050355755435));
#28929=CARTESIAN_POINT('Ctrl Pts',(-1.78699976874446,2.4414267493514,8.8088962876417));
#28930=CARTESIAN_POINT('Ctrl Pts',(-3.02075930388085,-0.170135163791943,
8.96728901772905));
#28931=CARTESIAN_POINT('Ctrl Pts',(-1.50155591647468,-2.62664473723439,
9.12568174781639));
#28932=CARTESIAN_POINT('Ctrl Pts',(1.38608743861396,-2.68936690662652,9.28407447790374));
#28933=CARTESIAN_POINT('Ctrl Pts',(3.01052279132919,-0.301139948908758,
9.44246720799109));
#28934=CARTESIAN_POINT('Ctrl Pts',(1.89132424664949,2.36153029622255,9.60085993807842));
#28935=CARTESIAN_POINT('Ctrl Pts',(-0.95152885032855,2.87202465047459,9.75925266816578));
#28936=CARTESIAN_POINT('Ctrl Pts',(-2.92720804128942,0.765105109741005,
9.9176453982531));
#28937=CARTESIAN_POINT('Ctrl Pts',(-2.23518206491529,-2.03909143557181,
10.0760381283405));
#28938=CARTESIAN_POINT('Ctrl Pts',(0.493872595584237,-2.98496609784301,
10.2344308584278));
#28939=CARTESIAN_POINT('Ctrl Pts',(2.77283745834433,-1.2104979039816,10.3928235885152));
#28940=CARTESIAN_POINT('Ctrl Pts',(2.52478247438834,1.66715512264539,10.5512163186025));
#28941=CARTESIAN_POINT('Ctrl Pts',(-0.0242279450261061,3.02544967775387,
10.7096090486898));
#28942=CARTESIAN_POINT('Ctrl Pts',(-2.55115827541772,1.62650674751413,10.8680017787772));
#28943=CARTESIAN_POINT('Ctrl Pts',(-2.75309563707472,-1.25474983923546,
11.0263945088645));
#28944=CARTESIAN_POINT('Ctrl Pts',(-0.446004821166146,-2.99249268093304,
11.1847872389519));
#28945=CARTESIAN_POINT('Ctrl Pts',(2.26755159243775,-2.00303333012067,11.3431799690392));
#28946=CARTESIAN_POINT('Ctrl Pts',(2.91457941804272,0.811886421775233,11.5015726991266));
#28947=CARTESIAN_POINT('Ctrl Pts',(0.905411146736239,2.88689511435851,11.6599654292139));
#28948=CARTESIAN_POINT('Ctrl Pts',(-1.92890175407427,2.33093774457201,11.8183581593013));
#28949=CARTESIAN_POINT('Ctrl Pts',(-3.00531391669236,-0.349315055610967,
11.9767508893886));
#28950=CARTESIAN_POINT('Ctrl Pts',(-1.34283927935057,-2.71122028167659,
12.1351436194759));
#28951=CARTESIAN_POINT('Ctrl Pts',(1.54342923731041,-2.60226035118638,12.2935363495633));
#28952=CARTESIAN_POINT('Ctrl Pts',(3.02309661947356,-0.121735677879665,
12.4519290796506));
#28953=CARTESIAN_POINT('Ctrl Pts',(1.74767097122464,2.46973256088184,12.610321809738));
#28954=CARTESIAN_POINT('Ctrl Pts',(-1.12049110537995,2.81041499225748,12.7687145398253));
#28955=CARTESIAN_POINT('Ctrl Pts',(-2.9674958642907,0.589831366882863,12.9271072699127));
#28956=CARTESIAN_POINT('Ctrl Pts',(-2.11007922931703,-2.16829388966213,
13.0855));
#28957=CARTESIAN_POINT('Ctrl Pts',(0.670353871905365,-2.95034886621271,
13.2438927300873));
#28958=CARTESIAN_POINT('Ctrl Pts',(2.83986131878408,-1.04360933112704,13.4022854601747));
#28959=CARTESIAN_POINT('Ctrl Pts',(2.4212668583934,1.81422147115141,13.560678190262));
#28960=CARTESIAN_POINT('Ctrl Pts',(-0.203944288793164,3.01866518067329,
13.7190709203494));
#28961=CARTESIAN_POINT('Ctrl Pts',(-2.64329121813584,1.47205444263079,13.8774636504367));
#28962=CARTESIAN_POINT('Ctrl Pts',(-2.67368000650243,-1.41611015417897,
14.0358563805241));
#28963=CARTESIAN_POINT('Ctrl Pts',(-0.267415892672147,-3.01370560710306,
14.1942491106114));
#28964=CARTESIAN_POINT('Ctrl Pts',(2.38255715767915,-1.86476650987348,14.3526418406987));
#28965=CARTESIAN_POINT('Ctrl Pts',(2.86119152920189,0.983623799605217,14.5110345707861));
#28966=CARTESIAN_POINT('Ctrl Pts',(0.732284749057705,2.93559053551808,14.6694273008734));
#28967=CARTESIAN_POINT('Ctrl Pts',(-2.06398826591936,2.21221273483691,14.8278200309608));
#28968=CARTESIAN_POINT('Ctrl Pts',(-2.9792497214951,-0.527260697179135,
14.9862127610481));
#28969=CARTESIAN_POINT('Ctrl Pts',(-1.17937792912025,-2.78621615209345,
15.1446054911355));
#28970=CARTESIAN_POINT('Ctrl Pts',(1.69531756961083,-2.50595911472641,15.3029982212228));
#28971=CARTESIAN_POINT('Ctrl Pts',(3.02498880706324,0.0580987272874007,
15.4613909513102));
#28972=CARTESIAN_POINT('Ctrl Pts',(1.59784257331787,2.5692084105368,15.6197836813975));
#28973=CARTESIAN_POINT('Ctrl Pts',(-1.28549428046646,2.73887517139744,15.7781764114849));
#28974=CARTESIAN_POINT('Ctrl Pts',(-2.9972985023641,0.412473546138461,15.9365691415722));
#28975=CARTESIAN_POINT('Ctrl Pts',(-1.97752076003333,-2.28983501405497,
16.0949618716595));
#28976=CARTESIAN_POINT('Ctrl Pts',(0.844466561504143,-2.90530703975596,
16.2533546017469));
#28977=CARTESIAN_POINT('Ctrl Pts',(2.89685096430251,-0.873033322266933,
16.4117473318342));
#28978=CARTESIAN_POINT('Ctrl Pts',(2.30919608865767,1.95487754111169,16.5701400619216));
#28979=CARTESIAN_POINT('Ctrl Pts',(-0.382940055981533,3.00121471998444,
16.7285327920089));
#28980=CARTESIAN_POINT('Ctrl Pts',(-2.72608444869231,1.31240082671298,16.8869255220963));
#28981=CARTESIAN_POINT('Ctrl Pts',(-2.58481744951702,-1.57246679552115,
17.0453182521836));
#28982=CARTESIAN_POINT('Ctrl Pts',(-0.0878818915475249,-3.02427020679184,
17.203710982271));
#28983=CARTESIAN_POINT('Ctrl Pts',(2.48914394632831,-1.71991057548322,17.3621037123583));
#28984=CARTESIAN_POINT('Ctrl Pts',(2.79769479678791,1.15188521389764,17.5204964424456));
#28985=CARTESIAN_POINT('Ctrl Pts',(0.55656954250919,2.97391442636023,17.678889172533));
#28986=CARTESIAN_POINT('Ctrl Pts',(-2.19177933323813,2.08566945764025,17.8372819026204));
#28987=CARTESIAN_POINT('Ctrl Pts',(-2.94266389939302,-0.703339986496753,
17.9956746327076));
#28988=CARTESIAN_POINT('Ctrl Pts',(-1.01173971559932,-2.85137377668732,
18.1540673627951));
#28989=CARTESIAN_POINT('Ctrl Pts',(1.84119720817182,-2.40079121292726,18.3124600928823));
#28990=CARTESIAN_POINT('Ctrl Pts',(3.01622810054042,0.237704456228855,18.4708528229697));
#28991=CARTESIAN_POINT('Ctrl Pts',(1.4423007823142,2.65965103826431,18.629245553057));
#28992=CARTESIAN_POINT('Ctrl Pts',(-1.44582613603297,2.65757264131764,18.7876382831444));
#28993=CARTESIAN_POINT('Ctrl Pts',(-3.01675747304847,0.233821287576979,
18.9460310132317));
#28994=CARTESIAN_POINT('Ctrl Pts',(-1.83750337070143,-2.40359689850469,
19.1044237433191));
#28995=CARTESIAN_POINT('Ctrl Pts',(1.01469204004945,-2.84940214716642,19.2628164734064));
#28996=CARTESIAN_POINT('Ctrl Pts',(2.94535405126905,-0.700537487938037,
19.4212092034938));
#28997=CARTESIAN_POINT('Ctrl Pts',(2.18541649734332,2.09105842264745,19.5796019335811));
#28998=CARTESIAN_POINT('Ctrl Pts',(0.360475263089987,2.67493939911702,19.6851970869727));
#28999=CARTESIAN_POINT('Ctrl Pts',(-0.474664453622252,2.51747565713062,
19.7379946636685));
#29000=CARTESIAN_POINT('Ctrl Pts',(-1.20564430054384,2.47375567929493,-0.109744663668461));
#29001=CARTESIAN_POINT('Ctrl Pts',(-2.02628048479849,2.07379890642209,-0.0569470869726798));
#29002=CARTESIAN_POINT('Ctrl Pts',(-3.22434565143208,0.400182792093866,
0.0486480664188827));
#29003=CARTESIAN_POINT('Ctrl Pts',(-2.08870600763785,-2.49275197258017,
0.207040796506227));
#29004=CARTESIAN_POINT('Ctrl Pts',(0.953193015447007,-3.10614148542747,
0.365433526593571));
#29005=CARTESIAN_POINT('Ctrl Pts',(3.12500470228055,-0.892643134941659,
0.523826256680916));
#29006=CARTESIAN_POINT('Ctrl Pts',(2.44957789432129,2.13637845083706,0.68221898676826));
#29007=CARTESIAN_POINT('Ctrl Pts',(-0.458647795308153,3.21736324519246,
0.840611716855605));
#29008=CARTESIAN_POINT('Ctrl Pts',(-2.94868627813188,1.36676141122684,0.999004446942949));
#29009=CARTESIAN_POINT('Ctrl Pts',(-2.75154988588746,-1.72972413092935,
1.15739717703029));
#29010=CARTESIAN_POINT('Ctrl Pts',(-0.0467393449572904,-3.24967802586467,
1.31578990711764));
#29011=CARTESIAN_POINT('Ctrl Pts',(2.70063836725792,-1.80812346852605,1.47418263720498));
#29012=CARTESIAN_POINT('Ctrl Pts',(2.98680972468806,1.28130219235844,1.63257536729233));
#29013=CARTESIAN_POINT('Ctrl Pts',(0.550950188244917,3.2029939889885,1.79096809737967));
#29014=CARTESIAN_POINT('Ctrl Pts',(-2.38701258366662,2.20565500429764,1.94936082746702));
#29015=CARTESIAN_POINT('Ctrl Pts',(-3.14957838625804,-0.80180918324656,
2.10775355755436));
#29016=CARTESIAN_POINT('Ctrl Pts',(-1.04178112698948,-3.07854306896254,
2.2661462876417));
#29017=CARTESIAN_POINT('Ctrl Pts',(2.01544067895206,-2.549654544323,2.42453901772905));
#29018=CARTESIAN_POINT('Ctrl Pts',(3.23589498051102,0.302857380478356,2.58293174781639));
#29019=CARTESIAN_POINT('Ctrl Pts',(1.50732273099005,2.87936039300554,2.74132447790374));
#29020=CARTESIAN_POINT('Ctrl Pts',(-1.5949449762732,2.83176433042226,2.89971720799108));
#29021=CARTESIAN_POINT('Ctrl Pts',(-3.24366282822075,0.203445412065843,
3.05810993807843));
#29022=CARTESIAN_POINT('Ctrl Pts',(-1.9362750553155,-2.61028300964445,3.21650266816577));
#29023=CARTESIAN_POINT('Ctrl Pts',(1.13573308688439,-3.04513528848185,3.37489539825311));
#29024=CARTESIAN_POINT('Ctrl Pts',(3.17269316854199,-0.704809622584737,
3.53328812834046));
#29025=CARTESIAN_POINT('Ctrl Pts',(2.31822570201349,2.27784286759623,3.69168085842781));
#29026=CARTESIAN_POINT('Ctrl Pts',(-0.648952098718329,3.18458784166478,
3.85007358851515));
#29027=CARTESIAN_POINT('Ctrl Pts',(-3.02470870901682,1.18906508190457,4.00846631860249));
#29028=CARTESIAN_POINT('Ctrl Pts',(-2.64390311385777,-1.89010974995907,
4.16685904868984));
#29029=CARTESIAN_POINT('Ctrl Pts',(0.146418271962415,-3.246736859336,4.32525177877718));
#29030=CARTESIAN_POINT('Ctrl Pts',(2.80330165993199,-1.64445685465812,4.48364450886452));
#29031=CARTESIAN_POINT('Ctrl Pts',(2.90540171220585,1.45649560042147,4.64203723895187));
#29032=CARTESIAN_POINT('Ctrl Pts',(0.359669751379629,3.23007371642187,4.80042996903921));
#29033=CARTESIAN_POINT('Ctrl Pts',(-2.5138465147678,2.05993064049482,4.95882269912656));
#29034=CARTESIAN_POINT('Ctrl Pts',(-3.09637381027549,-0.987526085984799,
5.1172154292139));
#29035=CARTESIAN_POINT('Ctrl Pts',(-0.857027054761158,-3.13500289806876,
5.27560815930125));
#29036=CARTESIAN_POINT('Ctrl Pts',(2.16336958524755,-2.4254011175679,5.43400088938859));
#29037=CARTESIAN_POINT('Ctrl Pts',(3.21218370019522,0.494585098517652,5.59239361947593));
#29038=CARTESIAN_POINT('Ctrl Pts',(1.33358065361335,2.96383217874895,5.75078634956329));
#29039=CARTESIAN_POINT('Ctrl Pts',(-1.76037844232411,2.73199675755249,5.90917907965061));
#29040=CARTESIAN_POINT('Ctrl Pts',(-3.25002018164994,0.0103615802535554,
6.06757180973798));
#29041=CARTESIAN_POINT('Ctrl Pts',(-1.77776255808964,-2.72071660239216,
6.2259645398253));
#29042=CARTESIAN_POINT('Ctrl Pts',(1.3146554010584,-2.97227517567693,6.38435726991266));
#29043=CARTESIAN_POINT('Ctrl Pts',(3.20896480174417,-0.515056739247718,
6.54275));
#29044=CARTESIAN_POINT('Ctrl Pts',(2.1787905775359,2.41155762168733,6.70114273008734));
#29045=CARTESIAN_POINT('Ctrl Pts',(-0.837020062071456,3.14040378919134,
6.85953546017469));
#29046=CARTESIAN_POINT('Ctrl Pts',(-3.09001414977857,1.00724927284447,7.01792819026203));
#29047=CARTESIAN_POINT('Ctrl Pts',(-2.52693005027509,-2.04385984463079,
7.17632092034938));
#29048=CARTESIAN_POINT('Ctrl Pts',(0.339066673656528,-3.23230139904882,
7.33471365043672));
#29049=CARTESIAN_POINT('Ctrl Pts',(2.8960556657748,-1.47499156750509,7.49310638052407));
#29050=CARTESIAN_POINT('Ctrl Pts',(2.81373014539465,1.62654886565846,7.6514991106114));
#29051=CARTESIAN_POINT('Ctrl Pts',(0.167117310113194,3.24573725802598,7.80989184069877));
#29052=CARTESIAN_POINT('Ctrl Pts',(-2.63179754998223,1.90692952134707,7.96828457078609));
#29053=CARTESIAN_POINT('Ctrl Pts',(-3.03222900048216,-1.16975460337304,
8.12667730087346));
#29054=CARTESIAN_POINT('Ctrl Pts',(-0.669244643485845,-3.18038522047927,
8.28507003096078));
#29055=CARTESIAN_POINT('Ctrl Pts',(2.30365447476264,-2.2925781566576,8.44346276104813));
#29056=CARTESIAN_POINT('Ctrl Pts',(3.17712271574022,0.68456540418354,8.60185549113548));
#29057=CARTESIAN_POINT('Ctrl Pts',(1.15512655292908,3.03783165929181,8.76024822122282));
#29058=CARTESIAN_POINT('Ctrl Pts',(-1.91959187311326,2.62257613505404,8.91864095131017));
#29059=CARTESIAN_POINT('Ctrl Pts',(-3.24489410227238,-0.182758880811296,
9.0770336813975));
#29060=CARTESIAN_POINT('Ctrl Pts',(-1.61296861068713,-2.82153695783264,
9.23542641148485));
#29061=CARTESIAN_POINT('Ctrl Pts',(1.48893258361032,-2.8889129971221,9.3938191415722));
#29062=CARTESIAN_POINT('Ctrl Pts',(3.23389805926952,-0.323483980639333,
9.55221187165954));
#29063=CARTESIAN_POINT('Ctrl Pts',(2.03165703588272,2.53675151168294,9.71060460174689));
#29064=CARTESIAN_POINT('Ctrl Pts',(-1.02213054532559,3.08512361045549,9.86899733183423));
#29065=CARTESIAN_POINT('Ctrl Pts',(-3.14440150762802,0.821874505203878,
10.0273900619216));
#29066=CARTESIAN_POINT('Ctrl Pts',(-2.40102847341415,-2.19038827912587,
10.1857827920089));
#29067=CARTESIAN_POINT('Ctrl Pts',(0.530517036106232,-3.2064451060136,10.3441755220963));
#29068=CARTESIAN_POINT('Ctrl Pts',(2.97857691064031,-1.30031462764898,10.5025682521836));
#29069=CARTESIAN_POINT('Ctrl Pts',(2.71211670196235,1.79085497414346,10.660960982271));
#29070=CARTESIAN_POINT('Ctrl Pts',(-0.0260256140978684,3.24993249328171,
10.8193537123583));
#29071=CARTESIAN_POINT('Ctrl Pts',(-2.74044953903841,1.74719056415196,10.9777464424457));
#29072=CARTESIAN_POINT('Ctrl Pts',(-2.95737028245133,-1.34784997531299,
11.136139172533));
#29073=CARTESIAN_POINT('Ctrl Pts',(-0.479097560645698,-3.21453014776045,
11.2945319026203));
#29074=CARTESIAN_POINT('Ctrl Pts',(2.43579976049286,-2.15165472840333,11.4529246327077));
#29075=CARTESIAN_POINT('Ctrl Pts',(3.13083586370518,0.872126904764919,11.611317362795));
#29076=CARTESIAN_POINT('Ctrl Pts',(0.972590992735389,3.10109743547788,11.7697100928824));
#29077=CARTESIAN_POINT('Ctrl Pts',(-2.07202272541781,2.50388904882577,11.9281028229697));
#29078=CARTESIAN_POINT('Ctrl Pts',(-3.22830269569097,-0.375233591875627,
12.0864955530571));
#29079=CARTESIAN_POINT('Ctrl Pts',(-1.44247549027371,-2.91238785250816,
12.2448882831444));
#29080=CARTESIAN_POINT('Ctrl Pts',(1.65794885510707,-2.79534329507605,12.4032810132317));
#29081=CARTESIAN_POINT('Ctrl Pts',(3.24740484239397,-0.1307682418392,12.5616737433191));
#29082=CARTESIAN_POINT('Ctrl Pts',(1.87734495097103,2.65298218586953,12.7200664734064));
#29083=CARTESIAN_POINT('Ctrl Pts',(-1.20362948971966,3.0189426286292,12.8784592034938));
#29084=CARTESIAN_POINT('Ctrl Pts',(-3.18767861318299,0.633595772187016,
13.0368519335811));
#29085=CARTESIAN_POINT('Ctrl Pts',(-2.26664323693112,-2.32917731827181,
13.1952446636685));
#29086=CARTESIAN_POINT('Ctrl Pts',(0.720092899353666,-3.16925933930592,
13.3536373937558));
#29087=CARTESIAN_POINT('Ctrl Pts',(3.05057381856114,-1.12104322886633,13.5120301238432));
#29088=CARTESIAN_POINT('Ctrl Pts',(2.60092041717278,1.94883337589723,13.6704228539305));
#29089=CARTESIAN_POINT('Ctrl Pts',(-0.219076580860588,3.24264459896475,
13.8288155840179));
#29090=CARTESIAN_POINT('Ctrl Pts',(-2.83941857707695,1.58127818160812,13.9872083141052));
#29091=CARTESIAN_POINT('Ctrl Pts',(-2.87206215778837,-1.52118292958987,
14.1456010441925));
#29092=CARTESIAN_POINT('Ctrl Pts',(-0.287257661300916,-3.23731703413455,
14.3039937742799));
#29093=CARTESIAN_POINT('Ctrl Pts',(2.55933852768325,-2.00312876376139,14.4623865043672));
#29094=CARTESIAN_POINT('Ctrl Pts',(3.07348669145905,1.05660688095643,14.6207792344546));
#29095=CARTESIAN_POINT('Ctrl Pts',(0.786618933970887,3.15340596754972,14.7791719645419));
#29096=CARTESIAN_POINT('Ctrl Pts',(-2.2171324086089,2.37635486118404,14.9375646946292));
#29097=CARTESIAN_POINT('Ctrl Pts',(-3.20030458502806,-0.566382473584868,
15.0959574247166));
#29098=CARTESIAN_POINT('Ctrl Pts',(-1.26688560774635,-2.99294827892075,
15.2543501548039));
#29099=CARTESIAN_POINT('Ctrl Pts',(1.82110702300624,-2.69189668354728,15.4127428848913));
#29100=CARTESIAN_POINT('Ctrl Pts',(3.24943742683135,0.0624095462628093,
15.5711356149786));
#29101=CARTESIAN_POINT('Ctrl Pts',(1.7163995608183,2.75983896106814,15.729528345066));
#29102=CARTESIAN_POINT('Ctrl Pts',(-1.38087559767885,2.94209468431,15.8879210751533));
#29103=CARTESIAN_POINT('Ctrl Pts',(-3.21969255232482,0.443078326528232,
16.0463138052407));
#29104=CARTESIAN_POINT('Ctrl Pts',(-2.12424917242148,-2.45973657111239,
16.204706535328));
#29105=CARTESIAN_POINT('Ctrl Pts',(0.907124431089416,-3.12087549196088,
16.3630992654154));
#29106=CARTESIAN_POINT('Ctrl Pts',(3.11179199122249,-0.937810793091581,
16.5214919955027));
#29107=CARTESIAN_POINT('Ctrl Pts',(2.48053420193034,2.09992586819762,16.6798847255901));
#29108=CARTESIAN_POINT('Ctrl Pts',(-0.411353505584467,3.2238993461078,16.8382774556774));
#29109=CARTESIAN_POINT('Ctrl Pts',(-2.92835491344629,1.40977856029352,16.9966701857647));
#29110=CARTESIAN_POINT('Ctrl Pts',(-2.77660616210399,-1.68914094686405,
17.1550629158521));
#29111=CARTESIAN_POINT('Ctrl Pts',(-0.0944025666701746,-3.24866550773817,
17.3134556459394));
#29112=CARTESIAN_POINT('Ctrl Pts',(2.67383386050354,-1.84752478479548,17.4718483760268));
#29113=CARTESIAN_POINT('Ctrl Pts',(3.00527861799256,1.23735298349299,17.6302411061141));
#29114=CARTESIAN_POINT('Ctrl Pts',(0.597865981467751,3.19457342078244,17.7886338362015));
#29115=CARTESIAN_POINT('Ctrl Pts',(-2.35440533867421,2.24042230497867,17.9470265662888));
#29116=CARTESIAN_POINT('Ctrl Pts',(-3.16100416204722,-0.75552652313063,
18.1054192963761));
#29117=CARTESIAN_POINT('Ctrl Pts',(-1.08680894633521,-3.06294047971977,
18.2638120264635));
#29118=CARTESIAN_POINT('Ctrl Pts',(1.97781066311423,-2.57892551637815,18.4222047565508));
#29119=CARTESIAN_POINT('Ctrl Pts',(3.24002669195714,0.255341690782801,18.5805974866382));
#29120=CARTESIAN_POINT('Ctrl Pts',(1.54931685428281,2.85699226584485,18.7389902167255));
#29121=CARTESIAN_POINT('Ctrl Pts',(-1.55310378277979,2.85475965565781,18.8973829468129));
#29122=CARTESIAN_POINT('Ctrl Pts',(-3.24059534293408,0.251170398141146,
19.0557756769002));
#29123=CARTESIAN_POINT('Ctrl Pts',(-1.97384274968036,-2.58193937867803,
19.2141684069875));
#29124=CARTESIAN_POINT('Ctrl Pts',(1.08998032784309,-3.06082255890563,19.3725611370749));
#29125=CARTESIAN_POINT('Ctrl Pts',(3.16389391825703,-0.752516084320418,
19.5309538671622));
#29126=CARTESIAN_POINT('Ctrl Pts',(2.34757039202943,2.24621112130266,19.6893465972496));
#29127=CARTESIAN_POINT('Ctrl Pts',(0.38722186627484,2.87341499502444,19.7949417506411));
#29128=CARTESIAN_POINT('Ctrl Pts',(-0.509883685250381,2.70426773226936,
19.8477393273369));
#29129=CARTESIAN_POINT('Ctrl Pts',(-1.28892185405322,2.64462557919718,0.));
#29130=CARTESIAN_POINT('Ctrl Pts',(-2.16624189914077,2.21704256404099,0.0527975766957814));
#29131=CARTESIAN_POINT('Ctrl Pts',(-3.44706110523448,0.427824646218769,
0.158392730087344));
#29132=CARTESIAN_POINT('Ctrl Pts',(-2.23297934450677,-2.66493400478364,
0.316785460174689));
#29133=CARTESIAN_POINT('Ctrl Pts',(1.01903298359751,-3.32069221456353,0.475178190262033));
#29134=CARTESIAN_POINT('Ctrl Pts',(3.34085837172009,-0.954300736940341,
0.633570920349377));
#29135=CARTESIAN_POINT('Ctrl Pts',(2.61877776038273,2.28394466972569,0.791963650436721));
#29136=CARTESIAN_POINT('Ctrl Pts',(-0.490328006709216,3.43959640275791,
0.950356380524067));
#29137=CARTESIAN_POINT('Ctrl Pts',(-3.15236109266777,1.46116781824645,1.10874911061141));
#29138=CARTESIAN_POINT('Ctrl Pts',(-2.94160788454626,-1.84920148739755,
1.26714184069876));
#29139=CARTESIAN_POINT('Ctrl Pts',(-0.0499677750165847,-3.47414326454672,
1.4255345707861));
#29140=CARTESIAN_POINT('Ctrl Pts',(2.88717975101212,-1.93301610795034,1.58392730087344));
#29141=CARTESIAN_POINT('Ctrl Pts',(3.19311784272742,1.36980566874669,1.74232003096079));
#29142=CARTESIAN_POINT('Ctrl Pts',(0.589006009320745,3.42423461791024,1.90071276104813));
#29143=CARTESIAN_POINT('Ctrl Pts',(-2.55189087162783,2.35800636743253,2.05910549113548));
#29144=CARTESIAN_POINT('Ctrl Pts',(-3.3671294354981,-0.857192605315573,
2.21749822122282));
#29145=CARTESIAN_POINT('Ctrl Pts',(-1.11374014799495,-3.29118749073838,
2.37589095131016));
#29146=CARTESIAN_POINT('Ctrl Pts',(2.15465335462323,-2.72576701186384,2.53428368139751));
#29147=CARTESIAN_POINT('Ctrl Pts',(3.45940818193263,0.323776669606257,2.69267641148485));
#29148=CARTESIAN_POINT('Ctrl Pts',(1.61143813992893,3.07824665580557,2.8510691415722));
#29149=CARTESIAN_POINT('Ctrl Pts',(-1.70511272271897,3.02736298704623,3.00946187165954));
#29150=CARTESIAN_POINT('Ctrl Pts',(-3.46771257873317,0.21749801131251,3.16785460174689));
#29151=CARTESIAN_POINT('Ctrl Pts',(-2.07001951830114,-2.79058327143165,
3.32624733183423));
#29152=CARTESIAN_POINT('Ctrl Pts',(1.214181658219,-3.2554721322885,3.48464006192158));
#29153=CARTESIAN_POINT('Ctrl Pts',(3.39184082676336,-0.753492987182631,
3.64303279200892));
#29154=CARTESIAN_POINT('Ctrl Pts',(2.47835266886366,2.4351804680864,3.80142552209627));
#29155=CARTESIAN_POINT('Ctrl Pts',(-0.693777212644261,3.40455710147877,
3.9598182521836));
#29156=CARTESIAN_POINT('Ctrl Pts',(-3.23363462626441,1.27119745787964,4.11821098227095));
#29157=CARTESIAN_POINT('Ctrl Pts',(-2.82652561946628,-2.02066543356311,
4.2766037123583));
#29158=CARTESIAN_POINT('Ctrl Pts',(0.156531831552572,-3.4709989426157,4.43499644244564));
#29159=CARTESIAN_POINT('Ctrl Pts',(2.9969343125167,-1.75804453855951,4.59338917253298));
#29160=CARTESIAN_POINT('Ctrl Pts',(3.10608672887731,1.55710022339821,4.75178190262033));
#29161=CARTESIAN_POINT('Ctrl Pts',(0.384513245395842,3.4531848252599,4.91017463270768));
#29162=CARTESIAN_POINT('Ctrl Pts',(-2.68748561176641,2.20221637440662,5.06856736279502));
#29163=CARTESIAN_POINT('Ctrl Pts',(-3.31024985609926,-1.05573754472964,
5.22696009288236));
#29164=CARTESIAN_POINT('Ctrl Pts',(-0.916224544750279,-3.35154717358869,
5.38535282296971));
#29165=CARTESIAN_POINT('Ctrl Pts',(2.31280016466036,-2.59293101942941,5.54374555305705));
#29166=CARTESIAN_POINT('Ctrl Pts',(3.43405909068504,0.528747609789137,5.70213828314441));
#29167=CARTESIAN_POINT('Ctrl Pts',(1.42569516383024,3.16855316714268,5.86053101323173));
#29168=CARTESIAN_POINT('Ctrl Pts',(-1.88197318619781,2.92070416160353,6.01892374331909));
#29169=CARTESIAN_POINT('Ctrl Pts',(-3.47450905408259,0.01107728641468,6.17731647340643));
#29170=CARTESIAN_POINT('Ctrl Pts',(-1.90055807621346,-2.90864485149298,
6.33570920349377));
#29171=CARTESIAN_POINT('Ctrl Pts',(1.40546268597539,-3.17757934779089,6.49410193358112));
#29172=CARTESIAN_POINT('Ctrl Pts',(3.43061785303504,-0.550633289598217,
6.65249466366846));
#29173=CARTESIAN_POINT('Ctrl Pts',(2.32928633223293,2.57813131078488,6.81088739375581));
#29174=CARTESIAN_POINT('Ctrl Pts',(-0.894835607648314,3.35732112084339,
6.96928012384315));
#29175=CARTESIAN_POINT('Ctrl Pts',(-3.30345091432585,1.07682307266153,7.1276728539305));
#29176=CARTESIAN_POINT('Ctrl Pts',(-2.70147286724138,-2.18503551933032,
7.28606558401784));
#29177=CARTESIAN_POINT('Ctrl Pts',(0.362487049837071,-3.45556638076552,
7.44445831410518));
#29178=CARTESIAN_POINT('Ctrl Pts',(3.09609512232424,-1.5768737637162,7.60285104419254));
#29179=CARTESIAN_POINT('Ctrl Pts',(3.00808312548869,1.738899589777,7.76124377427986));
#29180=CARTESIAN_POINT('Ctrl Pts',(0.178660615820388,3.46993029577413,7.91963650436722));
#29181=CARTESIAN_POINT('Ctrl Pts',(-2.81358388712632,2.03864699820239,8.07802923445455));
#29182=CARTESIAN_POINT('Ctrl Pts',(-3.2416743673507,-1.25055314530725,8.23642196454191));
#29183=CARTESIAN_POINT('Ctrl Pts',(-0.71547142578278,-3.40006419234473,
8.39481469462925));
#29184=CARTESIAN_POINT('Ctrl Pts',(2.46277496220876,-2.45093356880478,8.5532074247166));
#29185=CARTESIAN_POINT('Ctrl Pts',(3.39657633638654,0.731850438460929,8.71160015480394));
#29186=CARTESIAN_POINT('Ctrl Pts',(1.23491469050688,3.24766401900608,8.86999288489128));
#29187=CARTESIAN_POINT('Ctrl Pts',(-2.05218397748206,2.80372552075669,9.02838561497863));
#29188=CARTESIAN_POINT('Ctrl Pts',(-3.46902890066391,-0.195382597830646,
9.18677834506597));
#29189=CARTESIAN_POINT('Ctrl Pts',(-1.72438130489958,-3.01642917843089,
9.34517107515332));
#29190=CARTESIAN_POINT('Ctrl Pts',(1.59177772860667,-3.08845908761769,9.50356380524066));
#29191=CARTESIAN_POINT('Ctrl Pts',(3.45727332720986,-0.345828012369911,
9.66195653532801));
#29192=CARTESIAN_POINT('Ctrl Pts',(2.17198982511594,2.71197272714333,9.82034926541533));
#29193=CARTESIAN_POINT('Ctrl Pts',(-1.09273224032263,3.29822257043638,9.97874199550271));
#29194=CARTESIAN_POINT('Ctrl Pts',(-3.36159497396661,0.878643900666754,
10.13713472559));
#29195=CARTESIAN_POINT('Ctrl Pts',(-2.56687488191302,-2.34168512267993,
10.2955274556774));
#29196=CARTESIAN_POINT('Ctrl Pts',(0.567161476628229,-3.42792411418417,
10.4539201857647));
#29197=CARTESIAN_POINT('Ctrl Pts',(3.1843163629363,-1.39013135131635,10.6123129158521));
#29198=CARTESIAN_POINT('Ctrl Pts',(2.89945092953635,1.91455482564153,10.7707056459394));
#29199=CARTESIAN_POINT('Ctrl Pts',(-0.0278232831696277,3.47441530880954,
10.9290983760268));
#29200=CARTESIAN_POINT('Ctrl Pts',(-2.92974080265911,1.86787438078978,11.0874911061141));
#29201=CARTESIAN_POINT('Ctrl Pts',(-3.16164492782793,-1.44095011139053,
11.2458838362014));
#29202=CARTESIAN_POINT('Ctrl Pts',(-0.512190300125254,-3.43656761458786,
11.4042765662888));
#29203=CARTESIAN_POINT('Ctrl Pts',(2.60404792854797,-2.300276126686,11.5626692963761));
#29204=CARTESIAN_POINT('Ctrl Pts',(3.34709230936765,0.932367387754601,11.7210620264635));
#29205=CARTESIAN_POINT('Ctrl Pts',(1.03977083873454,3.31529975659725,11.8794547565508));
#29206=CARTESIAN_POINT('Ctrl Pts',(-2.21514369676135,2.67684035307953,12.0378474866382));
#29207=CARTESIAN_POINT('Ctrl Pts',(-3.45129147468958,-0.401152128140284,
12.1962402167255));
#29208=CARTESIAN_POINT('Ctrl Pts',(-1.54211170119684,-3.11355542333973,
12.3546329468129));
#29209=CARTESIAN_POINT('Ctrl Pts',(1.77246847290372,-2.98842623896573,12.5130256769002));
#29210=CARTESIAN_POINT('Ctrl Pts',(3.47171306531437,-0.139800805798732,
12.6714184069876));
#29211=CARTESIAN_POINT('Ctrl Pts',(2.00701893071743,2.8362318108572,12.8298111370749));
#29212=CARTESIAN_POINT('Ctrl Pts',(-1.28676787405936,3.22747026500092,12.9882038671622));
#29213=CARTESIAN_POINT('Ctrl Pts',(-3.40786136207529,0.67736017749117,13.1465965972496));
#29214=CARTESIAN_POINT('Ctrl Pts',(-2.42320724454521,-2.4900607468815,13.3049893273369));
#29215=CARTESIAN_POINT('Ctrl Pts',(0.769831926801966,-3.38816981239912,
13.4633820574243));
#29216=CARTESIAN_POINT('Ctrl Pts',(3.2612863183382,-1.19847712660562,13.6217747875116));
#29217=CARTESIAN_POINT('Ctrl Pts',(2.78057397595216,2.08344528064305,13.780167517599));
#29218=CARTESIAN_POINT('Ctrl Pts',(-0.234208872928009,3.4666240172562,13.9385602476863));
#29219=CARTESIAN_POINT('Ctrl Pts',(-3.03554593601806,1.69050192058546,14.0969529777737));
#29220=CARTESIAN_POINT('Ctrl Pts',(-3.0704443090743,-1.62625570500076,14.255345707861));
#29221=CARTESIAN_POINT('Ctrl Pts',(-0.307099429929689,-3.46092846116604,
14.4137384379484));
#29222=CARTESIAN_POINT('Ctrl Pts',(2.73611989768734,-2.14149101764928,14.5721311680357));
#29223=CARTESIAN_POINT('Ctrl Pts',(3.28578185371621,1.12958996230764,14.730523898123));
#29224=CARTESIAN_POINT('Ctrl Pts',(0.84095311888407,3.37122139958136,14.8889166282103));
#29225=CARTESIAN_POINT('Ctrl Pts',(-2.37027655129843,2.54049698753116,15.0473093582977));
#29226=CARTESIAN_POINT('Ctrl Pts',(-3.42135944856103,-0.605504249990604,
15.2057020883851));
#29227=CARTESIAN_POINT('Ctrl Pts',(-1.35439328637246,-3.19968040574805,
15.3640948184724));
#29228=CARTESIAN_POINT('Ctrl Pts',(1.94689647640166,-2.87783425236815,15.5224875485598));
#29229=CARTESIAN_POINT('Ctrl Pts',(3.47388604659947,0.0667203652382213,
15.6808802786471));
#29230=CARTESIAN_POINT('Ctrl Pts',(1.83495654831874,2.95046951159947,15.8392730087344));
#29231=CARTESIAN_POINT('Ctrl Pts',(-1.47625691489125,3.14531419722255,15.9976657388218));
#29232=CARTESIAN_POINT('Ctrl Pts',(-3.44208660228554,0.473683106918002,
16.1560584689091));
#29233=CARTESIAN_POINT('Ctrl Pts',(-2.27097758480962,-2.62963812816981,
16.3144511989965));
#29234=CARTESIAN_POINT('Ctrl Pts',(0.96978230067469,-3.33644394416579,16.4728439290838));
#29235=CARTESIAN_POINT('Ctrl Pts',(3.32673301814246,-1.00258826391623,16.6312366591711));
#29236=CARTESIAN_POINT('Ctrl Pts',(2.65187231520301,2.24497419528354,16.7896293892585));
#29237=CARTESIAN_POINT('Ctrl Pts',(-0.4397669551874,3.44658397223117,16.9480221193458));
#29238=CARTESIAN_POINT('Ctrl Pts',(-3.13062537820028,1.50715629387405,17.1064148494332));
#29239=CARTESIAN_POINT('Ctrl Pts',(-2.96839487469096,-1.80581509820695,
17.2648075795206));
#29240=CARTESIAN_POINT('Ctrl Pts',(-0.10092324179282,-3.47306080868451,
17.4232003096079));
#29241=CARTESIAN_POINT('Ctrl Pts',(2.85852377467875,-1.97513899410775,17.5815930396952));
#29242=CARTESIAN_POINT('Ctrl Pts',(3.21286243919721,1.32282075308833,17.7399857697826));
#29243=CARTESIAN_POINT('Ctrl Pts',(0.639162420426306,3.41523241520465,17.8983784998699));
#29244=CARTESIAN_POINT('Ctrl Pts',(-2.51703134411028,2.3951751523171,18.0567712299573));
#29245=CARTESIAN_POINT('Ctrl Pts',(-3.37934442470143,-0.807713059764507,
18.2151639600446));
#29246=CARTESIAN_POINT('Ctrl Pts',(-1.16187817707109,-3.27450718275222,
18.3735566901319));
#29247=CARTESIAN_POINT('Ctrl Pts',(2.11442411805664,-2.75705981982905,18.5319494202193));
#29248=CARTESIAN_POINT('Ctrl Pts',(3.46382528337386,0.272978925336754,18.6903421503066));
#29249=CARTESIAN_POINT('Ctrl Pts',(1.65633292625143,3.05433349342538,18.848734880394));
#29250=CARTESIAN_POINT('Ctrl Pts',(-1.66038142952661,3.05194666999799,19.0071276104813));
#29251=CARTESIAN_POINT('Ctrl Pts',(-3.4644332128197,0.268519508705312,19.1655203405687));
#29252=CARTESIAN_POINT('Ctrl Pts',(-2.11018212865929,-2.76028185885138,
19.323913070656));
#29253=CARTESIAN_POINT('Ctrl Pts',(1.16526861563674,-3.27224297064484,19.4823058007433));
#29254=CARTESIAN_POINT('Ctrl Pts',(3.38243378524502,-0.804494680702798,
19.6406985308307));
#29255=CARTESIAN_POINT('Ctrl Pts',(2.50972428671554,2.40136381995787,19.799091260918));
#29256=CARTESIAN_POINT('Ctrl Pts',(0.413968469459689,3.07189059093186,19.9046864143096));
#29257=CARTESIAN_POINT('Ctrl Pts',(-0.545102916878511,2.8910598074081,19.9574839910054));
#29258=CARTESIAN_POINT('Ctrl Pts',(-2.94191884508495,-0.00265442804262754,
18.1778238829104));
#29259=CARTESIAN_POINT('Ctrl Pts',(-2.94401095921365,-0.232682134900822,
18.1902705752885));
#29260=CARTESIAN_POINT('Ctrl Pts',(-2.91929265776683,-0.462265462611949,
18.2027172676665));
#29261=CARTESIAN_POINT('Ctrl Pts',(-2.86604786999785,-0.685030711582192,
18.2151639600446));
#29262=CARTESIAN_POINT('Ctrl Pts',(-2.64018900882465,-1.62997776742708,
18.2679615367404));
#29263=CARTESIAN_POINT('Ctrl Pts',(-1.90103359294787,-2.45224247508964,
18.3207591134362));
#29264=CARTESIAN_POINT('Ctrl Pts',(-0.985405502488203,-2.77713360176707,
18.3735566901319));
#29265=CARTESIAN_POINT('Ctrl Pts',(-0.0697774120285166,-3.1020247284445,
18.4263542668277));
#29266=CARTESIAN_POINT('Ctrl Pts',(1.02232335301407,-2.92954227413678,18.4791518435235));
#29267=CARTESIAN_POINT('Ctrl Pts',(1.7932739297549,-2.33829458945527,18.5319494202193));
#29268=CARTESIAN_POINT('Ctrl Pts',(2.56422450649571,-1.74704690477378,18.5847469969151));
#29269=CARTESIAN_POINT('Ctrl Pts',(3.01402489493477,-0.737033989718538,
18.6375445736108));
#29270=CARTESIAN_POINT('Ctrl Pts',(2.93767636296726,0.231531562490516,18.6903421503066));
#29271=CARTESIAN_POINT('Ctrl Pts',(2.86132783099973,1.2000971146996,18.7431397270024));
#29272=CARTESIAN_POINT('Ctrl Pts',(2.25883037862559,2.12721530406249,18.7959373036982));
#29273=CARTESIAN_POINT('Ctrl Pts',(1.40479592647551,2.59037659483937,18.848734880394));
#29274=CARTESIAN_POINT('Ctrl Pts',(0.550761474325412,3.05353788561626,18.9015324570898));
#29275=CARTESIAN_POINT('Ctrl Pts',(-0.554809977600626,3.05274227780712,
18.9543300337855));
#29276=CARTESIAN_POINT('Ctrl Pts',(-1.40827100077916,2.58843994702042,19.0071276104813));
#29277=CARTESIAN_POINT('Ctrl Pts',(-1.68238460173924,2.4393158741341,19.0240850736542));
#29278=CARTESIAN_POINT('Ctrl Pts',(-1.93049154169819,2.24237837966061,19.0410425368271));
#29279=CARTESIAN_POINT('Ctrl Pts',(-2.14350474087479,2.01162918712774,19.058));
#29280=CARTESIAN_POINT('Ctrl Pts',(-1.37997554054989,-1.93359434039964,
5.03069808033274E-17));
#29281=CARTESIAN_POINT('Ctrl Pts',(-1.43480608311011,-1.90379100615021,
4.05392308728466E-17));
#29282=CARTESIAN_POINT('Ctrl Pts',(-1.48827102383981,-1.87175009325149,
-2.56174624183488E-16));
#29283=CARTESIAN_POINT('Ctrl Pts',(-1.54021573000326,-1.83750293771675,
-2.32452945780892E-16));
#29284=CARTESIAN_POINT('Ctrl Pts',(-1.60834066683741,-1.79258815274882,
-2.34206640027434E-16));
#29285=CARTESIAN_POINT('Ctrl Pts',(-1.67385212815421,-1.74388071234801,
2.35502939941775E-16));
#29286=CARTESIAN_POINT('Ctrl Pts',(-1.7366654506395,-1.6917391145835,2.60208521396521E-16));
#29287=CARTESIAN_POINT('Ctrl Pts',(-1.77318557553109,-1.66142360846054,
2.74572527065185E-16));
#29288=CARTESIAN_POINT('Ctrl Pts',(-1.80879333390789,-1.62994627115077,
-1.27188329331984E-16));
#29289=CARTESIAN_POINT('Ctrl Pts',(-1.84346892862395,-1.59737031707875,
-1.73472347597681E-16));
#29290=CARTESIAN_POINT('Ctrl Pts',(-1.85655816608735,-1.58507364554545,
-1.90943497286695E-16));
#29291=CARTESIAN_POINT('Ctrl Pts',(-1.86951455362061,-1.57262038350302,
-1.1893963212715E-16));
#29292=CARTESIAN_POINT('Ctrl Pts',(-1.8823369229035,-1.56001375633204,-1.66533453693773E-16));
#29293=CARTESIAN_POINT('Ctrl Pts',(-1.89389529438543,-1.54864985963231,
-2.09435592742768E-16));
#29294=CARTESIAN_POINT('Ctrl Pts',(-1.90534102035706,-1.53716495022738,
3.49299600923418E-16));
#29295=CARTESIAN_POINT('Ctrl Pts',(-1.9166678489872,-1.52556749612954,3.05311331771918E-16));
#29296=CARTESIAN_POINT('Ctrl Pts',(-1.97639856958762,-1.46440966342857,
7.33442825493013E-17));
#29297=CARTESIAN_POINT('Ctrl Pts',(-2.03287303298855,-1.40007886819707,
-7.0183037565297E-16));
#29298=CARTESIAN_POINT('Ctrl Pts',(-2.08599777480493,-1.33296674038781,
-4.44089209850063E-16));
#29299=CARTESIAN_POINT('Ctrl Pts',(-2.13221332454416,-1.274582948301,-2.19868832287029E-16));
#29300=CARTESIAN_POINT('Ctrl Pts',(-2.17589371235756,-1.21409310252408,
-1.30713211170112E-16));
#29301=CARTESIAN_POINT('Ctrl Pts',(-2.21696145780543,-1.1517270622244,-1.2490009027033E-16));
#29302=CARTESIAN_POINT('Ctrl Pts',(-2.23761972751426,-1.12035513111075,
-1.21975921483168E-16));
#29303=CARTESIAN_POINT('Ctrl Pts',(-2.257616638896,-1.08850807754864,-6.50635459664472E-19));
#29304=CARTESIAN_POINT('Ctrl Pts',(-2.27694058302463,-1.05621312605931,
2.77555756156289E-17));
#29305=CARTESIAN_POINT('Ctrl Pts',(-2.28638312411741,-1.04043237216676,
4.16361174751555E-17));
#29306=CARTESIAN_POINT('Ctrl Pts',(-2.29566596401088,-1.0245426554578,-3.86134059335254E-16));
#29307=CARTESIAN_POINT('Ctrl Pts',(-2.30477629260578,-1.00856764802397,
-3.60822483003176E-16));
#29308=CARTESIAN_POINT('Ctrl Pts',(-2.34868382122166,-0.931575573728042,
-2.38832507500552E-16));
#29309=CARTESIAN_POINT('Ctrl Pts',(-2.38864775623492,-0.852506148187216,
7.6589648086775E-17));
#29310=CARTESIAN_POINT('Ctrl Pts',(-2.42457139730333,-0.771756361747471,
1.11022302462516E-16));
#29311=CARTESIAN_POINT('Ctrl Pts',(-2.46298089184026,-0.685418830559891,
1.47837636621387E-16));
#29312=CARTESIAN_POINT('Ctrl Pts',(-2.496772671788,-0.597159876911868,-2.6411927253517E-16));
#29313=CARTESIAN_POINT('Ctrl Pts',(-2.52578830996096,-0.5074153351261,-2.22044604925031E-16));
#29314=CARTESIAN_POINT('Ctrl Pts',(-2.54755003859068,-0.440106928786774,
-1.90488604217428E-16));
#29315=CARTESIAN_POINT('Ctrl Pts',(-2.56662441067748,-0.371961718591897,
-1.06288902356375E-16));
#29316=CARTESIAN_POINT('Ctrl Pts',(-2.58292557654155,-0.303150270529533,
-1.11022302462516E-16));
#29317=CARTESIAN_POINT('Ctrl Pts',(-2.5951514509396,-0.251541684482761,
-1.14572352542121E-16));
#29318=CARTESIAN_POINT('Ctrl Pts',(-2.60581707499254,-0.199558087757334,
-1.32861127945469E-16));
#29319=CARTESIAN_POINT('Ctrl Pts',(-2.61487919945664,-0.147268754493998,
-1.38777878078145E-16));
#29320=CARTESIAN_POINT('Ctrl Pts',(-2.61743940316675,-0.132496131854521,
-1.4044946024428E-16));
#29321=CARTESIAN_POINT('Ctrl Pts',(-2.61987158272419,-0.117699096439989,
-1.07679138130245E-16));
#29322=CARTESIAN_POINT('Ctrl Pts',(-2.62217466731863,-0.102879189619736,
-1.11022302462516E-16));
#29323=CARTESIAN_POINT('Ctrl Pts',(-2.62424692676471,-0.089544598275464,
-1.14030400334403E-16));
#29324=CARTESIAN_POINT('Ctrl Pts',(-2.62621322332593,-0.0762007531359675,
9.91403158685596E-17));
#29325=CARTESIAN_POINT('Ctrl Pts',(-2.62807300875564,-0.0628502760411497,
1.11022302462516E-16));
#29326=CARTESIAN_POINT('Ctrl Pts',(-2.64084702393496,0.0288480426655374,
1.92634231820763E-16));
#29327=CARTESIAN_POINT('Ctrl Pts',(-2.64860284780981,0.120877572624176,
2.34034299737326E-18));
#29328=CARTESIAN_POINT('Ctrl Pts',(-2.65120733482282,0.212843544851723,
-5.55111512312578E-17));
#29329=CARTESIAN_POINT('Ctrl Pts',(-2.65227730220756,0.250624724138807,
-7.92775250599356E-17));
#29330=CARTESIAN_POINT('Ctrl Pts',(-2.65247737800954,0.28839553131628,1.67382252759083E-16));
#29331=CARTESIAN_POINT('Ctrl Pts',(-2.65179610762442,0.326129846634779,
1.66533453693773E-16));
#29332=CARTESIAN_POINT('Ctrl Pts',(-2.65019510065319,0.41480668214537,1.65536101357303E-16));
#29333=CARTESIAN_POINT('Ctrl Pts',(-2.64373047396203,0.503281469119527,
3.1574695155968E-17));
#29334=CARTESIAN_POINT('Ctrl Pts',(-2.63264650872894,0.591292908473233,
5.55111512312578E-17));
#29335=CARTESIAN_POINT('Ctrl Pts',(-2.62134112159331,0.681062532730685,
7.99257805534553E-17));
#29336=CARTESIAN_POINT('Ctrl Pts',(-2.60522989313478,0.770350844351005,
-2.70863134523007E-16));
#29337=CARTESIAN_POINT('Ctrl Pts',(-2.58451809222978,0.858883818120269,
-4.16333634234434E-16));
#29338=CARTESIAN_POINT('Ctrl Pts',(-2.57994896726511,0.878414626788261,
-4.48425140661245E-16));
#29339=CARTESIAN_POINT('Ctrl Pts',(-2.57515574764109,0.897908663068738,
2.12915568004684E-16));
#29340=CARTESIAN_POINT('Ctrl Pts',(-2.57014030159083,0.917362948618063,
1.94289029309402E-16));
#29341=CARTESIAN_POINT('Ctrl Pts',(-2.56645391643843,0.931661973805637,
1.80598403391229E-16));
#29342=CARTESIAN_POINT('Ctrl Pts',(-2.56264940755798,0.945931896412831,
-2.32436284838826E-16));
#29343=CARTESIAN_POINT('Ctrl Pts',(-2.55872953347648,0.960165880107832,
-2.22044604925031E-16));
#29344=CARTESIAN_POINT('Ctrl Pts',(-2.53414545266093,1.04943645314397,-1.56871618880494E-16));
#29345=CARTESIAN_POINT('Ctrl Pts',(-2.50500995111573,1.13736326277131,-2.05141327217914E-17));
#29346=CARTESIAN_POINT('Ctrl Pts',(-2.4716122792232,1.22366382845986,-2.77555756156289E-17));
#29347=CARTESIAN_POINT('Ctrl Pts',(-2.4375744436594,1.31161859588862,-3.51358218572908E-17));
#29348=CARTESIAN_POINT('Ctrl Pts',(-2.39910931031647,1.39788496430102,-3.16197773120891E-16));
#29349=CARTESIAN_POINT('Ctrl Pts',(-2.35646765233004,1.48216671345376,-3.33066907387547E-16));
#29350=CARTESIAN_POINT('Ctrl Pts',(-2.31346972634883,1.56715263057712,-3.50076982061372E-16));
#29351=CARTESIAN_POINT('Ctrl Pts',(-2.26622490268864,1.65012150115931,-2.40346217807297E-16));
#29352=CARTESIAN_POINT('Ctrl Pts',(-2.21493810777665,1.7307598326539,-2.77555756156289E-16));
#29353=CARTESIAN_POINT('Ctrl Pts',(-2.18420890619665,1.77907541852398,-2.99850372277004E-16));
#29354=CARTESIAN_POINT('Ctrl Pts',(-2.15202766717645,1.82655410022214,-8.23577960215966E-17));
#29355=CARTESIAN_POINT('Ctrl Pts',(-2.11843029730051,1.87312475572319,-1.11022302462516E-16));
#29356=CARTESIAN_POINT('Ctrl Pts',(-2.10910817041026,1.88604652791983,-1.18975727604888E-16));
#29357=CARTESIAN_POINT('Ctrl Pts',(-2.09967596196574,1.89889961347673,3.5091792826265E-16));
#29358=CARTESIAN_POINT('Ctrl Pts',(-2.09014599464406,1.91166724455946,3.33066907387547E-16));
#29359=CARTESIAN_POINT('Ctrl Pts',(-2.03133578634427,1.99045734090759,2.22906796592623E-16));
#29360=CARTESIAN_POINT('Ctrl Pts',(-1.96871406102828,2.0661248657246,1.99254278682365E-16));
#29361=CARTESIAN_POINT('Ctrl Pts',(-1.902552599463,2.13836101844373,1.66533453693773E-16));
#29362=CARTESIAN_POINT('Ctrl Pts',(-1.8362287723598,2.21077444448052,1.33732329173934E-16));
#29363=CARTESIAN_POINT('Ctrl Pts',(-1.76634741320835,2.27974053651805,-4.02039597886661E-17));
#29364=CARTESIAN_POINT('Ctrl Pts',(-1.69313231821204,2.34493242732506,-5.55111512312578E-17));
#29365=CARTESIAN_POINT('Ctrl Pts',(-1.62133085597193,2.40886559693137,-7.05227923200634E-17));
#29366=CARTESIAN_POINT('Ctrl Pts',(-1.54632261932841,2.46916967164754,2.95537804665533E-16));
#29367=CARTESIAN_POINT('Ctrl Pts',(-1.46827783385673,2.52550895680454,3.33066907387547E-16));
#29368=CARTESIAN_POINT('Ctrl Pts',(-1.41015813731654,2.56746463823574,3.6101470746729E-16));
#29369=CARTESIAN_POINT('Ctrl Pts',(-1.35035358675696,2.60722107009064,1.43731543267252E-17));
#29370=CARTESIAN_POINT('Ctrl Pts',(-1.28892185405322,2.64462557919718,0.));
#29371=CARTESIAN_POINT('Origin',(0.,0.,0.));
#29372=CARTESIAN_POINT('Origin',(-1.44337567297407,-2.5,-6.));
#29373=CARTESIAN_POINT('',(-1.44337567297407,-2.5,-6.));
#29374=CARTESIAN_POINT('',(1.44337567297406,-2.5,-6.));
#29375=CARTESIAN_POINT('',(-0.721687836487033,-2.5,-6.));
#29376=CARTESIAN_POINT('',(-1.44337567297407,-2.5,-3.));
#29377=CARTESIAN_POINT('',(-1.44337567297407,-2.5,-6.));
#29378=CARTESIAN_POINT('',(1.44337567297406,-2.5,-3.));
#29379=CARTESIAN_POINT('',(-1.44337567297407,-2.5,-3.));
#29380=CARTESIAN_POINT('',(1.44337567297406,-2.5,-6.));
#29381=CARTESIAN_POINT('Origin',(-2.88675134594813,3.53525079574969E-16,
-6.));
#29382=CARTESIAN_POINT('',(-2.88675134594813,3.53525079574969E-16,-6.));
#29383=CARTESIAN_POINT('',(-2.52590742770461,-0.625,-6.));
#29384=CARTESIAN_POINT('',(-2.88675134594813,5.55111512312578E-16,-3.));
#29385=CARTESIAN_POINT('',(-2.88675134594813,3.53525079574969E-16,-6.));
#29386=CARTESIAN_POINT('',(-2.88675134594813,3.53525079574969E-16,-3.));
#29387=CARTESIAN_POINT('Origin',(-1.44337567297406,2.5,-6.));
#29388=CARTESIAN_POINT('',(-1.44337567297406,2.5,-6.));
#29389=CARTESIAN_POINT('',(-1.80421959121758,1.875,-6.));
#29390=CARTESIAN_POINT('',(-1.44337567297406,2.5,-3.));
#29391=CARTESIAN_POINT('',(-1.44337567297406,2.5,-6.));
#29392=CARTESIAN_POINT('',(-1.44337567297406,2.5,-3.));
#29393=CARTESIAN_POINT('Origin',(1.44337567297406,2.5,-6.));
#29394=CARTESIAN_POINT('',(1.44337567297406,2.5,-6.));
#29395=CARTESIAN_POINT('',(0.721687836487033,2.5,-6.));
#29396=CARTESIAN_POINT('',(1.44337567297406,2.5,-3.));
#29397=CARTESIAN_POINT('',(1.44337567297406,2.5,-6.));
#29398=CARTESIAN_POINT('',(1.44337567297406,2.5,-3.));
#29399=CARTESIAN_POINT('Origin',(2.88675134594813,0.,-6.));
#29400=CARTESIAN_POINT('',(2.88675134594813,0.,-6.));
#29401=CARTESIAN_POINT('',(2.52590742770461,0.625,-6.));
#29402=CARTESIAN_POINT('',(2.88675134594813,0.,-3.));
#29403=CARTESIAN_POINT('',(2.88675134594813,0.,-6.));
#29404=CARTESIAN_POINT('',(2.88675134594813,0.,-3.));
#29405=CARTESIAN_POINT('Origin',(1.44337567297406,-2.5,-6.));
#29406=CARTESIAN_POINT('',(1.80421959121758,-1.875,-6.));
#29407=CARTESIAN_POINT('',(1.44337567297406,-2.5,-3.));
#29408=CARTESIAN_POINT('Origin',(0.,0.,-3.));
#29409=CARTESIAN_POINT('Origin',(0.,0.,0.));
#29410=CARTESIAN_POINT('',(-5.,-6.12323399573677E-16,0.));
#29411=CARTESIAN_POINT('Origin',(0.,0.,0.));
#29412=CARTESIAN_POINT('Origin',(0.,0.,-6.));
#29413=CARTESIAN_POINT('',(-5.,-6.12323399573677E-16,-6.));
#29414=CARTESIAN_POINT('',(-5.,-6.12323399573677E-16,-6.));
#29415=CARTESIAN_POINT('Origin',(0.,0.,-6.));
#29416=CARTESIAN_POINT('Origin',(0.,0.,-6.));
#29417=CARTESIAN_POINT('Origin',(0.,0.,20.));
#32603=UNCERTAINTY_MEASURE_WITH_UNIT(LENGTH_MEASURE(0.01),#32628,
'DISTANCE_ACCURACY_VALUE',
'Maximum model space distance between geometric entities at asserted c
onnectivities');
#32607=UNCERTAINTY_MEASURE_WITH_UNIT(LENGTH_MEASURE(0.01),#32628,
'DISTANCE_ACCURACY_VALUE',
'Maximum model space distance between geometric entities at asserted c
onnectivities');
#32623=(
GEOMETRIC_REPRESENTATION_CONTEXT(3)
GLOBAL_UNCERTAINTY_ASSIGNED_CONTEXT((#32603))
GLOBAL_UNIT_ASSIGNED_CONTEXT((#32628,#32630,#32631))
REPRESENTATION_CONTEXT('','3D')
);
#32627=(
GEOMETRIC_REPRESENTATION_CONTEXT(3)
GLOBAL_UNCERTAINTY_ASSIGNED_CONTEXT((#32607))
GLOBAL_UNIT_ASSIGNED_CONTEXT((#32628,#32630,#32631))
REPRESENTATION_CONTEXT('','3D')
);
#32628=(
LENGTH_UNIT()
NAMED_UNIT(*)
SI_UNIT(.MILLI.,.METRE.)
);
#32630=(
NAMED_UNIT(*)
PLANE_ANGLE_UNIT()
SI_UNIT($,.RADIAN.)
);
#32631=(
NAMED_UNIT(*)
SI_UNIT($,.STERADIAN.)
SOLID_ANGLE_UNIT()
);
#32647=SHAPE_DEFINITION_REPRESENTATION(#32666,#32722);
#32666=PRODUCT_DEFINITION_SHAPE('',$,#32742);
#32722=SHAPE_REPRESENTATION('',(#9354),#32623);
#32726=PRODUCT_DEFINITION_CONTEXT('part definition',#32785,'design');
#32742=PRODUCT_DEFINITION('Socket head cap screw M6x20',
'Socket head cap screw M6x20',#32761,#32726);
#32761=PRODUCT_DEFINITION_FORMATION('',$,#32802);
#32785=APPLICATION_CONTEXT(
'Core Data for Automotive Mechanical Design Process');
#32786=PRODUCT_CONTEXT('part definition',#32785,'mechanical');
#32802=PRODUCT('Socket head cap screw M6x20',
'Socket head cap screw M6x20',$,(#32786));
#32809=PRESENTATION_STYLE_ASSIGNMENT((#32816));
#32816=SURFACE_STYLE_USAGE(.BOTH.,#32823);
#32823=SURFACE_SIDE_STYLE('',(#32830));
#32830=SURFACE_STYLE_FILL_AREA(#32837);
#32837=FILL_AREA_STYLE('Dark gray',(#32844));
#32844=FILL_AREA_STYLE_COLOUR('Dark gray',#32851);
#32851=COLOUR_RGB('Dark gray',0.250980392156863,0.282352941176471,0.32156862745098);
ENDSEC;
END-ISO-10303-21;
